ISO-10303-21;
HEADER;
FILE_DESCRIPTION (('STEP AP214'),
    '1' );
FILE_NAME ('hex screw gradec_din_DIN EN 24018 - M10 x 40-WS.step',
    '2026-10-09T14:04:53',
    ( '' ),
    ( '' ),
    'SwSTEP 2.0',
    'SolidWorks 2021',
    '' );
FILE_SCHEMA (( 'AUTOMOTIVE_DESIGN' ));
ENDSEC;

DATA;
#77=CARTESIAN_POINT ( 'NONE',  ( 9.250997389131581983, 1.340359594676612611E-15, 0.000000000000000000 ) ) ;
#168=CONICAL_SURFACE ( 'NONE', #3618, 4.172000000000001485, 0.9599310885968750373 ) ;
#226=AXIS2_PLACEMENT_3D ( 'NONE', #49892, #10498, #83857 ) ;
#302=EDGE_LOOP ( 'NONE', ( #4266, #95495, #92686, #39494, #82857, #4404 ) ) ;
#303=ADVANCED_FACE ( 'NONE', ( #91748 ), #25570, .T. ) ;
#308=DIRECTION ( 'NONE',  ( -0.5735764363510512664, 0.8191520442889881348, 1.003171929053520309E-16 ) ) ;
#332=DIRECTION ( 'NONE',  ( -1.000000000000000000, -1.224606353822377258E-16, -0.000000000000000000 ) ) ;
#385=CARTESIAN_POINT ( 'NONE',  ( 14.27307692307692299, -4.171999999999999709, 0.000000000000000000 ) ) ;
#403=FACE_OUTER_BOUND ( 'NONE', #11304, .T. ) ;
#448=FACE_OUTER_BOUND ( 'NONE', #50951, .T. ) ;
#497=AXIS2_PLACEMENT_3D ( 'NONE', #11558, #44489, #45027 ) ;
#498=LINE ( 'NONE', #24845, #77218 ) ;
#516=EDGE_CURVE ( 'NONE', #54910, #26965, #77693, .T. ) ;
#527=ORIENTED_EDGE ( 'NONE', *, *, #13782, .T. ) ;
#530=DIRECTION ( 'NONE',  ( -0.5735764363510512664, 0.8191520442889881348, 1.003171929053520309E-16 ) ) ;
#555=DIRECTION ( 'NONE',  ( -1.000000000000000000, -1.224606353822377258E-16, -0.000000000000000000 ) ) ;
#578=CARTESIAN_POINT ( 'NONE',  ( 16.33361799548379523, 1.482358050883964840E-15, 0.000000000000000000 ) ) ;
#625=CARTESIAN_POINT ( 'NONE',  ( 14.27307692307692299, 4.172000000000003261, 0.000000000000000000 ) ) ;
#626=CARTESIAN_POINT ( 'NONE',  ( 15.17407431220850533, 1.340359594676612611E-15, 0.000000000000000000 ) ) ;
#627=ORIENTED_EDGE ( 'NONE', *, *, #74226, .F. ) ;
#635=CARTESIAN_POINT ( 'NONE',  ( 7.770228158362351145, -1.925929944387235853E-31, 5.000000000000002665 ) ) ;
#667=FACE_OUTER_BOUND ( 'NONE', #72152, .T. ) ;
#692=EDGE_LOOP ( 'NONE', ( #73594, #52506, #89356, #104672, #50248 ) ) ;
#726=AXIS2_PLACEMENT_3D ( 'NONE', #94977, #36763, #4887 ) ;
#734=CIRCLE ( 'NONE', #59380, 5.000000000000001776 ) ;
#752=ORIENTED_EDGE ( 'NONE', *, *, #96773, .F. ) ;
#755=ORIENTED_EDGE ( 'NONE', *, *, #93443, .F. ) ;
#776=DIRECTION ( 'NONE',  ( 0.000000000000000000, 0.000000000000000000, 1.000000000000000000 ) ) ;
#807=EDGE_CURVE ( 'NONE', #32720, #23780, #96223, .T. ) ;
#831=CIRCLE ( 'NONE', #81768, 5.000000000000002665 ) ;
#856=AXIS2_PLACEMENT_3D ( 'NONE', #13280, #12756, #60808 ) ;
#860=DIRECTION ( 'NONE',  ( -1.000000000000000000, -1.224606353822377258E-16, -0.000000000000000000 ) ) ;
#899=EDGE_CURVE ( 'NONE', #9931, #76623, #63269, .T. ) ;
#910=EDGE_CURVE ( 'NONE', #58651, #47940, #97897, .T. ) ;
#915=CARTESIAN_POINT ( 'NONE',  ( 0.4973051450610691537, -3.866309095671421669, -8.000000000000001776 ) ) ;
#931=DIRECTION ( 'NONE',  ( 0.000000000000000000, -1.000000000000000000, 0.000000000000000000 ) ) ;
#933=ORIENTED_EDGE ( 'NONE', *, *, #61001, .T. ) ;
#997=ORIENTED_EDGE ( 'NONE', *, *, #16088, .F. ) ;
#1017=DIRECTION ( 'NONE',  ( -1.000000000000000000, -1.224606353822377258E-16, -0.000000000000000000 ) ) ;
#1023=FACE_OUTER_BOUND ( 'NONE', #27594, .T. ) ;
#1028=AXIS2_PLACEMENT_3D ( 'NONE', #14538, #72264, #28810 ) ;
#1037=EDGE_LOOP ( 'NONE', ( #8175, #51723, #94062, #91131, #68624 ) ) ;
#1048=VECTOR ( 'NONE', #46311, 1000.000000000000000 ) ;
#1064=CARTESIAN_POINT ( 'NONE',  ( 9.250997389131581983, 1.340359594676612611E-15, 0.000000000000000000 ) ) ;
#1070=EDGE_CURVE ( 'NONE', #86142, #96901, #21475, .T. ) ;
#1081=DIRECTION ( 'NONE',  ( 0.000000000000000000, -1.000000000000000000, 0.000000000000000000 ) ) ;
#1087=ORIENTED_EDGE ( 'NONE', *, *, #4626, .T. ) ;
#1088=ORIENTED_EDGE ( 'NONE', *, *, #51547, .T. ) ;
#1107=ORIENTED_EDGE ( 'NONE', *, *, #6750, .F. ) ;
#1123=DIRECTION ( 'NONE',  ( -1.000000000000000000, -1.224606353822377258E-16, -0.000000000000000000 ) ) ;
#1127=DIRECTION ( 'NONE',  ( -1.000000000000000000, -1.224606353822377258E-16, -0.000000000000000000 ) ) ;
#1153=ORIENTED_EDGE ( 'NONE', *, *, #98100, .T. ) ;
#1253=EDGE_CURVE ( 'NONE', #84621, #81027, #106601, .T. ) ;
#1266=CIRCLE ( 'NONE', #102861, 8.000000000000000000 ) ;
#1275=FACE_OUTER_BOUND ( 'NONE', #82360, .T. ) ;
#1301=EDGE_CURVE ( 'NONE', #72256, #53057, #78955, .T. ) ;
#1334=CONICAL_SURFACE ( 'NONE', #70289, 4.172000000000001485, 0.9599310885968750373 ) ;
#1342=EDGE_CURVE ( 'NONE', #27470, #31549, #77439, .T. ) ;
#1380=ORIENTED_EDGE ( 'NONE', *, *, #50736, .F. ) ;
#1405=CARTESIAN_POINT ( 'NONE',  ( 27.02022815836235026, 5.000000000000004441, 6.123233995736770227E-16 ) ) ;
#1427=AXIS2_PLACEMENT_3D ( 'NONE', #11060, #73010, #21864 ) ;
#1430=AXIS2_PLACEMENT_3D ( 'NONE', #49604, #72807, #41516 ) ;
#1443=DIRECTION ( 'NONE',  ( -1.000000000000000000, -1.224606353822377258E-16, -0.000000000000000000 ) ) ;
#1476=FACE_OUTER_BOUND ( 'NONE', #103523, .T. ) ;
#1523=ADVANCED_FACE ( 'NONE', ( #46142 ), #49156, .F. ) ;
#1563=VECTOR ( 'NONE', #93447, 1000.000000000000000 ) ;
#1576=EDGE_CURVE ( 'NONE', #43900, #49621, #104578, .T. ) ;
#1618=VERTEX_POINT ( 'NONE', #100378 ) ;
#1622=AXIS2_PLACEMENT_3D ( 'NONE', #22279, #78353, #70278 ) ;
#1665=ORIENTED_EDGE ( 'NONE', *, *, #86180, .T. ) ;
#1686=VERTEX_POINT ( 'NONE', #17893 ) ;
#1714=ADVANCED_FACE ( 'NONE', ( #83651 ), #83964, .T. ) ;
#1723=AXIS2_PLACEMENT_3D ( 'NONE', #90274, #56829, #76068 ) ;
#1768=EDGE_CURVE ( 'NONE', #52464, #53278, #44388, .T. ) ;
#1787=CARTESIAN_POINT ( 'NONE',  ( 23.73746414932995208, 1.482358050883964840E-15, 0.000000000000000000 ) ) ;
#1807=ORIENTED_EDGE ( 'NONE', *, *, #14201, .F. ) ;
#1824=EDGE_LOOP ( 'NONE', ( #9401, #76936, #1087, #43914, #53407 ) ) ;
#1827=CARTESIAN_POINT ( 'NONE',  ( 37.06438722625302518, 1.482358050883964840E-15, 0.000000000000000000 ) ) ;
#1843=LINE ( 'NONE', #42852, #91545 ) ;
#1849=ADVANCED_FACE ( 'NONE', ( #36760 ), #102980, .T. ) ;
#1873=CARTESIAN_POINT ( 'NONE',  ( 13.37207953394533355, 1.482358050883964840E-15, 0.000000000000000000 ) ) ;
#1877=VECTOR ( 'NONE', #23294, 999.9999999999998863 ) ;
#1879=DIRECTION ( 'NONE',  ( 0.000000000000000000, -1.000000000000000000, 0.000000000000000000 ) ) ;
#1882=DIRECTION ( 'NONE',  ( 1.734723475976806108E-16, -1.000000000000000000, 0.000000000000000000 ) ) ;
#1900=EDGE_CURVE ( 'NONE', #76623, #55395, #20051, .T. ) ;
#1912=ORIENTED_EDGE ( 'NONE', *, *, #68254, .F. ) ;
#1925=AXIS2_PLACEMENT_3D ( 'NONE', #36403, #11524, #44452 ) ;
#1955=DIRECTION ( 'NONE',  ( 0.000000000000000000, -1.000000000000000000, 0.000000000000000000 ) ) ;
#1987=DIRECTION ( 'NONE',  ( 0.000000000000000000, 0.000000000000000000, -1.000000000000000000 ) ) ;
#2007=AXIS2_PLACEMENT_3D ( 'NONE', #42460, #85062, #66747 ) ;
#2014=CARTESIAN_POINT ( 'NONE',  ( 38.86638200451619696, 1.340359594676612611E-15, 0.000000000000000000 ) ) ;
#2025=VERTEX_POINT ( 'NONE', #42013 ) ;
#2035=EDGE_LOOP ( 'NONE', ( #19354, #16414, #90087, #17768, #101633 ) ) ;
#2041=DIRECTION ( 'NONE',  ( 0.000000000000000000, -1.000000000000000000, 0.000000000000000000 ) ) ;
#2069=ORIENTED_EDGE ( 'NONE', *, *, #43770, .T. ) ;
#2096=CARTESIAN_POINT ( 'NONE',  ( 32.04230769230768772, 1.411358822780289120E-15, 0.000000000000000000 ) ) ;
#2106=ORIENTED_EDGE ( 'NONE', *, *, #75155, .T. ) ;
#2117=CARTESIAN_POINT ( 'NONE',  ( 0.000000000000000000, 0.000000000000000000, 0.000000000000000000 ) ) ;
#2125=FILL_AREA_STYLE ('',( #34020 ) ) ;
#2211=CARTESIAN_POINT ( 'NONE',  ( 14.85284876471456350, -5.000000000000000000, 6.123233995736768255E-16 ) ) ;
#2234=VERTEX_POINT ( 'NONE', #89917 ) ;
#2235=DIRECTION ( 'NONE',  ( -1.000000000000000000, -0.000000000000000000, -0.000000000000000000 ) ) ;
#2249=DIRECTION ( 'NONE',  ( 0.000000000000000000, 0.000000000000000000, 1.000000000000000000 ) ) ;
#2256=ORIENTED_EDGE ( 'NONE', *, *, #36061, .F. ) ;
#2259=VECTOR ( 'NONE', #85723, 1000.000000000000000 ) ;
#2271=ORIENTED_EDGE ( 'NONE', *, *, #75007, .F. ) ;
#2275=EDGE_CURVE ( 'NONE', #22430, #60654, #61658, .T. ) ;
#2276=CARTESIAN_POINT ( 'NONE',  ( 46.85000000000000142, 5.109226446042757607E-16, -4.171999999999999709 ) ) ;
#2281=DIRECTION ( 'NONE',  ( 1.000000000000000000, 0.000000000000000000, 0.000000000000000000 ) ) ;
#2294=CONICAL_SURFACE ( 'NONE', #16094, 5.000000000000001776, 0.9599310885968803664 ) ;
#2307=EDGE_CURVE ( 'NONE', #85900, #31075, #15125, .T. ) ;
#2328=VECTOR ( 'NONE', #32417, 1000.000000000000000 ) ;
#2351=ORIENTED_EDGE ( 'NONE', *, *, #65543, .T. ) ;
#2372=CARTESIAN_POINT ( 'NONE',  ( 40.02592568779148507, 5.000000000000002665, 0.000000000000000000 ) ) ;
#2373=DIRECTION ( 'NONE',  ( 0.000000000000000000, -1.000000000000000000, 0.000000000000000000 ) ) ;
#2385=AXIS2_PLACEMENT_3D ( 'NONE', #20676, #104174, #78839 ) ;
#2432=ORIENTED_EDGE ( 'NONE', *, *, #64318, .F. ) ;
#2451=ORIENTED_EDGE ( 'NONE', *, *, #8287, .F. ) ;
#2463=DIRECTION ( 'NONE',  ( 1.000000000000000000, 0.000000000000000000, 0.000000000000000000 ) ) ;
#2494=VERTEX_POINT ( 'NONE', #52637 ) ;
#2496=PRODUCT_DEFINITION_FORMATION_WITH_SPECIFIED_SOURCE ( 'ANY', '', #75968, .NOT_KNOWN. ) ;
#2545=CARTESIAN_POINT ( 'NONE',  ( 17.81438722625302518, 1.482358050883964840E-15, 0.000000000000000000 ) ) ;
#2546=CIRCLE ( 'NONE', #57651, 5.000000000000002665 ) ;
#2566=VERTEX_POINT ( 'NONE', #68855 ) ;
#2574=CARTESIAN_POINT ( 'NONE',  ( 23.73746414932995208, 6.123233995736772199E-16, -5.000000000000001776 ) ) ;
#2627=VERTEX_POINT ( 'NONE', #22442 ) ;
#2637=CONICAL_SURFACE ( 'NONE', #73229, 4.172000000000001485, 0.9599310885968750373 ) ;
#2638=CARTESIAN_POINT ( 'NONE',  ( 31.46253585067004721, 4.999999999999994671, 6.123233995736758394E-16 ) ) ;
#2644=DIRECTION ( 'NONE',  ( -1.000000000000000000, -1.224606353822377258E-16, -0.000000000000000000 ) ) ;
#2653=ORIENTED_EDGE ( 'NONE', *, *, #45199, .F. ) ;
#2677=CONICAL_SURFACE ( 'NONE', #11288, 8.000000000000000000, 1.047197551196600296 ) ;
#2685=ORIENTED_EDGE ( 'NONE', *, *, #14362, .T. ) ;
#2686=DIRECTION ( 'NONE',  ( -1.000000000000000000, -1.224606353822377258E-16, -0.000000000000000000 ) ) ;
#2688=CARTESIAN_POINT ( 'NONE',  ( 11.31153846153846132, -4.171999999999999709, 0.000000000000000000 ) ) ;
#2694=CARTESIAN_POINT ( 'NONE',  ( 34.10284876471455817, 6.123233995736772199E-16, -5.000000000000001776 ) ) ;
#2699=DIRECTION ( 'NONE',  ( -1.000000000000000000, -1.224606353822377258E-16, -0.000000000000000000 ) ) ;
#2706=DIRECTION ( 'NONE',  ( -1.000000000000000000, -1.224606353822377258E-16, -0.000000000000000000 ) ) ;
#2717=ORIENTED_EDGE ( 'NONE', *, *, #21402, .F. ) ;
#2734=ORIENTED_EDGE ( 'NONE', *, *, #52484, .F. ) ;
#2746=AXIS2_PLACEMENT_3D ( 'NONE', #28991, #37062, #54782 ) ;
#2753=DIRECTION ( 'NONE',  ( -1.000000000000000000, -0.000000000000000000, -0.000000000000000000 ) ) ;
#2763=AXIS2_PLACEMENT_3D ( 'NONE', #105700, #25226, #91008 ) ;
#2772=ORIENTED_EDGE ( 'NONE', *, *, #33202, .T. ) ;
#2823=VECTOR ( 'NONE', #83219, 999.9999999999998863 ) ;
#2869=CARTESIAN_POINT ( 'NONE',  ( 11.89131030317610183, 1.482358050883964840E-15, 0.000000000000000000 ) ) ;
#2875=CARTESIAN_POINT ( 'NONE',  ( 41.50669491856072568, 5.000000000000002665, 0.000000000000000000 ) ) ;
#2909=ORIENTED_EDGE ( 'NONE', *, *, #91249, .F. ) ;
#2911=FACE_OUTER_BOUND ( 'NONE', #70556, .T. ) ;
#2931=EDGE_CURVE ( 'NONE', #52425, #96464, #4502, .T. ) ;
#2935=CARTESIAN_POINT ( 'NONE',  ( 29.08076923076923137, 1.411358822780289120E-15, 0.000000000000000000 ) ) ;
#2940=DIRECTION ( 'NONE',  ( 0.000000000000000000, -1.000000000000000000, 0.000000000000000000 ) ) ;
#2954=AXIS2_PLACEMENT_3D ( 'NONE', #68956, #94281, #4204 ) ;
#2974=DIRECTION ( 'NONE',  ( 1.000000000000000000, 1.224606353822377258E-16, 0.000000000000000000 ) ) ;
#2987=DIRECTION ( 'NONE',  ( -0.5735764363510510444, -0.8191520442889883569, 0.000000000000000000 ) ) ;
#2992=AXIS2_PLACEMENT_3D ( 'NONE', #9193, #58842, #1081 ) ;
#2993=AXIS2_PLACEMENT_3D ( 'NONE', #33026, #81514, #9236 ) ;
#2994=CYLINDRICAL_SURFACE ( 'NONE', #45972, 5.000000000000002665 ) ;
#2999=DIRECTION ( 'NONE',  ( -0.5735764363510512664, 0.8191520442889881348, 1.003171929053520309E-16 ) ) ;
#3026=CIRCLE ( 'NONE', #46156, 5.000000000000002665 ) ;
#3051=VERTEX_POINT ( 'NONE', #79967 ) ;
#3059=ORIENTED_EDGE ( 'NONE', *, *, #40415, .T. ) ;
#3082=ADVANCED_FACE ( 'NONE', ( #47597 ), #47902, .T. ) ;
#3092=CARTESIAN_POINT ( 'NONE',  ( 0.000000000000000000, 0.000000000000000000, 0.000000000000000000 ) ) ;
#3094=AXIS2_PLACEMENT_3D ( 'NONE', #80471, #7116, #97192 ) ;
#3105=FACE_OUTER_BOUND ( 'NONE', #16111, .T. ) ;
#3109=EDGE_CURVE ( 'NONE', #6957, #89827, #80638, .T. ) ;
#3113=EDGE_LOOP ( 'NONE', ( #74997, #77625, #9958, #10789, #7746 ) ) ;
#3148=ORIENTED_EDGE ( 'NONE', *, *, #34199, .F. ) ;
#3151=CARTESIAN_POINT ( 'NONE',  ( 0.000000000000000000, 6.123233995736770227E-16, -5.000000000000002665 ) ) ;
#3152=VECTOR ( 'NONE', #87057, 1000.000000000000000 ) ;
#3154=CARTESIAN_POINT ( 'NONE',  ( 8.929771841637641927, 5.000000000000003553, 0.000000000000000000 ) ) ;
#3171=EDGE_LOOP ( 'NONE', ( #74284, #98708, #71481, #35631, #68430 ) ) ;
#3180=DIRECTION ( 'NONE',  ( -1.000000000000000000, -1.224606353822377258E-16, -0.000000000000000000 ) ) ;
#3250=CARTESIAN_POINT ( 'NONE',  ( 37.38561277374697056, 6.123233995736770227E-16, -5.000000000000002665 ) ) ;
#3257=VERTEX_POINT ( 'NONE', #76129 ) ;
#3280=ORIENTED_EDGE ( 'NONE', *, *, #13425, .F. ) ;
#3307=VECTOR ( 'NONE', #30858, 1000.000000000000227 ) ;
#3317=AXIS2_PLACEMENT_3D ( 'NONE', #18814, #17717, #2041 ) ;
#3319=ORIENTED_EDGE ( 'NONE', *, *, #17107, .T. ) ;
#3371=CONICAL_SURFACE ( 'NONE', #68836, 4.172000000000001485, 0.9599310885968750373 ) ;
#3426=ORIENTED_EDGE ( 'NONE', *, *, #105196, .T. ) ;
#3434=CARTESIAN_POINT ( 'NONE',  ( 30.56153846153846132, -4.171999999999999709, 5.616230220889763424E-16 ) ) ;
#3480=ADVANCED_FACE ( 'NONE', ( #35384 ), #66597, .T. ) ;
#3482=CIRCLE ( 'NONE', #48267, 5.000000000000002665 ) ;
#3488=CARTESIAN_POINT ( 'NONE',  ( 29.66054107240687543, 5.000000000000002665, 0.000000000000000000 ) ) ;
#3493=ORIENTED_EDGE ( 'NONE', *, *, #101233, .T. ) ;
#3494=AXIS2_PLACEMENT_3D ( 'NONE', #30252, #64725, #46423 ) ;
#3496=CARTESIAN_POINT ( 'NONE',  ( 6.849999999999999645, 6.123233995736770227E-16, -5.000000000000002665 ) ) ;
#3505=CIRCLE ( 'NONE', #68963, 4.172000000000001485 ) ;
#3514=ORIENTED_EDGE ( 'NONE', *, *, #45773, .T. ) ;
#3522=DIRECTION ( 'NONE',  ( 0.000000000000000000, -1.000000000000000000, 0.000000000000000000 ) ) ;
#3524=DIRECTION ( 'NONE',  ( -1.000000000000000000, -0.000000000000000000, -0.000000000000000000 ) ) ;
#3544=CARTESIAN_POINT ( 'NONE',  ( 0.000000000000000000, 0.000000000000000000, 0.000000000000000000 ) ) ;
#3548=CARTESIAN_POINT ( 'NONE',  ( 20.77592568779148863, 1.482358050883964840E-15, 0.000000000000000000 ) ) ;
#3564=B_SPLINE_CURVE_WITH_KNOTS ( 'NONE', 3,
 ( #82944, #48960, #9042, #43025, #915, #34962 ),
 .UNSPECIFIED., .F., .F.,
 ( 4, 2, 4 ),
 ( 0.02753256083616404531, 0.02987018135583072859, 0.03220780187549741186 ),
 .UNSPECIFIED. ) ;
#3591=EDGE_LOOP ( 'NONE', ( #104513, #19307, #67025, #28616, #102805, #31099 ) ) ;
#3618=AXIS2_PLACEMENT_3D ( 'NONE', #103862, #46696, #81174 ) ;
#3629=CIRCLE ( 'NONE', #75909, 4.172000000000001485 ) ;
#3649=CIRCLE ( 'NONE', #84638, 5.000000000000001776 ) ;
#3658=CONICAL_SURFACE ( 'NONE', #53537, 4.172000000000001485, 0.9599310885968750373 ) ;
#3669=ORIENTED_EDGE ( 'NONE', *, *, #72906, .T. ) ;
#3686=EDGE_CURVE ( 'NONE', #36949, #61957, #53132, .T. ) ;
#3696=CARTESIAN_POINT ( 'NONE',  ( 37.96538461538461462, 4.172000000000003261, 5.109226446042759579E-16 ) ) ;
#3708=DIRECTION ( 'NONE',  ( -1.000000000000000000, -1.224606353822377258E-16, -0.000000000000000000 ) ) ;
#3756=AXIS2_PLACEMENT_3D ( 'NONE', #79920, #6028, #93995 ) ;
#3761=FACE_OUTER_BOUND ( 'NONE', #78513, .T. ) ;
#3776=EDGE_CURVE ( 'NONE', #106154, #95649, #42564, .T. ) ;
#3802=CARTESIAN_POINT ( 'NONE',  ( 28.17977184163764193, 5.000000000000003553, 0.000000000000000000 ) ) ;
#3848=CARTESIAN_POINT ( 'NONE',  ( 0.000000000000000000, 0.000000000000000000, 8.000000000000000000 ) ) ;
#3862=CARTESIAN_POINT ( 'NONE',  ( 46.02200000000003399, 6.123233995736772199E-16, -5.000000000000004441 ) ) ;
#3865=EDGE_CURVE ( 'NONE', #23643, #26151, #77064, .T. ) ;
#3867=LINE ( 'NONE', #46444, #19090 ) ;
#3885=CARTESIAN_POINT ( 'NONE',  ( 6.249999999999998224, 8.000000000000000000, 0.000000000000000000 ) ) ;
#3888=CARTESIAN_POINT ( 'NONE',  ( 0.000000000000000000, 0.000000000000000000, 0.000000000000000000 ) ) ;
#3925=CARTESIAN_POINT ( 'NONE',  ( 0.000000000000000000, 6.123233995736770227E-16, -5.000000000000002665 ) ) ;
#3951=AXIS2_PLACEMENT_3D ( 'NONE', #9451, #90393, #49382 ) ;
#3958=CIRCLE ( 'NONE', #15953, 5.000000000000001776 ) ;
#3966=DIRECTION ( 'NONE',  ( 0.000000000000000000, -1.000000000000000000, 0.000000000000000000 ) ) ;
#3971=CYLINDRICAL_SURFACE ( 'NONE', #82703, 5.000000000000002665 ) ;
#4002=VERTEX_POINT ( 'NONE', #30197 ) ;
#4016=EDGE_CURVE ( 'NONE', #9392, #61254, #104056, .T. ) ;
#4019=CIRCLE ( 'NONE', #64309, 5.000000000000001776 ) ;
#4029=ORIENTED_EDGE ( 'NONE', *, *, #33718, .F. ) ;
#4042=VERTEX_POINT ( 'NONE', #80301 ) ;
#4051=AXIS2_PLACEMENT_3D ( 'NONE', #100580, #82808, #26741 ) ;
#4053=CARTESIAN_POINT ( 'NONE',  ( 31.14131030317610538, 1.482358050883964840E-15, 0.000000000000000000 ) ) ;
#4067=FACE_OUTER_BOUND ( 'NONE', #6089, .T. ) ;
#4073=CYLINDRICAL_SURFACE ( 'NONE', #89190, 5.000000000000002665 ) ;
#4096=DIRECTION ( 'NONE',  ( 0.000000000000000000, 0.000000000000000000, 1.000000000000000000 ) ) ;
#4122=EDGE_CURVE ( 'NONE', #54910, #33830, #73652, .T. ) ;
#4146=CARTESIAN_POINT ( 'NONE',  ( 8.349999999999999645, -4.171999999999999709, 5.616230220889763424E-16 ) ) ;
#4157=CARTESIAN_POINT ( 'NONE',  ( 0.000000000000000000, 6.123233995736770227E-16, -5.000000000000002665 ) ) ;
#4181=LINE ( 'NONE', #53268, #57851 ) ;
#4204=DIRECTION ( 'NONE',  ( 0.000000000000000000, -1.000000000000000000, 0.000000000000000000 ) ) ;
#4230=ORIENTED_EDGE ( 'NONE', *, *, #1342, .F. ) ;
#4236=EDGE_CURVE ( 'NONE', #67515, #56640, #44350, .T. ) ;
#4241=CONICAL_SURFACE ( 'NONE', #30052, 4.172000000000001485, 0.9599310885968750373 ) ;
#4244=CIRCLE ( 'NONE', #104159, 5.000000000000002665 ) ;
#4266=ORIENTED_EDGE ( 'NONE', *, *, #15158, .F. ) ;
#4270=CARTESIAN_POINT ( 'NONE',  ( 45.36923076923077502, 1.411358822780289120E-15, 0.000000000000000000 ) ) ;
#4271=ORIENTED_EDGE ( 'NONE', *, *, #55132, .T. ) ;
#4298=ORIENTED_EDGE ( 'NONE', *, *, #76053, .T. ) ;
#4301=ORIENTED_EDGE ( 'NONE', *, *, #58791, .T. ) ;
#4306=DIRECTION ( 'NONE',  ( -1.000000000000000000, -1.224606353822377258E-16, -0.000000000000000000 ) ) ;
#4337=VERTEX_POINT ( 'NONE', #20433 ) ;
#4351=CARTESIAN_POINT ( 'NONE',  ( 0.000000000000000000, 0.000000000000000000, 0.000000000000000000 ) ) ;
#4384=CIRCLE ( 'NONE', #37137, 5.000000000000002665 ) ;
#4404=ORIENTED_EDGE ( 'NONE', *, *, #78238, .F. ) ;
#4410=CARTESIAN_POINT ( 'NONE',  ( 0.000000000000000000, 0.000000000000000000, 0.000000000000000000 ) ) ;
#4455=ORIENTED_EDGE ( 'NONE', *, *, #79542, .F. ) ;
#4476=CIRCLE ( 'NONE', #64762, 5.000000000000001776 ) ;
#4482=ADVANCED_FACE ( 'NONE', ( #6288 ), #54294, .T. ) ;
#4487=AXIS2_PLACEMENT_3D ( 'NONE', #23117, #21531, #79202 ) ;
#4498=CARTESIAN_POINT ( 'NONE',  ( 42.98746414932995208, 3.851859888774471706E-31, 5.000000000000001776 ) ) ;
#4502=LINE ( 'NONE', #29871, #97892 ) ;
#4521=AXIS2_PLACEMENT_3D ( 'NONE', #66192, #16045, #48927 ) ;
#4528=EDGE_CURVE ( 'NONE', #37991, #7878, #4641, .T. ) ;
#4554=VECTOR ( 'NONE', #66909, 1000.000000000000000 ) ;
#4584=DIRECTION ( 'NONE',  ( 0.000000000000000000, 1.000000000000000000, 0.000000000000000000 ) ) ;
#4585=CARTESIAN_POINT ( 'NONE',  ( 6.249999999999998224, 0.000000000000000000, 0.000000000000000000 ) ) ;
#4586=CARTESIAN_POINT ( 'NONE',  ( 9.830769230769229594, 4.172000000000003261, 5.109226446042759579E-16 ) ) ;
#4611=ADVANCED_FACE ( 'NONE', ( #73683 ), #8950, .T. ) ;
#4626=EDGE_CURVE ( 'NONE', #85522, #2566, #20145, .T. ) ;
#4641=CIRCLE ( 'NONE', #57967, 4.172000000000001485 ) ;
#4705=ORIENTED_EDGE ( 'NONE', *, *, #34689, .F. ) ;
#4722=CARTESIAN_POINT ( 'NONE',  ( 43.88846153846154152, 1.411358822780289120E-15, 0.000000000000000000 ) ) ;
#4726=AXIS2_PLACEMENT_3D ( 'NONE', #18404, #41591, #99822 ) ;
#4745=ORIENTED_EDGE ( 'NONE', *, *, #9734, .F. ) ;
#4760=ORIENTED_EDGE ( 'NONE', *, *, #96594, .F. ) ;
#4771=CARTESIAN_POINT ( 'NONE',  ( 19.29515645702225868, -5.000000000000000000, 6.123233995736768255E-16 ) ) ;
#4790=CARTESIAN_POINT ( 'NONE',  ( 44.46823338009918558, 1.482358050883964840E-15, 0.000000000000000000 ) ) ;
#4800=DIRECTION ( 'NONE',  ( -0.000000000000000000, 0.5000000000000009992, 0.8660254037844380415 ) ) ;
#4820=ADVANCED_FACE ( 'NONE', ( #76879 ), #2994, .T. ) ;
#4826=CARTESIAN_POINT ( 'NONE',  ( 0.4969600502617477211, 4.995646404165273502, -7.347286611336973472 ) ) ;
#4869=CIRCLE ( 'NONE', #96198, 5.000000000000001776 ) ;
#4876=ADVANCED_FACE ( 'NONE', ( #59654 ), #8076, .T. ) ;
#4887=DIRECTION ( 'NONE',  ( 0.000000000000000000, -1.000000000000000000, 0.000000000000000000 ) ) ;
#4890=ADVANCED_BREP_SHAPE_REPRESENTATION ( '', ( #55270, #10728 ), #54068 ) ;
#4943=AXIS2_PLACEMENT_3D ( 'NONE', #69059, #35649, #93853 ) ;
#4953=CARTESIAN_POINT ( 'NONE',  ( 39.44615384615384812, -4.171999999999999709, 5.616230220889763424E-16 ) ) ;
#4965=ORIENTED_EDGE ( 'NONE', *, *, #69598, .F. ) ;
#4967=LINE ( 'NONE', #70758, #62684 ) ;
#5037=VERTEX_POINT ( 'NONE', #15863 ) ;
#5039=DIRECTION ( 'NONE',  ( 0.000000000000000000, -1.000000000000000000, 0.000000000000000000 ) ) ;
#5091=ADVANCED_FACE ( 'NONE', ( #33138 ), #24001, .T. ) ;
#5105=VECTOR ( 'NONE', #65890, 1000.000000000000000 ) ;
#5145=CARTESIAN_POINT ( 'NONE',  ( 13.69330508143927538, 1.340359594676612611E-15, 0.000000000000000000 ) ) ;
#5164=VERTEX_POINT ( 'NONE', #90826 ) ;
#5178=DIRECTION ( 'NONE',  ( 0.000000000000000000, -1.000000000000000000, 0.000000000000000000 ) ) ;
#5182=LINE ( 'NONE', #48266, #98409 ) ;
#5198=VECTOR ( 'NONE', #11222, 999.9999999999998863 ) ;
#5242=AXIS2_PLACEMENT_3D ( 'NONE', #8587, #24803, #89522 ) ;
#5278=EDGE_CURVE ( 'NONE', #29468, #6808, #20078, .T. ) ;
#5327=CARTESIAN_POINT ( 'NONE',  ( 24.63846153846153797, 1.411358822780289120E-15, 0.000000000000000000 ) ) ;
#5347=VECTOR ( 'NONE', #23157, 999.9999999999998863 ) ;
#5358=DIRECTION ( 'NONE',  ( 0.000000000000000000, 1.000000000000000000, 0.000000000000000000 ) ) ;
#5364=CARTESIAN_POINT ( 'NONE',  ( -3.962208369018801833E-15, 6.732211846623392226, -4.339467034331192075 ) ) ;
#5409=DIRECTION ( 'NONE',  ( -1.000000000000000000, -1.224606353822377258E-16, -0.000000000000000000 ) ) ;
#5430=DIRECTION ( 'NONE',  ( -1.000000000000000000, -1.224606353822377258E-16, -0.000000000000000000 ) ) ;
#5460=ORIENTED_EDGE ( 'NONE', *, *, #18934, .T. ) ;
#5471=CARTESIAN_POINT ( 'NONE',  ( 0.000000000000000000, 6.123233995736770227E-16, -5.000000000000002665 ) ) ;
#5478=ORIENTED_EDGE ( 'NONE', *, *, #65308, .F. ) ;
#5502=ORIENTED_EDGE ( 'NONE', *, *, #38130, .T. ) ;
#5509=CARTESIAN_POINT ( 'NONE',  ( 35.58361799548379167, 5.000000000000003553, 0.000000000000000000 ) ) ;
#5551=DIRECTION ( 'NONE',  ( 0.000000000000000000, 1.000000000000000000, 0.000000000000000000 ) ) ;
#5559=DIRECTION ( 'NONE',  ( -1.000000000000000000, -1.224606353822377258E-16, -0.000000000000000000 ) ) ;
#5568=AXIS2_PLACEMENT_3D ( 'NONE', #8980, #9504, #58064 ) ;
#5572=AXIS2_PLACEMENT_3D ( 'NONE', #68233, #43427, #1879 ) ;
#5574=ADVANCED_FACE ( 'NONE', ( #62144 ), #16626, .T. ) ;
#5586=EDGE_CURVE ( 'NONE', #55144, #76220, #28725, .T. ) ;
#5663=EDGE_CURVE ( 'NONE', #71421, #42859, #35331, .T. ) ;
#5670=VECTOR ( 'NONE', #29501, 1000.000000000000000 ) ;
#5679=CARTESIAN_POINT ( 'NONE',  ( 0.000000000000000000, 0.000000000000000000, 0.000000000000000000 ) ) ;
#5680=CARTESIAN_POINT ( 'NONE',  ( 31.14131030317610538, 6.123233995736772199E-16, -5.000000000000001776 ) ) ;
#5699=EDGE_LOOP ( 'NONE', ( #104620, #52003, #82601, #48326, #24013 ) ) ;
#5702=ADVANCED_FACE ( 'NONE', ( #85886 ), #44889, .T. ) ;
#5813=VECTOR ( 'NONE', #101501, 1000.000000000000000 ) ;
#5820=EDGE_LOOP ( 'NONE', ( #74062, #94489, #56019, #35333 ) ) ;
#5855=EDGE_CURVE ( 'NONE', #20128, #65067, #23140, .T. ) ;
#5867=ORIENTED_EDGE ( 'NONE', *, *, #75496, .F. ) ;
#5878=LINE ( 'NONE', #37240, #47627 ) ;
#5882=DIRECTION ( 'NONE',  ( 0.000000000000000000, 0.000000000000000000, 1.000000000000000000 ) ) ;
#5903=ADVANCED_FACE ( 'NONE', ( #7978 ), #87633, .T. ) ;
#5946=EDGE_CURVE ( 'NONE', #13798, #49621, #22627, .T. ) ;
#5993=DIRECTION ( 'NONE',  ( -1.000000000000000000, -1.224606353822377258E-16, -0.000000000000000000 ) ) ;
#6002=ORIENTED_EDGE ( 'NONE', *, *, #11672, .F. ) ;
#6028=DIRECTION ( 'NONE',  ( -1.000000000000000000, -1.224606353822377258E-16, -0.000000000000000000 ) ) ;
#6061=AXIS2_PLACEMENT_3D ( 'NONE', #65117, #39796, #49454 ) ;
#6083=CONICAL_SURFACE ( 'NONE', #71518, 4.172000000000001485, 0.9599310885968750373 ) ;
#6089=EDGE_LOOP ( 'NONE', ( #106095, #92588, #104698, #22490, #35574 ) ) ;
#6092=DIRECTION ( 'NONE',  ( -1.000000000000000000, -0.000000000000000000, -0.000000000000000000 ) ) ;
#6104=CARTESIAN_POINT ( 'NONE',  ( 0.000000000000000000, 0.000000000000000000, 0.000000000000000000 ) ) ;
#6127=ADVANCED_FACE ( 'NONE', ( #99653 ), #104874, .T. ) ;
#6133=ORIENTED_EDGE ( 'NONE', *, *, #10812, .T. ) ;
#6134=CARTESIAN_POINT ( 'NONE',  ( 0.000000000000000000, 1.502314598737159031E-15, -8.000000000000000000 ) ) ;
#6199=AXIS2_PLACEMENT_3D ( 'NONE', #59354, #61486, #84149 ) ;
#6227=EDGE_CURVE ( 'NONE', #9931, #104720, #83468, .T. ) ;
#6231=AXIS2_PLACEMENT_3D ( 'NONE', #82141, #96757, #97796 ) ;
#6285=CIRCLE ( 'NONE', #33903, 4.171999999999999709 ) ;
#6288=FACE_OUTER_BOUND ( 'NONE', #62195, .T. ) ;
#6320=ORIENTED_EDGE ( 'NONE', *, *, #94779, .T. ) ;
#6349=FACE_OUTER_BOUND ( 'NONE', #13298, .T. ) ;
#6438=AXIS2_PLACEMENT_3D ( 'NONE', #94938, #30743, #63629 ) ;
#6479=ADVANCED_FACE ( 'NONE', ( #57986 ), #90907, .T. ) ;
#6487=VERTEX_POINT ( 'NONE', #33748 ) ;
#6492=CARTESIAN_POINT ( 'NONE',  ( 8.929771841637641927, 6.123233995736772199E-16, -5.000000000000001776 ) ) ;
#6508=AXIS2_PLACEMENT_3D ( 'NONE', #45208, #36080, #27988 ) ;
#6551=AXIS2_PLACEMENT_3D ( 'NONE', #99514, #33222, #98972 ) ;
#6569=VERTEX_POINT ( 'NONE', #61199 ) ;
#6600=CYLINDRICAL_SURFACE ( 'NONE', #79649, 5.000000000000002665 ) ;
#6605=DIRECTION ( 'NONE',  ( 1.000000000000000000, 1.224606353822377258E-16, 0.000000000000000000 ) ) ;
#6609=DIRECTION ( 'NONE',  ( 0.000000000000000000, -1.000000000000000000, 0.000000000000000000 ) ) ;
#6655=VECTOR ( 'NONE', #308, 1000.000000000000227 ) ;
#6692=AXIS2_PLACEMENT_3D ( 'NONE', #34960, #49504, #50552 ) ;
#6698=AXIS2_PLACEMENT_3D ( 'NONE', #100132, #860, #82356 ) ;
#6699=CARTESIAN_POINT ( 'NONE',  ( 41.82792046605465686, 1.340359594676612611E-15, 0.000000000000000000 ) ) ;
#6712=CONICAL_SURFACE ( 'NONE', #75621, 5.000000000000001776, 0.9599310885968803664 ) ;
#6714=CARTESIAN_POINT ( 'NONE',  ( 38.54515645702225868, -5.000000000000000000, 6.123233995736768255E-16 ) ) ;
#6742=FACE_OUTER_BOUND ( 'NONE', #12802, .T. ) ;
#6750=EDGE_CURVE ( 'NONE', #63565, #43261, #37353, .T. ) ;
#6760=DIRECTION ( 'NONE',  ( -1.000000000000000000, -0.000000000000000000, -0.000000000000000000 ) ) ;
#6762=CARTESIAN_POINT ( 'NONE',  ( 46.02200000000003399, 0.000000000000000000, 0.000000000000000000 ) ) ;
#6776=AXIS2_PLACEMENT_3D ( 'NONE', #18682, #25172, #76339 ) ;
#6785=LINE ( 'NONE', #32144, #86091 ) ;
#6794=ADVANCED_FACE ( 'NONE', ( #30978 ), #39100, .T. ) ;
#6808=VERTEX_POINT ( 'NONE', #71387 ) ;
#6825=CIRCLE ( 'NONE', #34198, 5.000000000000001776 ) ;
#6881=CONICAL_SURFACE ( 'NONE', #70634, 5.000000000000001776, 0.9599310885968803664 ) ;
#6922=AXIS2_PLACEMENT_3D ( 'NONE', #17181, #33370, #16633 ) ;
#6933=CARTESIAN_POINT ( 'NONE',  ( 0.01688885742776573967, 6.535341423375589542, -4.680456609903974829 ) ) ;
#6957=VERTEX_POINT ( 'NONE', #18500 ) ;
#6960=ORIENTED_EDGE ( 'NONE', *, *, #72848, .T. ) ;
#6992=EDGE_LOOP ( 'NONE', ( #96704, #15774, #68654 ) ) ;
#7000=ORIENTED_EDGE ( 'NONE', *, *, #62847, .T. ) ;
#7017=ADVANCED_FACE ( 'NONE', ( #51363 ), #32250, .T. ) ;
#7018=CARTESIAN_POINT ( 'NONE',  ( 15.75384615384615294, -4.171999999999999709, 0.000000000000000000 ) ) ;
#7037=EDGE_LOOP ( 'NONE', ( #38228, #93247, #73189, #106362, #44468 ) ) ;
#7042=CARTESIAN_POINT ( 'NONE',  ( 0.000000000000000000, 6.123233995736770227E-16, -5.000000000000002665 ) ) ;
#7084=VERTEX_POINT ( 'NONE', #98064 ) ;
#7087=CARTESIAN_POINT ( 'NONE',  ( 38.86638200451619696, 1.340359594676612611E-15, 0.000000000000000000 ) ) ;
#7097=VERTEX_POINT ( 'NONE', #15552 ) ;
#7104=ORIENTED_EDGE ( 'NONE', *, *, #81782, .F. ) ;
#7116=DIRECTION ( 'NONE',  ( -1.000000000000000000, -1.224606353822377258E-16, -0.000000000000000000 ) ) ;
#7127=EDGE_CURVE ( 'NONE', #8257, #60803, #80276, .T. ) ;
#7132=CARTESIAN_POINT ( 'NONE',  ( 20.77592568779148863, 6.123233995736772199E-16, -5.000000000000001776 ) ) ;
#7141=DIRECTION ( 'NONE',  ( 0.000000000000000000, -1.000000000000000000, 0.000000000000000000 ) ) ;
#7153=PLANE ( 'NONE',  #93258 ) ;
#7175=CIRCLE ( 'NONE', #82946, 5.000000000000002665 ) ;
#7189=DIRECTION ( 'NONE',  ( -1.000000000000000000, -1.224606353822377258E-16, -0.000000000000000000 ) ) ;
#7192=DIRECTION ( 'NONE',  ( 0.000000000000000000, 0.000000000000000000, 1.000000000000000000 ) ) ;
#7214=ORIENTED_EDGE ( 'NONE', *, *, #82612, .T. ) ;
#7253=VERTEX_POINT ( 'NONE', #82419 ) ;
#7277=DIRECTION ( 'NONE',  ( 0.000000000000000000, -1.000000000000000000, 0.000000000000000000 ) ) ;
#7301=CIRCLE ( 'NONE', #19458, 5.000000000000001776 ) ;
#7310=CARTESIAN_POINT ( 'NONE',  ( 16.33361799548379523, 5.000000000000003553, 0.000000000000000000 ) ) ;
#7318=ADVANCED_FACE ( 'NONE', ( #103388 ), #102322, .F. ) ;
#7343=AXIS2_PLACEMENT_3D ( 'NONE', #91158, #1017, #65266 ) ;
#7397=ORIENTED_EDGE ( 'NONE', *, *, #82612, .F. ) ;
#7398=CARTESIAN_POINT ( 'NONE',  ( 4.993259224064100499E-16, 0.3912769055735416113, -8.000000000000000000 ) ) ;
#7401=CYLINDRICAL_SURFACE ( 'NONE', #66858, 5.000000000000002665 ) ;
#7426=ORIENTED_EDGE ( 'NONE', *, *, #60694, .T. ) ;
#7499=DIRECTION ( 'NONE',  ( -1.000000000000000000, -0.000000000000000000, -0.000000000000000000 ) ) ;
#7557=DIRECTION ( 'NONE',  ( -1.000000000000000000, -0.000000000000000000, -0.000000000000000000 ) ) ;
#7574=EDGE_LOOP ( 'NONE', ( #83506, #41165, #36261, #87356, #51452 ) ) ;
#7580=DIRECTION ( 'NONE',  ( 0.000000000000000000, -1.000000000000000000, 0.000000000000000000 ) ) ;
#7606=CARTESIAN_POINT ( 'NONE',  ( 43.88846153846154152, 4.172000000000003261, 5.109226446042759579E-16 ) ) ;
#7619=ORIENTED_EDGE ( 'NONE', *, *, #68254, .T. ) ;
#7656=CARTESIAN_POINT ( 'NONE',  ( 20.77592568779148863, -5.000000000000000888, 6.123233995736769241E-16 ) ) ;
#7657=DIRECTION ( 'NONE',  ( 0.000000000000000000, -1.000000000000000000, 0.000000000000000000 ) ) ;
#7661=CARTESIAN_POINT ( 'NONE',  ( 37.06438722625302518, 1.482358050883964840E-15, 0.000000000000000000 ) ) ;
#7697=DIRECTION ( 'NONE',  ( 0.000000000000000000, -1.000000000000000000, 0.000000000000000000 ) ) ;
#7707=DIRECTION ( 'NONE',  ( 0.000000000000000000, -1.000000000000000000, 0.000000000000000000 ) ) ;
#7726=ADVANCED_FACE ( 'NONE', ( #8797 ), #84561, .T. ) ;
#7746=ORIENTED_EDGE ( 'NONE', *, *, #89325, .T. ) ;
#7754=ORIENTED_EDGE ( 'NONE', *, *, #12253, .F. ) ;
#7782=CARTESIAN_POINT ( 'NONE',  ( 42.40769230769231513, 1.411358822780289120E-15, 0.000000000000000000 ) ) ;
#7786=DIRECTION ( 'NONE',  ( 0.5735764363510470476, -0.8191520442889911324, 1.003171929053524007E-16 ) ) ;
#7822=DIRECTION ( 'NONE',  ( 0.000000000000000000, -1.000000000000000000, 0.000000000000000000 ) ) ;
#7842=DIRECTION ( 'NONE',  ( 1.000000000000000000, 1.224606353822377258E-16, 0.000000000000000000 ) ) ;
#7844=CARTESIAN_POINT ( 'NONE',  ( 10.73176661990081371, -5.000000000000000000, 0.000000000000000000 ) ) ;
#7862=PLANE ( 'NONE',  #10850 ) ;
#7878=VERTEX_POINT ( 'NONE', #103133 ) ;
#7932=VERTEX_POINT ( 'NONE', #82010 ) ;
#7978=FACE_OUTER_BOUND ( 'NONE', #45317, .T. ) ;
#7980=DIRECTION ( 'NONE',  ( 0.000000000000000000, -1.000000000000000000, 0.000000000000000000 ) ) ;
#7988=DIRECTION ( 'NONE',  ( -1.000000000000000000, -0.000000000000000000, -0.000000000000000000 ) ) ;
#8011=CARTESIAN_POINT ( 'NONE',  ( 35.58361799548379167, 1.482358050883964840E-15, 0.000000000000000000 ) ) ;
#8014=ORIENTED_EDGE ( 'NONE', *, *, #77722, .F. ) ;
#8051=DIRECTION ( 'NONE',  ( -1.000000000000000000, -1.224606353822377258E-16, -0.000000000000000000 ) ) ;
#8076=CONICAL_SURFACE ( 'NONE', #64909, 5.000000000000001776, 0.9599310885968803664 ) ;
#8110=EDGE_CURVE ( 'NONE', #47541, #96607, #88104, .T. ) ;
#8116=ORIENTED_EDGE ( 'NONE', *, *, #94745, .F. ) ;
#8130=PRESENTATION_STYLE_ASSIGNMENT (( #90122 ) ) ;
#8144=EDGE_CURVE ( 'NONE', #57214, #1618, #77783, .T. ) ;
#8153=CARTESIAN_POINT ( 'NONE',  ( 34.10284876471455817, -5.000000000000000888, 6.123233995736769241E-16 ) ) ;
#8175=ORIENTED_EDGE ( 'NONE', *, *, #47294, .F. ) ;
#8181=CIRCLE ( 'NONE', #15107, 5.000000000000001776 ) ;
#8183=DIRECTION ( 'NONE',  ( -1.000000000000000000, -1.224606353822377258E-16, -0.000000000000000000 ) ) ;
#8188=DIRECTION ( 'NONE',  ( -0.5735764363510512664, 0.8191520442889881348, 1.003171929053520309E-16 ) ) ;
#8221=DIRECTION ( 'NONE',  ( 0.000000000000000000, -1.000000000000000000, 0.000000000000000000 ) ) ;
#8239=CIRCLE ( 'NONE', #61628, 4.171999999999999709 ) ;
#8257=VERTEX_POINT ( 'NONE', #60444 ) ;
#8287=EDGE_CURVE ( 'NONE', #84621, #33159, #69582, .T. ) ;
#8309=DIRECTION ( 'NONE',  ( 0.000000000000000000, -1.000000000000000000, 0.000000000000000000 ) ) ;
#8335=EDGE_CURVE ( 'NONE', #76065, #65523, #12379, .T. ) ;
#8353=DIRECTION ( 'NONE',  ( -1.000000000000000000, -1.224606353822377258E-16, -0.000000000000000000 ) ) ;
#8378=ORIENTED_EDGE ( 'NONE', *, *, #1576, .F. ) ;
#8381=LINE ( 'NONE', #7310, #22132 ) ;
#8384=AXIS2_PLACEMENT_3D ( 'NONE', #78315, #96105, #38421 ) ;
#8419=ORIENTED_EDGE ( 'NONE', *, *, #87474, .F. ) ;
#8431=DIRECTION ( 'NONE',  ( -1.000000000000000000, -1.224606353822377258E-16, -0.000000000000000000 ) ) ;
#8439=VERTEX_POINT ( 'NONE', #24756 ) ;
#8447=DIRECTION ( 'NONE',  ( 0.000000000000000000, -1.000000000000000000, 0.000000000000000000 ) ) ;
#8456=ORIENTED_EDGE ( 'NONE', *, *, #106767, .F. ) ;
#8458=ORIENTED_EDGE ( 'NONE', *, *, #95898, .T. ) ;
#8473=EDGE_CURVE ( 'NONE', #75630, #85144, #73589, .T. ) ;
#8513=AXIS2_PLACEMENT_3D ( 'NONE', #89838, #98446, #49354 ) ;
#8537=ADVANCED_FACE ( 'NONE', ( #52586 ), #11615, .T. ) ;
#8540=VERTEX_POINT ( 'NONE', #102746 ) ;
#8544=EDGE_CURVE ( 'NONE', #6569, #25032, #97683, .T. ) ;
#8570=LINE ( 'NONE', #15067, #41803 ) ;
#8587=CARTESIAN_POINT ( 'NONE',  ( 29.66054107240687543, 1.482358050883964840E-15, 0.000000000000000000 ) ) ;
#8609=ADVANCED_FACE ( 'NONE', ( #76865 ), #80524, .T. ) ;
#8625=CARTESIAN_POINT ( 'NONE',  ( 20.77592568779148863, 1.482358050883964840E-15, 0.000000000000000000 ) ) ;
#8661=AXIS2_PLACEMENT_3D ( 'NONE', #98191, #5993, #72330 ) ;
#8706=DIRECTION ( 'NONE',  ( 0.5735764363510470476, -0.8191520442889911324, 1.003171929053524007E-16 ) ) ;
#8751=DIRECTION ( 'NONE',  ( 1.000000000000000000, 1.224606353822377258E-16, 0.000000000000000000 ) ) ;
#8754=EDGE_CURVE ( 'NONE', #54320, #71171, #10688, .T. ) ;
#8763=LINE ( 'NONE', #50803, #102353 ) ;
#8771=CIRCLE ( 'NONE', #60467, 5.000000000000001776 ) ;
#8782=AXIS2_PLACEMENT_3D ( 'NONE', #65453, #89737, #25564 ) ;
#8789=VERTEX_POINT ( 'NONE', #18293 ) ;
#8797=FACE_OUTER_BOUND ( 'NONE', #36057, .T. ) ;
#8867=DIRECTION ( 'NONE',  ( -1.000000000000000000, -0.000000000000000000, -0.000000000000000000 ) ) ;
#8878=VERTEX_POINT ( 'NONE', #30102 ) ;
#8901=DIRECTION ( 'NONE',  ( 0.000000000000000000, -1.000000000000000000, 0.000000000000000000 ) ) ;
#8905=DIRECTION ( 'NONE',  ( -1.000000000000000000, -0.000000000000000000, -0.000000000000000000 ) ) ;
#8917=DIRECTION ( 'NONE',  ( -1.000000000000000000, -1.224606353822377258E-16, -0.000000000000000000 ) ) ;
#8938=LINE ( 'NONE', #74729, #75194 ) ;
#8950=CYLINDRICAL_SURFACE ( 'NONE', #32197, 5.000000000000002665 ) ;
#8960=AXIS2_PLACEMENT_3D ( 'NONE', #54857, #46784, #87787 ) ;
#8978=DIRECTION ( 'NONE',  ( -1.000000000000000000, -1.224606353822377258E-16, -0.000000000000000000 ) ) ;
#8980=CARTESIAN_POINT ( 'NONE',  ( 18.13561277374696701, 1.340359594676612611E-15, 0.000000000000000000 ) ) ;
#8996=FACE_OUTER_BOUND ( 'NONE', #42730, .T. ) ;
#8998=DIRECTION ( 'NONE',  ( 0.000000000000000000, -1.000000000000000000, 0.000000000000000000 ) ) ;
#9009=DIRECTION ( 'NONE',  ( 0.000000000000000000, -1.000000000000000000, 0.000000000000000000 ) ) ;
#9013=FACE_OUTER_BOUND ( 'NONE', #89613, .T. ) ;
#9034=CONICAL_SURFACE ( 'NONE', #76258, 4.172000000000001485, 0.9599310885968750373 ) ;
#9038=DIRECTION ( 'NONE',  ( -1.000000000000000000, -1.224606353822377258E-16, -0.000000000000000000 ) ) ;
#9042=CARTESIAN_POINT ( 'NONE',  ( 0.06730325657375685333, -1.557442666578433776, -8.000000000000000000 ) ) ;
#9083=CARTESIAN_POINT ( 'NONE',  ( 10.73176661990081371, 1.340359594676612611E-15, 0.000000000000000000 ) ) ;
#9100=ORIENTED_EDGE ( 'NONE', *, *, #59454, .F. ) ;
#9111=CARTESIAN_POINT ( 'NONE',  ( 36.48461538461538822, 1.411358822780289120E-15, 0.000000000000000000 ) ) ;
#9113=ORIENTED_EDGE ( 'NONE', *, *, #57976, .F. ) ;
#9145=EDGE_CURVE ( 'NONE', #60319, #16386, #56408, .T. ) ;
#9167=DIRECTION ( 'NONE',  ( 0.5735764363510470476, -0.8191520442889911324, 1.003171929053524007E-16 ) ) ;
#9168=EDGE_LOOP ( 'NONE', ( #70085, #29767, #81179, #71520, #89635 ) ) ;
#9170=CIRCLE ( 'NONE', #43612, 4.172000000000001485 ) ;
#9181=ORIENTED_EDGE ( 'NONE', *, *, #61082, .F. ) ;
#9193=CARTESIAN_POINT ( 'NONE',  ( 19.61638200451619696, 1.340359594676612611E-15, 0.000000000000000000 ) ) ;
#9236=DIRECTION ( 'NONE',  ( 0.000000000000000000, 1.000000000000000000, 0.000000000000000000 ) ) ;
#9250=DIRECTION ( 'NONE',  ( 1.734723475976806108E-16, -1.000000000000000000, 0.000000000000000000 ) ) ;
#9262=DIRECTION ( 'NONE',  ( -1.000000000000000000, -1.224606353822377258E-16, -0.000000000000000000 ) ) ;
#9268=ORIENTED_EDGE ( 'NONE', *, *, #102948, .T. ) ;
#9292=CARTESIAN_POINT ( 'NONE',  ( 45.94900261086841198, -5.000000000000000888, 6.123233995736769241E-16 ) ) ;
#9347=ORIENTED_EDGE ( 'NONE', *, *, #12253, .T. ) ;
#9358=CIRCLE ( 'NONE', #100609, 5.000000000000002665 ) ;
#9392=VERTEX_POINT ( 'NONE', #44971 ) ;
#9401=ORIENTED_EDGE ( 'NONE', *, *, #75895, .F. ) ;
#9419=CARTESIAN_POINT ( 'NONE',  ( 6.849999999999999645, -4.618802153516998743, 7.999999999999998224 ) ) ;
#9451=CARTESIAN_POINT ( 'NONE',  ( 26.69900261086841198, 1.482358050883964840E-15, 0.000000000000000000 ) ) ;
#9470=CARTESIAN_POINT ( 'NONE',  ( 29.98176661990081371, 5.000000000000004441, 6.123233995736770227E-16 ) ) ;
#9472=DIRECTION ( 'NONE',  ( 1.000000000000000000, 1.224606353822377258E-16, 0.000000000000000000 ) ) ;
#9504=DIRECTION ( 'NONE',  ( -1.000000000000000000, -1.224606353822377258E-16, -0.000000000000000000 ) ) ;
#9507=ORIENTED_EDGE ( 'NONE', *, *, #85508, .T. ) ;
#9543=EDGE_CURVE ( 'NONE', #32861, #39589, #4384, .T. ) ;
#9546=ORIENTED_EDGE ( 'NONE', *, *, #12276, .F. ) ;
#9548=CARTESIAN_POINT ( 'NONE',  ( 6.849999999999999645, 4.618802153517004960, 7.999999999999998224 ) ) ;
#9572=CARTESIAN_POINT ( 'NONE',  ( 18.13561277374696701, 5.000000000000004441, 6.123233995736770227E-16 ) ) ;
#9575=DIRECTION ( 'NONE',  ( 0.000000000000000000, -1.000000000000000000, 0.000000000000000000 ) ) ;
#9594=FACE_OUTER_BOUND ( 'NONE', #33994, .T. ) ;
#9657=AXIS2_PLACEMENT_3D ( 'NONE', #37888, #30306, #88528 ) ;
#9668=DIRECTION ( 'NONE',  ( 0.000000000000000000, 1.000000000000000000, 0.000000000000000000 ) ) ;
#9677=VERTEX_POINT ( 'NONE', #19535 ) ;
#9685=DIRECTION ( 'NONE',  ( -1.000000000000000000, -1.224606353822377258E-16, -0.000000000000000000 ) ) ;
#9734=EDGE_CURVE ( 'NONE', #88628, #75560, #11553, .T. ) ;
#9771=LINE ( 'NONE', #90714, #34532 ) ;
#9793=CARTESIAN_POINT ( 'NONE',  ( 22.25669491856071858, 5.000000000000002665, 0.000000000000000000 ) ) ;
#9795=ADVANCED_FACE ( 'NONE', ( #8996 ), #64599, .T. ) ;
#9800=CARTESIAN_POINT ( 'NONE',  ( 20.19615384615384457, 1.411358822780289120E-15, 0.000000000000000000 ) ) ;
#9803=EDGE_CURVE ( 'NONE', #80882, #19372, #81808, .T. ) ;
#9830=AXIS2_PLACEMENT_3D ( 'NONE', #105109, #23148, #31251 ) ;
#9850=CARTESIAN_POINT ( 'NONE',  ( 19.29515645702225868, 3.851859888774471706E-31, 5.000000000000001776 ) ) ;
#9853=CARTESIAN_POINT ( 'NONE',  ( 0.000000000000000000, 0.000000000000000000, 0.000000000000000000 ) ) ;
#9871=EDGE_CURVE ( 'NONE', #58651, #76997, #66179, .T. ) ;
#9900=DIRECTION ( 'NONE',  ( 0.000000000000000000, 1.000000000000000000, 0.000000000000000000 ) ) ;
#9931=VERTEX_POINT ( 'NONE', #11114 ) ;
#9945=VECTOR ( 'NONE', #17899, 1000.000000000000000 ) ;
#9948=VECTOR ( 'NONE', #92149, 1000.000000000000227 ) ;
#9958=ORIENTED_EDGE ( 'NONE', *, *, #70282, .T. ) ;
#9964=AXIS2_PLACEMENT_3D ( 'NONE', #41363, #82889, #1955 ) ;
#9968=LINE ( 'NONE', #17016, #24478 ) ;
#9989=DIRECTION ( 'NONE',  ( -1.000000000000000000, -0.000000000000000000, -0.000000000000000000 ) ) ;
#10025=DIRECTION ( 'NONE',  ( -1.000000000000000000, -1.224606353822377258E-16, -0.000000000000000000 ) ) ;
#10032=DIRECTION ( 'NONE',  ( -1.000000000000000000, -1.224606353822377258E-16, -0.000000000000000000 ) ) ;
#10042=CARTESIAN_POINT ( 'NONE',  ( 43.30868969682389036, 1.340359594676612611E-15, 0.000000000000000000 ) ) ;
#10094=DIRECTION ( 'NONE',  ( -1.000000000000000000, -1.224606353822377258E-16, -0.000000000000000000 ) ) ;
#10133=EDGE_LOOP ( 'NONE', ( #997, #9347, #82640, #56830, #44651 ) ) ;
#10161=EDGE_CURVE ( 'NONE', #61495, #7932, #103340, .T. ) ;
#10166=ORIENTED_EDGE ( 'NONE', *, *, #73204, .F. ) ;
#10222=DIRECTION ( 'NONE',  ( -1.000000000000000000, -1.224606353822377258E-16, -0.000000000000000000 ) ) ;
#10230=CIRCLE ( 'NONE', #68859, 4.172000000000001485 ) ;
#10246=CIRCLE ( 'NONE', #42992, 5.000000000000001776 ) ;
#10249=CARTESIAN_POINT ( 'NONE',  ( -1.007969207232617206E-15, -0.7818963812180719231, 7.999999999999996447 ) ) ;
#10258=CARTESIAN_POINT ( 'NONE',  ( 11.89131030317610183, 1.482358050883964840E-15, 0.000000000000000000 ) ) ;
#10268=CIRCLE ( 'NONE', #91218, 5.000000000000001776 ) ;
#10323=CARTESIAN_POINT ( 'NONE',  ( 17.81438722625302518, -5.000000000000000888, 6.123233995736769241E-16 ) ) ;
#10353=CARTESIAN_POINT ( 'NONE',  ( 40.02592568779148507, 3.851859888774471706E-31, 5.000000000000001776 ) ) ;
#10384=DIRECTION ( 'NONE',  ( -1.000000000000000000, -1.224606353822377258E-16, -0.000000000000000000 ) ) ;
#10393=CIRCLE ( 'NONE', #68946, 5.000000000000002665 ) ;
#10429=DIRECTION ( 'NONE',  ( 1.000000000000000000, 1.224606353822377258E-16, 0.000000000000000000 ) ) ;
#10461=CIRCLE ( 'NONE', #27772, 4.172000000000001485 ) ;
#10468=LINE ( 'NONE', #51462, #52512 ) ;
#10472=ORIENTED_EDGE ( 'NONE', *, *, #38723, .T. ) ;
#10486=EDGE_CURVE ( 'NONE', #84262, #58211, #60755, .T. ) ;
#10496=CARTESIAN_POINT ( 'NONE',  ( 40.02592568779148507, 1.482358050883964840E-15, 0.000000000000000000 ) ) ;
#10498=DIRECTION ( 'NONE',  ( -1.000000000000000000, -1.224606353822377258E-16, -0.000000000000000000 ) ) ;
#10518=CIRCLE ( 'NONE', #93221, 4.172000000000001485 ) ;
#10551=CIRCLE ( 'NONE', #77784, 4.172000000000001485 ) ;
#10607=ORIENTED_EDGE ( 'NONE', *, *, #36911, .F. ) ;
#10615=DIRECTION ( 'NONE',  ( -1.000000000000000000, -1.224606353822377258E-16, -0.000000000000000000 ) ) ;
#10619=EDGE_CURVE ( 'NONE', #50381, #54238, #47604, .T. ) ;
#10622=CARTESIAN_POINT ( 'NONE',  ( 26.69900261086841198, 5.000000000000002665, 0.000000000000000000 ) ) ;
#10655=AXIS2_PLACEMENT_3D ( 'NONE', #75717, #59017, #66033 ) ;
#10673=ORIENTED_EDGE ( 'NONE', *, *, #79542, .T. ) ;
#10677=DIRECTION ( 'NONE',  ( 0.000000000000000000, -1.000000000000000000, 0.000000000000000000 ) ) ;
#10688=LINE ( 'NONE', #3151, #78753 ) ;
#10728=AXIS2_PLACEMENT_3D ( 'NONE', #14983, #57033, #47878 ) ;
#10744=ORIENTED_EDGE ( 'NONE', *, *, #1253, .T. ) ;
#10747=CARTESIAN_POINT ( 'NONE',  ( 32.62207953394533178, 6.123233995736772199E-16, -5.000000000000001776 ) ) ;
#10754=DIRECTION ( 'NONE',  ( 0.000000000000000000, -1.000000000000000000, 0.000000000000000000 ) ) ;
#10766=DIRECTION ( 'NONE',  ( -1.000000000000000000, -1.224606353822377258E-16, -0.000000000000000000 ) ) ;
#10789=ORIENTED_EDGE ( 'NONE', *, *, #59454, .T. ) ;
#10804=DIRECTION ( 'NONE',  ( 0.5735764363510468256, 0.8191520442889913545, 0.000000000000000000 ) ) ;
#10812=EDGE_CURVE ( 'NONE', #90027, #93494, #76135, .T. ) ;
#10842=FACE_OUTER_BOUND ( 'NONE', #103040, .T. ) ;
#10850=AXIS2_PLACEMENT_3D ( 'NONE', #42365, #106564, #32715 ) ;
#10869=EDGE_LOOP ( 'NONE', ( #89444, #59402, #32070, #30606, #40797, #85016 ) ) ;
#10873=DIRECTION ( 'NONE',  ( -0.5735764363510512664, 0.8191520442889881348, 1.003171929053520309E-16 ) ) ;
#10878=ADVANCED_FACE ( 'NONE', ( #84772 ), #34663, .T. ) ;
#10895=CYLINDRICAL_SURFACE ( 'NONE', #94624, 5.000000000000002665 ) ;
#10923=CARTESIAN_POINT ( 'NONE',  ( 15.75384615384615294, 4.172000000000003261, 0.000000000000000000 ) ) ;
#10994=CYLINDRICAL_SURFACE ( 'NONE', #1925, 5.000000000000002665 ) ;
#11003=ORIENTED_EDGE ( 'NONE', *, *, #75155, .F. ) ;
#11034=CIRCLE ( 'NONE', #41992, 4.172000000000001485 ) ;
#11046=EDGE_LOOP ( 'NONE', ( #96340, #59294, #10673, #73708, #61062 ) ) ;
#11060=CARTESIAN_POINT ( 'NONE',  ( 11.31153846153846132, 1.411358822780289120E-15, 0.000000000000000000 ) ) ;
#11065=DIRECTION ( 'NONE',  ( 0.000000000000000000, 1.000000000000000000, 0.000000000000000000 ) ) ;
#11093=DIRECTION ( 'NONE',  ( -1.000000000000000000, -1.224606353822377258E-16, -0.000000000000000000 ) ) ;
#11103=AXIS2_PLACEMENT_3D ( 'NONE', #14874, #7842, #22491 ) ;
#11105=ADVANCED_FACE ( 'NONE', ( #96056 ), #26925, .T. ) ;
#11108=AXIS2_PLACEMENT_3D ( 'NONE', #81696, #74152, #7822 ) ;
#11114=CARTESIAN_POINT ( 'NONE',  ( 14.27307692307692299, -4.171999999999999709, 5.616230220889763424E-16 ) ) ;
#11122=EDGE_LOOP ( 'NONE', ( #42829, #88538, #19052 ) ) ;
#11130=FACE_OUTER_BOUND ( 'NONE', #77142, .T. ) ;
#11140=EDGE_CURVE ( 'NONE', #58193, #98966, #59313, .T. ) ;
#11146=AXIS2_PLACEMENT_3D ( 'NONE', #85368, #68112, #101010 ) ;
#11150=ORIENTED_EDGE ( 'NONE', *, *, #56410, .T. ) ;
#11153=CARTESIAN_POINT ( 'NONE',  ( 0.000000000000000000, 0.000000000000000000, 5.000000000000002665 ) ) ;
#11186=DIRECTION ( 'NONE',  ( -1.000000000000000000, -0.000000000000000000, -0.000000000000000000 ) ) ;
#11192=VECTOR ( 'NONE', #28463, 1000.000000000000000 ) ;
#11193=EDGE_LOOP ( 'NONE', ( #69742, #60668, #92130, #31934, #3059 ) ) ;
#11196=CYLINDRICAL_SURFACE ( 'NONE', #87093, 5.000000000000002665 ) ;
#11209=EDGE_CURVE ( 'NONE', #24250, #95368, #100949, .T. ) ;
#11214=AXIS2_PLACEMENT_3D ( 'NONE', #24240, #97541, #64669 ) ;
#11218=VECTOR ( 'NONE', #21081, 999.9999999999998863 ) ;
#11222=DIRECTION ( 'NONE',  ( 0.5735764363510468256, 0.8191520442889913545, 0.000000000000000000 ) ) ;
#11288=AXIS2_PLACEMENT_3D ( 'NONE', #74113, #35294, #18033 ) ;
#11296=AXIS2_PLACEMENT_3D ( 'NONE', #72505, #41203, #97842 ) ;
#11304=EDGE_LOOP ( 'NONE', ( #64549, #79262, #86103, #12533, #72452 ) ) ;
#11330=EDGE_CURVE ( 'NONE', #78717, #62030, #39819, .T. ) ;
#11352=ADVANCED_FACE ( 'NONE', ( #38247, #105592 ), #22600, .T. ) ;
#11370=CARTESIAN_POINT ( 'NONE',  ( 40.92692307692308162, -4.171999999999999709, 5.616230220889763424E-16 ) ) ;
#11376=CIRCLE ( 'NONE', #78531, 4.172000000000001485 ) ;
#11393=DIRECTION ( 'NONE',  ( -1.000000000000000000, -0.000000000000000000, -0.000000000000000000 ) ) ;
#11398=DIRECTION ( 'NONE',  ( 0.000000000000000000, -1.000000000000000000, 0.000000000000000000 ) ) ;
#11413=EDGE_CURVE ( 'NONE', #95368, #85900, #75066, .T. ) ;
#11421=DIRECTION ( 'NONE',  ( -1.000000000000000000, -1.224606353822377258E-16, -0.000000000000000000 ) ) ;
#11501=DIRECTION ( 'NONE',  ( 1.000000000000000000, 1.224606353822377258E-16, 0.000000000000000000 ) ) ;
#11505=DIRECTION ( 'NONE',  ( 0.000000000000000000, -1.000000000000000000, 0.000000000000000000 ) ) ;
#11518=DIRECTION ( 'NONE',  ( 1.734723475976806108E-16, -1.000000000000000000, 0.000000000000000000 ) ) ;
#11524=DIRECTION ( 'NONE',  ( -1.000000000000000000, -0.000000000000000000, -0.000000000000000000 ) ) ;
#11553=B_SPLINE_CURVE_WITH_KNOTS ( 'NONE', 3,
 ( #73729, #91005, #40839, #25224, #57537, #81806, #7398, #98538 ),
 .UNSPECIFIED., .F., .F.,
 ( 4, 2, 2, 4 ),
 ( 0.02285338878549945940, 0.02519297481083175236, 0.02636276782349789710, 0.02753256083616404531 ),
 .UNSPECIFIED. ) ;
#11554=CARTESIAN_POINT ( 'NONE',  ( 29.08076923076923137, 1.411358822780289120E-15, 0.000000000000000000 ) ) ;
#11558=CARTESIAN_POINT ( 'NONE',  ( 13.69330508143927538, 1.340359594676612611E-15, 0.000000000000000000 ) ) ;
#11578=CARTESIAN_POINT ( 'NONE',  ( 29.08076923076923137, -4.171999999999999709, 0.000000000000000000 ) ) ;
#11582=ORIENTED_EDGE ( 'NONE', *, *, #75895, .T. ) ;
#11591=DIRECTION ( 'NONE',  ( -1.000000000000000000, -1.224606353822377258E-16, -0.000000000000000000 ) ) ;
#11596=DIRECTION ( 'NONE',  ( 0.000000000000000000, 0.000000000000000000, -1.000000000000000000 ) ) ;
#11615=CONICAL_SURFACE ( 'NONE', #35774, 5.000000000000001776, 0.9599310885968803664 ) ;
#11620=DIRECTION ( 'NONE',  ( -1.000000000000000000, -1.224606353822377258E-16, -0.000000000000000000 ) ) ;
#11672=EDGE_CURVE ( 'NONE', #19372, #62030, #95782, .T. ) ;
#11693=AXIS2_PLACEMENT_3D ( 'NONE', #68508, #10766, #101399 ) ;
#11727=ORIENTED_EDGE ( 'NONE', *, *, #69410, .F. ) ;
#11738=CARTESIAN_POINT ( 'NONE',  ( 18.71538461538461462, 1.411358822780289120E-15, 0.000000000000000000 ) ) ;
#11739=CIRCLE ( 'NONE', #37609, 4.172000000000001485 ) ;
#11742=AXIS2_PLACEMENT_3D ( 'NONE', #43593, #39106, #10677 ) ;
#11758=VERTEX_POINT ( 'NONE', #1405 ) ;
#11809=FACE_OUTER_BOUND ( 'NONE', #67899, .T. ) ;
#11919=AXIS2_PLACEMENT_3D ( 'NONE', #90054, #87033, #5039 ) ;
#11939=AXIS2_PLACEMENT_3D ( 'NONE', #2869, #10429, #59541 ) ;
#11946=DIRECTION ( 'NONE',  ( -1.000000000000000000, -0.000000000000000000, -0.000000000000000000 ) ) ;
#11958=CARTESIAN_POINT ( 'NONE',  ( 24.05868969682389036, 1.340359594676612611E-15, 0.000000000000000000 ) ) ;
#11963=DIRECTION ( 'NONE',  ( 0.000000000000000000, -1.000000000000000000, 0.000000000000000000 ) ) ;
#11970=EDGE_CURVE ( 'NONE', #52425, #48048, #10461, .T. ) ;
#12028=ADVANCED_FACE ( 'NONE', ( #103325 ), #62346, .T. ) ;
#12085=CIRCLE ( 'NONE', #23273, 5.000000000000001776 ) ;
#12124=DIRECTION ( 'NONE',  ( 0.5735764363510468256, 0.8191520442889913545, 0.000000000000000000 ) ) ;
#12130=LINE ( 'NONE', #4586, #31031 ) ;
#12145=DIRECTION ( 'NONE',  ( 0.000000000000000000, 0.000000000000000000, 1.000000000000000000 ) ) ;
#12146=ORIENTED_EDGE ( 'NONE', *, *, #74226, .T. ) ;
#12170=CARTESIAN_POINT ( 'NONE',  ( 23.15769230769230802, 1.411358822780289120E-15, 0.000000000000000000 ) ) ;
#12178=AXIS2_PLACEMENT_3D ( 'NONE', #49321, #82229, #106503 ) ;
#12253=EDGE_CURVE ( 'NONE', #48472, #12693, #56867, .T. ) ;
#12271=ORIENTED_EDGE ( 'NONE', *, *, #72420, .T. ) ;
#12276=EDGE_CURVE ( 'NONE', #35868, #106280, #8771, .T. ) ;
#12310=ORIENTED_EDGE ( 'NONE', *, *, #64504, .T. ) ;
#12333=ORIENTED_EDGE ( 'NONE', *, *, #17161, .T. ) ;
#12337=DIRECTION ( 'NONE',  ( 0.000000000000000000, -1.000000000000000000, 0.000000000000000000 ) ) ;
#12344=EDGE_CURVE ( 'NONE', #42513, #58193, #84271, .T. ) ;
#12379=LINE ( 'NONE', #62549, #60398 ) ;
#12455=ORIENTED_EDGE ( 'NONE', *, *, #27425, .T. ) ;
#12482=CARTESIAN_POINT ( 'NONE',  ( 0.4964154566687890013, 4.996589667937373136, 7.345652830558761615 ) ) ;
#12485=DIRECTION ( 'NONE',  ( 0.000000000000000000, 0.000000000000000000, -1.000000000000000000 ) ) ;
#12488=CARTESIAN_POINT ( 'NONE',  ( 22.57792046605466041, 1.340359594676612611E-15, 0.000000000000000000 ) ) ;
#12503=ADVANCED_FACE ( 'NONE', ( #70301 ), #82502, .T. ) ;
#12533=ORIENTED_EDGE ( 'NONE', *, *, #807, .F. ) ;
#12536=CIRCLE ( 'NONE', #24668, 5.000000000000001776 ) ;
#12568=FACE_OUTER_BOUND ( 'NONE', #1037, .T. ) ;
#12573=ORIENTED_EDGE ( 'NONE', *, *, #11413, .F. ) ;
#12589=AXIS2_PLACEMENT_3D ( 'NONE', #59311, #2644, #44188 ) ;
#12610=DIRECTION ( 'NONE',  ( -1.000000000000000000, -1.224606353822377258E-16, -0.000000000000000000 ) ) ;
#12636=CARTESIAN_POINT ( 'NONE',  ( 40.92692307692308162, 1.411358822780289120E-15, 0.000000000000000000 ) ) ;
#12690=VERTEX_POINT ( 'NONE', #71873 ) ;
#12693=VERTEX_POINT ( 'NONE', #7656 ) ;
#12699=CARTESIAN_POINT ( 'NONE',  ( 29.98176661990081371, 1.340359594676612611E-15, 0.000000000000000000 ) ) ;
#12710=ADVANCED_FACE ( 'NONE', ( #80486 ), #6712, .T. ) ;
#12712=ORIENTED_EDGE ( 'NONE', *, *, #43450, .F. ) ;
#12724=ORIENTED_EDGE ( 'NONE', *, *, #72401, .F. ) ;
#12745=DIRECTION ( 'NONE',  ( -1.000000000000000000, -1.224606353822377258E-16, -0.000000000000000000 ) ) ;
#12756=DIRECTION ( 'NONE',  ( -1.000000000000000000, -1.224606353822377258E-16, -0.000000000000000000 ) ) ;
#12783=ADVANCED_FACE ( 'NONE', ( #67521 ), #104894, .T. ) ;
#12793=VERTEX_POINT ( 'NONE', #10323 ) ;
#12802=EDGE_LOOP ( 'NONE', ( #72566, #68423, #38087, #7104, #2271 ) ) ;
#12854=ORIENTED_EDGE ( 'NONE', *, *, #18507, .F. ) ;
#12855=EDGE_CURVE ( 'NONE', #81401, #1618, #31331, .T. ) ;
#12857=CARTESIAN_POINT ( 'NONE',  ( 39.44615384615384812, -4.171999999999999709, 0.000000000000000000 ) ) ;
#12870=CARTESIAN_POINT ( 'NONE',  ( 24.63846153846153797, 1.411358822780289120E-15, 0.000000000000000000 ) ) ;
#12890=FACE_OUTER_BOUND ( 'NONE', #103743, .T. ) ;
#12910=AXIS2_PLACEMENT_3D ( 'NONE', #99038, #11093, #18711 ) ;
#12914=AXIS2_PLACEMENT_3D ( 'NONE', #21853, #55746, #38554 ) ;
#12926=CARTESIAN_POINT ( 'NONE',  ( 21.67692307692307452, 1.411358822780289120E-15, 0.000000000000000000 ) ) ;
#12939=ORIENTED_EDGE ( 'NONE', *, *, #95754, .F. ) ;
#12943=CARTESIAN_POINT ( 'NONE',  ( 38.54515645702225868, 3.851859888774471706E-31, 5.000000000000001776 ) ) ;
#12944=ORIENTED_EDGE ( 'NONE', *, *, #20820, .F. ) ;
#12950=DIRECTION ( 'NONE',  ( 1.000000000000000000, 1.224606353822377258E-16, 0.000000000000000000 ) ) ;
#12954=CARTESIAN_POINT ( 'NONE',  ( 6.249999999999998224, 1.502314598737158834E-15, -7.999999999999998224 ) ) ;
#12994=ORIENTED_EDGE ( 'NONE', *, *, #33671, .T. ) ;
#13007=ORIENTED_EDGE ( 'NONE', *, *, #102184, .F. ) ;
#13019=CARTESIAN_POINT ( 'NONE',  ( 42.98746414932995208, -5.000000000000000888, 6.123233995736769241E-16 ) ) ;
#13040=AXIS2_PLACEMENT_3D ( 'NONE', #45702, #55878, #46759 ) ;
#13086=AXIS2_PLACEMENT_3D ( 'NONE', #4790, #27514, #69007 ) ;
#13122=EDGE_CURVE ( 'NONE', #58651, #96607, #10468, .T. ) ;
#13133=VERTEX_POINT ( 'NONE', #44451 ) ;
#13144=CIRCLE ( 'NONE', #16624, 5.000000000000001776 ) ;
#13163=EDGE_CURVE ( 'NONE', #4002, #13133, #102488, .T. ) ;
#13182=DIRECTION ( 'NONE',  ( 0.000000000000000000, 0.000000000000000000, 1.000000000000000000 ) ) ;
#13214=CARTESIAN_POINT ( 'NONE',  ( 41.50669491856072568, 6.123233995736772199E-16, -5.000000000000001776 ) ) ;
#13228=AXIS2_PLACEMENT_3D ( 'NONE', #7661, #9262, #16297 ) ;
#13270=CARTESIAN_POINT ( 'NONE',  ( 35.58361799548379167, 5.000000000000002665, 0.000000000000000000 ) ) ;
#13280=CARTESIAN_POINT ( 'NONE',  ( 17.23461538461538467, 1.411358822780289120E-15, 0.000000000000000000 ) ) ;
#13298=EDGE_LOOP ( 'NONE', ( #21950, #42109, #63129, #30414, #40022 ) ) ;
#13368=LINE ( 'NONE', #70576, #79355 ) ;
#13375=DIRECTION ( 'NONE',  ( -1.000000000000000000, -0.000000000000000000, -0.000000000000000000 ) ) ;
#13376=CIRCLE ( 'NONE', #92611, 5.000000000000002665 ) ;
#13379=DIRECTION ( 'NONE',  ( 0.000000000000000000, -1.000000000000000000, 0.000000000000000000 ) ) ;
#13424=CARTESIAN_POINT ( 'NONE',  ( 0.7145311798163210826, 4.618802153517001408, -8.000000000000000000 ) ) ;
#13425=EDGE_CURVE ( 'NONE', #53278, #67995, #2546, .T. ) ;
#13438=DIRECTION ( 'NONE',  ( -1.000000000000000000, -0.000000000000000000, -0.000000000000000000 ) ) ;
#13440=ORIENTED_EDGE ( 'NONE', *, *, #100852, .F. ) ;
#13460=DIRECTION ( 'NONE',  ( 0.5735764363510468256, 0.8191520442889913545, 0.000000000000000000 ) ) ;
#13549=CONICAL_SURFACE ( 'NONE', #65221, 5.000000000000001776, 0.9599310885968803664 ) ;
#13553=AXIS2_PLACEMENT_3D ( 'NONE', #100885, #27049, #59934 ) ;
#13562=CONICAL_SURFACE ( 'NONE', #44628, 4.172000000000001485, 0.9599310885968750373 ) ;
#13574=CARTESIAN_POINT ( 'NONE',  ( 21.09715123528542691, 5.000000000000004441, 6.123233995736770227E-16 ) ) ;
#13600=VERTEX_POINT ( 'NONE', #78284 ) ;
#13609=FACE_OUTER_BOUND ( 'NONE', #63895, .T. ) ;
#13626=CARTESIAN_POINT ( 'NONE',  ( 0.000000000000000000, 0.000000000000000000, 0.000000000000000000 ) ) ;
#13630=CARTESIAN_POINT ( 'NONE',  ( 45.94900261086841198, 1.482358050883964840E-15, 0.000000000000000000 ) ) ;
#13659=DIRECTION ( 'NONE',  ( -1.000000000000000000, -1.224606353822377258E-16, -0.000000000000000000 ) ) ;
#13664=EDGE_CURVE ( 'NONE', #106696, #77934, #30203, .T. ) ;
#13684=CARTESIAN_POINT ( 'NONE',  ( 16.65484354297773351, -5.000000000000000000, 0.000000000000000000 ) ) ;
#13699=VECTOR ( 'NONE', #13375, 1000.000000000000000 ) ;
#13709=VERTEX_POINT ( 'NONE', #97117 ) ;
#13763=DIRECTION ( 'NONE',  ( -1.000000000000000000, -1.224606353822377258E-16, -0.000000000000000000 ) ) ;
#13782=EDGE_CURVE ( 'NONE', #19325, #45319, #14695, .T. ) ;
#13783=EDGE_LOOP ( 'NONE', ( #77580, #88427, #82724, #49959, #2734 ) ) ;
#13790=AXIS2_PLACEMENT_3D ( 'NONE', #47462, #95499, #39924 ) ;
#13798=VERTEX_POINT ( 'NONE', #31879 ) ;
#13812=VERTEX_POINT ( 'NONE', #24851 ) ;
#13898=DIRECTION ( 'NONE',  ( 1.000000000000000000, 1.224606353822377258E-16, 0.000000000000000000 ) ) ;
#13941=VECTOR ( 'NONE', #71665, 1000.000000000000000 ) ;
#13972=ADVANCED_FACE ( 'NONE', ( #90229 ), #102644, .T. ) ;
#14005=DIRECTION ( 'NONE',  ( 0.000000000000000000, -1.000000000000000000, 0.000000000000000000 ) ) ;
#14023=AXIS2_PLACEMENT_3D ( 'NONE', #63593, #77640, #96482 ) ;
#14055=DIRECTION ( 'NONE',  ( -1.000000000000000000, -0.000000000000000000, -0.000000000000000000 ) ) ;
#14077=EDGE_LOOP ( 'NONE', ( #52730, #10744, #78900, #27368, #95321 ) ) ;
#14088=CARTESIAN_POINT ( 'NONE',  ( 15.75384615384615294, 4.172000000000003261, 5.109226446042759579E-16 ) ) ;
#14104=ORIENTED_EDGE ( 'NONE', *, *, #7127, .F. ) ;
#14114=LINE ( 'NONE', #3925, #52810 ) ;
#14132=ADVANCED_FACE ( 'NONE', ( #106393 ), #68147, .T. ) ;
#14152=VERTEX_POINT ( 'NONE', #9292 ) ;
#14178=DIRECTION ( 'NONE',  ( -0.5735764363510512664, 0.8191520442889881348, 1.003171929053520309E-16 ) ) ;
#14187=ORIENTED_EDGE ( 'NONE', *, *, #86062, .F. ) ;
#14201=EDGE_CURVE ( 'NONE', #1618, #14152, #73273, .T. ) ;
#14206=AXIS2_PLACEMENT_3D ( 'NONE', #62247, #104254, #45519 ) ;
#14221=ORIENTED_EDGE ( 'NONE', *, *, #33519, .F. ) ;
#14225=DIRECTION ( 'NONE',  ( 1.000000000000000000, 1.224606353822377258E-16, 0.000000000000000000 ) ) ;
#14275=DIRECTION ( 'NONE',  ( 1.000000000000000000, 0.000000000000000000, -0.000000000000000000 ) ) ;
#14278=VECTOR ( 'NONE', #20367, 1000.000000000000000 ) ;
#14340=CIRCLE ( 'NONE', #74627, 5.000000000000001776 ) ;
#14362=EDGE_CURVE ( 'NONE', #98844, #29601, #104318, .T. ) ;
#14365=CARTESIAN_POINT ( 'NONE',  ( 11.89131030317610183, 1.482358050883964840E-15, 0.000000000000000000 ) ) ;
#14403=DIRECTION ( 'NONE',  ( -1.000000000000000000, -0.000000000000000000, -0.000000000000000000 ) ) ;
#14422=DIRECTION ( 'NONE',  ( -1.000000000000000000, -1.224606353822377258E-16, -0.000000000000000000 ) ) ;
#14425=EDGE_CURVE ( 'NONE', #13798, #19325, #100854, .T. ) ;
#14430=DIRECTION ( 'NONE',  ( 0.000000000000000000, 1.000000000000000000, 0.000000000000000000 ) ) ;
#14475=AXIS2_PLACEMENT_3D ( 'NONE', #101898, #43143, #44209 ) ;
#14487=EDGE_CURVE ( 'NONE', #41603, #29093, #104400, .T. ) ;
#14488=DIRECTION ( 'NONE',  ( 0.5735764363510468256, 0.8191520442889913545, 0.000000000000000000 ) ) ;
#14496=ADVANCED_FACE ( 'NONE', ( #106411 ), #66521, .T. ) ;
#14533=DIRECTION ( 'NONE',  ( 0.000000000000000000, -1.000000000000000000, 0.000000000000000000 ) ) ;
#14538=CARTESIAN_POINT ( 'NONE',  ( 0.000000000000000000, 0.000000000000000000, 0.000000000000000000 ) ) ;
#14564=EDGE_LOOP ( 'NONE', ( #88890, #95619, #23379, #52815, #47729 ) ) ;
#14582=EDGE_CURVE ( 'NONE', #95530, #42925, #82552, .T. ) ;
#14585=ORIENTED_EDGE ( 'NONE', *, *, #32180, .F. ) ;
#14630=CONICAL_SURFACE ( 'NONE', #62882, 4.172000000000001485, 0.9599310885968750373 ) ;
#14656=CIRCLE ( 'NONE', #856, 4.172000000000001485 ) ;
#14677=EDGE_CURVE ( 'NONE', #77056, #45751, #35531, .T. ) ;
#14681=DIRECTION ( 'NONE',  ( -1.000000000000000000, -0.000000000000000000, -0.000000000000000000 ) ) ;
#14685=CIRCLE ( 'NONE', #38894, 5.000000000000001776 ) ;
#14693=AXIS2_PLACEMENT_3D ( 'NONE', #55423, #47340, #80234 ) ;
#14695=CIRCLE ( 'NONE', #81824, 5.000000000000002665 ) ;
#14709=DIRECTION ( 'NONE',  ( -1.000000000000000000, -1.224606353822377258E-16, -0.000000000000000000 ) ) ;
#14710=FACE_OUTER_BOUND ( 'NONE', #42710, .T. ) ;
#14745=DIRECTION ( 'NONE',  ( 0.000000000000000000, -1.000000000000000000, 0.000000000000000000 ) ) ;
#14771=ADVANCED_FACE ( 'NONE', ( #28079 ), #71147, .T. ) ;
#14796=VERTEX_POINT ( 'NONE', #37762 ) ;
#14830=EDGE_CURVE ( 'NONE', #88025, #40649, #4476, .T. ) ;
#14835=CARTESIAN_POINT ( 'NONE',  ( 29.98176661990081371, 0.000000000000000000, 5.000000000000002665 ) ) ;
#14874=CARTESIAN_POINT ( 'NONE',  ( 26.69900261086841198, 1.482358050883964840E-15, 0.000000000000000000 ) ) ;
#14888=AXIS2_PLACEMENT_3D ( 'NONE', #32795, #49471, #9009 ) ;
#14890=ORIENTED_EDGE ( 'NONE', *, *, #8473, .T. ) ;
#14903=AXIS2_PLACEMENT_3D ( 'NONE', #67202, #101684, #101148 ) ;
#14962=ORIENTED_EDGE ( 'NONE', *, *, #97659, .T. ) ;
#14971=DIRECTION ( 'NONE',  ( -1.000000000000000000, -0.000000000000000000, -0.000000000000000000 ) ) ;
#14983=CARTESIAN_POINT ( 'NONE',  ( 0.000000000000000000, 0.000000000000000000, 0.000000000000000000 ) ) ;
#14985=DIRECTION ( 'NONE',  ( -1.000000000000000000, -1.224606353822377258E-16, -0.000000000000000000 ) ) ;
#15012=CIRCLE ( 'NONE', #101189, 4.172000000000001485 ) ;
#15036=ORIENTED_EDGE ( 'NONE', *, *, #105196, .F. ) ;
#15061=VECTOR ( 'NONE', #50083, 1000.000000000000000 ) ;
#15067=CARTESIAN_POINT ( 'NONE',  ( 29.66054107240687543, -5.000000000000000000, 6.123233995736768255E-16 ) ) ;
#15075=ORIENTED_EDGE ( 'NONE', *, *, #75200, .F. ) ;
#15092=DIRECTION ( 'NONE',  ( -1.000000000000000000, -1.224606353822377258E-16, -0.000000000000000000 ) ) ;
#15095=ORIENTED_EDGE ( 'NONE', *, *, #55747, .F. ) ;
#15107=AXIS2_PLACEMENT_3D ( 'NONE', #92250, #49674, #51260 ) ;
#15113=EDGE_CURVE ( 'NONE', #45889, #3051, #79513, .T. ) ;
#15121=CARTESIAN_POINT ( 'NONE',  ( 42.40769230769231513, 4.172000000000003261, 0.000000000000000000 ) ) ;
#15124=EDGE_CURVE ( 'NONE', #55161, #63565, #45572, .T. ) ;
#15125=CIRCLE ( 'NONE', #23788, 5.000000000000001776 ) ;
#15130=CARTESIAN_POINT ( 'NONE',  ( 40.02592568779148507, 6.123233995736772199E-16, -5.000000000000001776 ) ) ;
#15144=VECTOR ( 'NONE', #28614, 1000.000000000000000 ) ;
#15158=EDGE_CURVE ( 'NONE', #75560, #51764, #49343, .T. ) ;
#15186=AXIS2_PLACEMENT_3D ( 'NONE', #15771, #81024, #7141 ) ;
#15309=EDGE_LOOP ( 'NONE', ( #47730, #74019, #20688, #95280, #103975 ) ) ;
#15337=AXIS2_PLACEMENT_3D ( 'NONE', #91793, #50258, #66443 ) ;
#15347=EDGE_LOOP ( 'NONE', ( #83293, #76470, #25726, #74518, #92935 ) ) ;
#15362=ORIENTED_EDGE ( 'NONE', *, *, #78370, .T. ) ;
#15385=FACE_OUTER_BOUND ( 'NONE', #31760, .T. ) ;
#15456=DIRECTION ( 'NONE',  ( 0.000000000000000000, -1.000000000000000000, 0.000000000000000000 ) ) ;
#15469=LINE ( 'NONE', #65087, #58952 ) ;
#15479=DIRECTION ( 'NONE',  ( -1.000000000000000000, -0.000000000000000000, -0.000000000000000000 ) ) ;
#15509=DIRECTION ( 'NONE',  ( 0.000000000000000000, 0.000000000000000000, 1.000000000000000000 ) ) ;
#15540=VECTOR ( 'NONE', #86495, 1000.000000000000000 ) ;
#15552=CARTESIAN_POINT ( 'NONE',  ( 21.67692307692307452, 4.172000000000003261, 0.000000000000000000 ) ) ;
#15582=ORIENTED_EDGE ( 'NONE', *, *, #29535, .F. ) ;
#15599=DIRECTION ( 'NONE',  ( 0.5735764363510470476, -0.8191520442889911324, 1.003171929053524007E-16 ) ) ;
#15607=CARTESIAN_POINT ( 'NONE',  ( 25.21823338009918203, 1.482358050883964840E-15, 0.000000000000000000 ) ) ;
#15625=VERTEX_POINT ( 'NONE', #13574 ) ;
#15643=DIRECTION ( 'NONE',  ( 0.000000000000000000, -1.000000000000000000, 0.000000000000000000 ) ) ;
#15654=DIRECTION ( 'NONE',  ( -1.000000000000000000, -1.224606353822377258E-16, -0.000000000000000000 ) ) ;
#15670=CIRCLE ( 'NONE', #44965, 4.172000000000001485 ) ;
#15692=SURFACE_STYLE_FILL_AREA ( #89599 ) ;
#15730=ORIENTED_EDGE ( 'NONE', *, *, #70013, .T. ) ;
#15743=DIRECTION ( 'NONE',  ( 0.000000000000000000, 1.000000000000000000, 0.000000000000000000 ) ) ;
#15766=DIRECTION ( 'NONE',  ( -1.000000000000000000, -1.224606353822377258E-16, -0.000000000000000000 ) ) ;
#15771=CARTESIAN_POINT ( 'NONE',  ( 40.92692307692308162, 1.411358822780289120E-15, 0.000000000000000000 ) ) ;
#15774=ORIENTED_EDGE ( 'NONE', *, *, #24625, .T. ) ;
#15784=FACE_OUTER_BOUND ( 'NONE', #43769, .T. ) ;
#15795=EDGE_LOOP ( 'NONE', ( #34786, #36071, #100139, #11003, #69701 ) ) ;
#15800=VECTOR ( 'NONE', #90209, 1000.000000000000000 ) ;
#15804=ORIENTED_EDGE ( 'NONE', *, *, #71346, .T. ) ;
#15863=CARTESIAN_POINT ( 'NONE',  ( 19.61638200451619696, 5.000000000000004441, 6.123233995736770227E-16 ) ) ;
#15865=ADVANCED_FACE ( 'NONE', ( #63081 ), #70640, .T. ) ;
#15892=FACE_OUTER_BOUND ( 'NONE', #66846, .T. ) ;
#15927=EDGE_LOOP ( 'NONE', ( #55495, #52244, #64431 ) ) ;
#15949=AXIS2_PLACEMENT_3D ( 'NONE', #20414, #75927, #53258 ) ;
#15953=AXIS2_PLACEMENT_3D ( 'NONE', #37967, #54610, #6609 ) ;
#15966=ORIENTED_EDGE ( 'NONE', *, *, #56368, .F. ) ;
#15996=EDGE_CURVE ( 'NONE', #63024, #71240, #47608, .T. ) ;
#16030=ORIENTED_EDGE ( 'NONE', *, *, #89402, .F. ) ;
#16031=EDGE_LOOP ( 'NONE', ( #61422, #77537, #27839, #41532, #8378, #83597 ) ) ;
#16045=DIRECTION ( 'NONE',  ( 1.000000000000000000, 0.000000000000000000, 0.000000000000000000 ) ) ;
#16079=FACE_OUTER_BOUND ( 'NONE', #81506, .T. ) ;
#16081=DIRECTION ( 'NONE',  ( 0.000000000000000000, 1.000000000000000000, 0.000000000000000000 ) ) ;
#16088=EDGE_CURVE ( 'NONE', #48472, #9392, #11034, .T. ) ;
#16094=AXIS2_PLACEMENT_3D ( 'NONE', #20301, #36996, #11065 ) ;
#16096=CARTESIAN_POINT ( 'NONE',  ( 9.250997389131581983, 1.340359594676612611E-15, 0.000000000000000000 ) ) ;
#16100=ORIENTED_EDGE ( 'NONE', *, *, #94161, .T. ) ;
#16105=ORIENTED_EDGE ( 'NONE', *, *, #68196, .F. ) ;
#16111=EDGE_LOOP ( 'NONE', ( #103322, #92492, #101614, #97977, #14187, #94699 ) ) ;
#16121=LINE ( 'NONE', #40932, #15061 ) ;
#16161=LINE ( 'NONE', #76932, #22466 ) ;
#16201=( GEOMETRIC_REPRESENTATION_CONTEXT ( 3 ) GLOBAL_UNCERTAINTY_ASSIGNED_CONTEXT ( ( #90975 ) ) GLOBAL_UNIT_ASSIGNED_CONTEXT ( ( #100830, #67428, #16739 ) ) REPRESENTATION_CONTEXT ( 'NONE', 'WORKASPACE' ) );
#16205=ADVANCED_FACE ( 'NONE', ( #85306 ), #58915, .T. ) ;
#16235=EDGE_LOOP ( 'NONE', ( #27180, #23625, #45310, #84678, #55412 ) ) ;
#16274=FACE_OUTER_BOUND ( 'NONE', #88106, .T. ) ;
#16279=CONICAL_SURFACE ( 'NONE', #69653, 4.172000000000001485, 0.9599310885968750373 ) ;
#16297=DIRECTION ( 'NONE',  ( 0.000000000000000000, -1.000000000000000000, 0.000000000000000000 ) ) ;
#16326=AXIS2_PLACEMENT_3D ( 'NONE', #93540, #34794, #26183 ) ;
#16329=CARTESIAN_POINT ( 'NONE',  ( 32.62207953394533178, 1.482358050883964840E-15, 0.000000000000000000 ) ) ;
#16350=AXIS2_PLACEMENT_3D ( 'NONE', #100300, #67943, #26992 ) ;
#16380=ADVANCED_FACE ( 'NONE', ( #64231 ), #67870, .T. ) ;
#16386=VERTEX_POINT ( 'NONE', #6492 ) ;
#16400=DIRECTION ( 'NONE',  ( 1.000000000000000000, 0.000000000000000000, -0.000000000000000000 ) ) ;
#16414=ORIENTED_EDGE ( 'NONE', *, *, #76256, .T. ) ;
#16422=DIRECTION ( 'NONE',  ( 0.000000000000000000, 0.000000000000000000, 1.000000000000000000 ) ) ;
#16424=VERTEX_POINT ( 'NONE', #65804 ) ;
#16452=VERTEX_POINT ( 'NONE', #15121 ) ;
#16457=CONICAL_SURFACE ( 'NONE', #99125, 5.000000000000001776, 0.9599310885968803664 ) ;
#16539=UNCERTAINTY_MEASURE_WITH_UNIT (LENGTH_MEASURE( 1.000000000000000082E-05 ), #17816, 'distance_accuracy_value', 'NONE');
#16608=ADVANCED_FACE ( 'NONE', ( #1023 ), #23161, .T. ) ;
#16620=DIRECTION ( 'NONE',  ( -1.000000000000000000, -1.224606353822377258E-16, -0.000000000000000000 ) ) ;
#16624=AXIS2_PLACEMENT_3D ( 'NONE', #47017, #22255, #61655 ) ;
#16626=CONICAL_SURFACE ( 'NONE', #47568, 4.172000000000001485, 0.9599310885968750373 ) ;
#16632=LINE ( 'NONE', #97528, #63951 ) ;
#16633=DIRECTION ( 'NONE',  ( 0.000000000000000000, -1.000000000000000000, 0.000000000000000000 ) ) ;
#16640=DIRECTION ( 'NONE',  ( 0.000000000000000000, 0.000000000000000000, 1.000000000000000000 ) ) ;
#16657=CARTESIAN_POINT ( 'NONE',  ( 26.11923076923076792, 1.411358822780289120E-15, 0.000000000000000000 ) ) ;
#16671=AXIS2_PLACEMENT_3D ( 'NONE', #92483, #51493, #2940 ) ;
#16695=ORIENTED_EDGE ( 'NONE', *, *, #28939, .F. ) ;
#16733=CARTESIAN_POINT ( 'NONE',  ( 37.06438722625302518, -5.000000000000000000, 6.123233995736768255E-16 ) ) ;
#16739=( NAMED_UNIT ( * ) SI_UNIT ( $, .STERADIAN. ) SOLID_ANGLE_UNIT ( ) );
#16747=DIRECTION ( 'NONE',  ( 0.000000000000000000, -1.000000000000000000, 0.000000000000000000 ) ) ;
#16760=ORIENTED_EDGE ( 'NONE', *, *, #91938, .F. ) ;
#16770=CARTESIAN_POINT ( 'NONE',  ( 0.000000000000000000, 0.000000000000000000, 0.000000000000000000 ) ) ;
#16776=ORIENTED_EDGE ( 'NONE', *, *, #69071, .F. ) ;
#16792=DIRECTION ( 'NONE',  ( 0.000000000000000000, -1.000000000000000000, 0.000000000000000000 ) ) ;
#16816=VECTOR ( 'NONE', #70586, 1000.000000000000000 ) ;
#16821=ADVANCED_FACE ( 'NONE', ( #87309 ), #16279, .T. ) ;
#16824=DIRECTION ( 'NONE',  ( -0.5735764363510510444, -0.8191520442889883569, 0.000000000000000000 ) ) ;
#16863=DIRECTION ( 'NONE',  ( -0.000000000000000000, 0.000000000000000000, 1.000000000000000000 ) ) ;
#16879=CARTESIAN_POINT ( 'NONE',  ( 18.71538461538461462, 1.411358822780289120E-15, 0.000000000000000000 ) ) ;
#16883=CARTESIAN_POINT ( 'NONE',  ( 45.94900261086841198, 1.482358050883964840E-15, 0.000000000000000000 ) ) ;
#16914=VECTOR ( 'NONE', #13460, 999.9999999999998863 ) ;
#16927=CIRCLE ( 'NONE', #94388, 5.000000000000002665 ) ;
#16937=ORIENTED_EDGE ( 'NONE', *, *, #77466, .T. ) ;
#16977=ADVANCED_FACE ( 'NONE', ( #64109 ), #73757, .T. ) ;
#16978=CARTESIAN_POINT ( 'NONE',  ( 23.15769230769230802, -4.171999999999999709, 5.616230220889763424E-16 ) ) ;
#16986=CARTESIAN_POINT ( 'NONE',  ( 22.25669491856071858, 6.123233995736772199E-16, -5.000000000000001776 ) ) ;
#17010=ORIENTED_EDGE ( 'NONE', *, *, #105904, .T. ) ;
#17016=CARTESIAN_POINT ( 'NONE',  ( 35.00384615384614762, -4.171999999999999709, 0.000000000000000000 ) ) ;
#17023=EDGE_LOOP ( 'NONE', ( #63418, #40567, #3669, #76789, #52329 ) ) ;
#17034=AXIS2_PLACEMENT_3D ( 'NONE', #64339, #15766, #7657 ) ;
#17041=AXIS2_PLACEMENT_3D ( 'NONE', #75289, #2463, #83385 ) ;
#17094=AXIS2_PLACEMENT_3D ( 'NONE', #55599, #72341, #23284 ) ;
#17101=CARTESIAN_POINT ( 'NONE',  ( 18.13561277374696701, 1.340359594676612611E-15, 0.000000000000000000 ) ) ;
#17107=EDGE_CURVE ( 'NONE', #75282, #5164, #9170, .T. ) ;
#17113=ORIENTED_EDGE ( 'NONE', *, *, #22161, .T. ) ;
#17115=CARTESIAN_POINT ( 'NONE',  ( 19.29515645702225868, 5.000000000000003553, 0.000000000000000000 ) ) ;
#17135=DIRECTION ( 'NONE',  ( -1.000000000000000000, -0.000000000000000000, -0.000000000000000000 ) ) ;
#17154=CARTESIAN_POINT ( 'NONE',  ( 36.48461538461538822, 1.411358822780289120E-15, 0.000000000000000000 ) ) ;
#17157=CYLINDRICAL_SURFACE ( 'NONE', #29689, 5.000000000000002665 ) ;
#17161=EDGE_CURVE ( 'NONE', #18270, #87322, #43536, .T. ) ;
#17181=CARTESIAN_POINT ( 'NONE',  ( 30.56153846153846132, 1.411358822780289120E-15, 0.000000000000000000 ) ) ;
#17189=FACE_OUTER_BOUND ( 'NONE', #29690, .T. ) ;
#17197=ORIENTED_EDGE ( 'NONE', *, *, #103518, .T. ) ;
#17199=VERTEX_POINT ( 'NONE', #25249 ) ;
#17204=ORIENTED_EDGE ( 'NONE', *, *, #81339, .F. ) ;
#17221=DIRECTION ( 'NONE',  ( 0.000000000000000000, -1.000000000000000000, 0.000000000000000000 ) ) ;
#17228=ORIENTED_EDGE ( 'NONE', *, *, #62201, .F. ) ;
#17288=EDGE_CURVE ( 'NONE', #18270, #91139, #93147, .T. ) ;
#17306=LINE ( 'NONE', #83085, #88030 ) ;
#17342=EDGE_CURVE ( 'NONE', #99464, #21850, #40218, .T. ) ;
#17395=LINE ( 'NONE', #59449, #63214 ) ;
#17403=DIRECTION ( 'NONE',  ( 1.734723475976806108E-16, -1.000000000000000000, 0.000000000000000000 ) ) ;
#17421=LINE ( 'NONE', #42207, #41287 ) ;
#17456=EDGE_CURVE ( 'NONE', #25785, #22430, #57373, .T. ) ;
#17491=CARTESIAN_POINT ( 'NONE',  ( 16.33361799548379523, 1.482358050883964840E-15, 0.000000000000000000 ) ) ;
#17492=CARTESIAN_POINT ( 'NONE',  ( 14.85284876471456350, -5.000000000000000888, 6.123233995736769241E-16 ) ) ;
#17513=AXIS2_PLACEMENT_3D ( 'NONE', #9548, #75348, #51066 ) ;
#17518=DIRECTION ( 'NONE',  ( 1.000000000000000000, 1.224606353822377258E-16, 0.000000000000000000 ) ) ;
#17546=AXIS2_PLACEMENT_3D ( 'NONE', #88442, #24259, #40938 ) ;
#17562=CARTESIAN_POINT ( 'NONE',  ( 35.90484354297773706, 1.340359594676612611E-15, 0.000000000000000000 ) ) ;
#17576=CARTESIAN_POINT ( 'NONE',  ( 13.69330508143927538, -5.000000000000000000, 0.000000000000000000 ) ) ;
#17585=AXIS2_PLACEMENT_3D ( 'NONE', #16879, #42737, #98828 ) ;
#17668=DIRECTION ( 'NONE',  ( 0.000000000000000000, -1.000000000000000000, 0.000000000000000000 ) ) ;
#17674=VERTEX_POINT ( 'NONE', #101105 ) ;
#17717=DIRECTION ( 'NONE',  ( -1.000000000000000000, -1.224606353822377258E-16, -0.000000000000000000 ) ) ;
#17727=VECTOR ( 'NONE', #71539, 1000.000000000000000 ) ;
#17753=ORIENTED_EDGE ( 'NONE', *, *, #89247, .T. ) ;
#17768=ORIENTED_EDGE ( 'NONE', *, *, #91249, .T. ) ;
#17774=ORIENTED_EDGE ( 'NONE', *, *, #18862, .F. ) ;
#17787=DIRECTION ( 'NONE',  ( 0.000000000000000000, 1.000000000000000000, 0.000000000000000000 ) ) ;
#17792=DIRECTION ( 'NONE',  ( -1.000000000000000000, -1.224606353822377258E-16, -0.000000000000000000 ) ) ;
#17795=DIRECTION ( 'NONE',  ( 0.000000000000000000, -1.000000000000000000, 0.000000000000000000 ) ) ;
#17816=( LENGTH_UNIT ( ) NAMED_UNIT ( * ) SI_UNIT ( .MILLI., .METRE. ) );
#17818=CIRCLE ( 'NONE', #105635, 4.172000000000001485 ) ;
#17825=CARTESIAN_POINT ( 'NONE',  ( 46.02200000000003399, 0.000000000000000000, 5.000000000000004441 ) ) ;
#17833=VECTOR ( 'NONE', #66743, 1000.000000000000227 ) ;
#17834=EDGE_CURVE ( 'NONE', #43261, #49147, #82534, .T. ) ;
#17840=ORIENTED_EDGE ( 'NONE', *, *, #102333, .T. ) ;
#17867=CARTESIAN_POINT ( 'NONE',  ( 41.50669491856072568, 1.482358050883964840E-15, 0.000000000000000000 ) ) ;
#17871=CARTESIAN_POINT ( 'NONE',  ( 19.61638200451619696, 6.123233995736770227E-16, -5.000000000000002665 ) ) ;
#17893=CARTESIAN_POINT ( 'NONE',  ( 0.7145311798163270778, 9.237604307034018802, 2.885982852862873934E-16 ) ) ;
#17899=DIRECTION ( 'NONE',  ( -0.5735764363510510444, -0.8191520442889883569, 0.000000000000000000 ) ) ;
#17932=LINE ( 'NONE', #65404, #15800 ) ;
#17952=EDGE_CURVE ( 'NONE', #6487, #6569, #42063, .T. ) ;
#17958=DIRECTION ( 'NONE',  ( 0.000000000000000000, -1.000000000000000000, 0.000000000000000000 ) ) ;
#17968=ORIENTED_EDGE ( 'NONE', *, *, #106108, .F. ) ;
#17979=DIRECTION ( 'NONE',  ( -0.5735764363510510444, -0.8191520442889883569, 0.000000000000000000 ) ) ;
#17984=AXIS2_PLACEMENT_3D ( 'NONE', #105219, #80929, #46968 ) ;
#18009=ORIENTED_EDGE ( 'NONE', *, *, #62607, .F. ) ;
#18033=DIRECTION ( 'NONE',  ( 0.000000000000000000, 0.000000000000000000, -1.000000000000000000 ) ) ;
#18085=DIRECTION ( 'NONE',  ( -1.000000000000000000, -1.224606353822377258E-16, -0.000000000000000000 ) ) ;
#18089=CARTESIAN_POINT ( 'NONE',  ( 19.29515645702225868, 1.482358050883964840E-15, 0.000000000000000000 ) ) ;
#18090=ORIENTED_EDGE ( 'NONE', *, *, #43802, .F. ) ;
#18105=CARTESIAN_POINT ( 'NONE',  ( 34.10284876471455817, 5.000000000000003553, 0.000000000000000000 ) ) ;
#18116=EDGE_LOOP ( 'NONE', ( #87553, #46351, #46931, #1380, #31859, #90225 ) ) ;
#18136=FACE_OUTER_BOUND ( 'NONE', #59587, .T. ) ;
#18256=ORIENTED_EDGE ( 'NONE', *, *, #36894, .F. ) ;
#18270=VERTEX_POINT ( 'NONE', #68904 ) ;
#18293=CARTESIAN_POINT ( 'NONE',  ( 24.05868969682389036, 5.000000000000004441, 6.123233995736770227E-16 ) ) ;
#18329=EDGE_LOOP ( 'NONE', ( #18009, #91946, #80374, #83191, #98438 ) ) ;
#18335=DIRECTION ( 'NONE',  ( 0.000000000000000000, 0.4999999999999999445, -0.8660254037844387076 ) ) ;
#18352=VECTOR ( 'NONE', #21688, 1000.000000000000000 ) ;
#18404=CARTESIAN_POINT ( 'NONE',  ( 27.59999999999999787, 1.411358822780289120E-15, 0.000000000000000000 ) ) ;
#18460=CONICAL_SURFACE ( 'NONE', #39164, 5.000000000000001776, 0.9599310885968803664 ) ;
#18500=CARTESIAN_POINT ( 'NONE',  ( 37.06438722625302518, 3.851859888774471706E-31, 5.000000000000001776 ) ) ;
#18506=DIRECTION ( 'NONE',  ( -1.000000000000000000, -0.000000000000000000, -0.000000000000000000 ) ) ;
#18507=EDGE_CURVE ( 'NONE', #54910, #11758, #30039, .T. ) ;
#18523=CARTESIAN_POINT ( 'NONE',  ( 23.15769230769230802, 4.172000000000003261, 0.000000000000000000 ) ) ;
#18540=ORIENTED_EDGE ( 'NONE', *, *, #102819, .F. ) ;
#18545=ORIENTED_EDGE ( 'NONE', *, *, #48465, .T. ) ;
#18565=ORIENTED_EDGE ( 'NONE', *, *, #78028, .F. ) ;
#18573=ADVANCED_FACE ( 'NONE', ( #89843 ), #38695, .T. ) ;
#18577=VECTOR ( 'NONE', #50316, 1000.000000000000227 ) ;
#18594=ORIENTED_EDGE ( 'NONE', *, *, #26377, .F. ) ;
#18599=CARTESIAN_POINT ( 'NONE',  ( 10.73176661990081371, 5.000000000000004441, 6.123233995736770227E-16 ) ) ;
#18615=DIRECTION ( 'NONE',  ( 0.000000000000000000, -1.000000000000000000, 0.000000000000000000 ) ) ;
#18618=EDGE_LOOP ( 'NONE', ( #36290, #95872, #89039, #102636, #103462, #53697 ) ) ;
#18682=CARTESIAN_POINT ( 'NONE',  ( 32.04230769230768772, 1.411358822780289120E-15, 0.000000000000000000 ) ) ;
#18687=ORIENTED_EDGE ( 'NONE', *, *, #93217, .F. ) ;
#18697=DIRECTION ( 'NONE',  ( 0.000000000000000000, -1.000000000000000000, 0.000000000000000000 ) ) ;
#18711=DIRECTION ( 'NONE',  ( 0.000000000000000000, -1.000000000000000000, 0.000000000000000000 ) ) ;
#18740=CONICAL_SURFACE ( 'NONE', #89382, 8.000000000000000000, 1.047197551196600296 ) ;
#18745=CARTESIAN_POINT ( 'NONE',  ( 35.90484354297773706, 0.000000000000000000, 5.000000000000002665 ) ) ;
#18765=CONICAL_SURFACE ( 'NONE', #34470, 4.172000000000001485, 0.9599310885968750373 ) ;
#18783=CARTESIAN_POINT ( 'NONE',  ( 46.85000000000000142, 5.616230220889764410E-16, -4.171999999999999709 ) ) ;
#18795=AXIS2_PLACEMENT_3D ( 'NONE', #30987, #46603, #79501 ) ;
#18802=EDGE_CURVE ( 'NONE', #5164, #75282, #91895, .T. ) ;
#18814=CARTESIAN_POINT ( 'NONE',  ( 34.42407431220851066, 1.340359594676612611E-15, 0.000000000000000000 ) ) ;
#18862=EDGE_CURVE ( 'NONE', #87871, #101395, #69503, .T. ) ;
#18867=ORIENTED_EDGE ( 'NONE', *, *, #76842, .F. ) ;
#18893=CIRCLE ( 'NONE', #11919, 5.000000000000002665 ) ;
#18914=VECTOR ( 'NONE', #76653, 1000.000000000000000 ) ;
#18922=DIRECTION ( 'NONE',  ( -0.5735764363510510444, -0.8191520442889883569, 0.000000000000000000 ) ) ;
#18934=EDGE_CURVE ( 'NONE', #103450, #48691, #59191, .T. ) ;
#18944=CARTESIAN_POINT ( 'NONE',  ( 38.86638200451619696, 1.340359594676612611E-15, 0.000000000000000000 ) ) ;
#18951=ORIENTED_EDGE ( 'NONE', *, *, #1900, .T. ) ;
#18955=ORIENTED_EDGE ( 'NONE', *, *, #56125, .T. ) ;
#18971=DIRECTION ( 'NONE',  ( -1.000000000000000000, -1.224606353822377258E-16, -0.000000000000000000 ) ) ;
#18997=ORIENTED_EDGE ( 'NONE', *, *, #47328, .T. ) ;
#19012=VERTEX_POINT ( 'NONE', #87948 ) ;
#19052=ORIENTED_EDGE ( 'NONE', *, *, #47504, .T. ) ;
#19078=ADVANCED_FACE ( 'NONE', ( #61518 ), #3658, .T. ) ;
#19090=VECTOR ( 'NONE', #14055, 1000.000000000000000 ) ;
#19124=VERTEX_POINT ( 'NONE', #30207 ) ;
#19135=CARTESIAN_POINT ( 'NONE',  ( 0.7145311798163271888, -9.237604307034018802, 8.246630900752838649E-17 ) ) ;
#19146=ORIENTED_EDGE ( 'NONE', *, *, #9803, .T. ) ;
#19157=ORIENTED_EDGE ( 'NONE', *, *, #4122, .T. ) ;
#19245=LINE ( 'NONE', #76883, #56431 ) ;
#19259=ORIENTED_EDGE ( 'NONE', *, *, #103826, .T. ) ;
#19295=FACE_OUTER_BOUND ( 'NONE', #85775, .T. ) ;
#19297=ORIENTED_EDGE ( 'NONE', *, *, #103347, .F. ) ;
#19307=ORIENTED_EDGE ( 'NONE', *, *, #89799, .T. ) ;
#19308=CARTESIAN_POINT ( 'NONE',  ( 0.000000000000000000, 6.123233995736770227E-16, -5.000000000000002665 ) ) ;
#19310=CARTESIAN_POINT ( 'NONE',  ( 21.09715123528542691, -5.000000000000000000, 0.000000000000000000 ) ) ;
#19311=DIRECTION ( 'NONE',  ( 0.000000000000000000, 1.000000000000000000, 0.000000000000000000 ) ) ;
#19325=VERTEX_POINT ( 'NONE', #83505 ) ;
#19327=AXIS2_PLACEMENT_3D ( 'NONE', #60536, #27124, #34681 ) ;
#19354=ORIENTED_EDGE ( 'NONE', *, *, #45773, .F. ) ;
#19372=VERTEX_POINT ( 'NONE', #93741 ) ;
#19377=CARTESIAN_POINT ( 'NONE',  ( 14.27307692307692299, 1.411358822780289120E-15, 0.000000000000000000 ) ) ;
#19458=AXIS2_PLACEMENT_3D ( 'NONE', #93881, #34614, #76087 ) ;
#19505=EDGE_CURVE ( 'NONE', #26189, #63565, #46756, .T. ) ;
#19535=CARTESIAN_POINT ( 'NONE',  ( 10.73176661990081371, 6.123233995736770227E-16, -5.000000000000002665 ) ) ;
#19541=AXIS2_PLACEMENT_3D ( 'NONE', #48891, #73163, #8447 ) ;
#19567=LINE ( 'NONE', #29250, #5813 ) ;
#19568=ORIENTED_EDGE ( 'NONE', *, *, #5278, .F. ) ;
#19571=AXIS2_PLACEMENT_3D ( 'NONE', #56907, #89830, #23531 ) ;
#19579=DIRECTION ( 'NONE',  ( -1.000000000000000000, -1.224606353822377258E-16, -0.000000000000000000 ) ) ;
#19651=DIRECTION ( 'NONE',  ( 1.000000000000000000, 1.224606353822377258E-16, 0.000000000000000000 ) ) ;
#19675=ORIENTED_EDGE ( 'NONE', *, *, #28448, .T. ) ;
#19681=DIRECTION ( 'NONE',  ( 0.000000000000000000, 0.000000000000000000, 1.000000000000000000 ) ) ;
#19725=AXIS2_PLACEMENT_3D ( 'NONE', #106655, #105597, #88894 ) ;
#19747=ORIENTED_EDGE ( 'NONE', *, *, #95409, .F. ) ;
#19841=FACE_OUTER_BOUND ( 'NONE', #27244, .T. ) ;
#19911=AXIS2_PLACEMENT_3D ( 'NONE', #89482, #39350, #32324 ) ;
#19921=AXIS2_PLACEMENT_3D ( 'NONE', #65665, #40848, #73741 ) ;
#19943=DIRECTION ( 'NONE',  ( 0.5735764363510468256, 0.8191520442889913545, 0.000000000000000000 ) ) ;
#19957=ORIENTED_EDGE ( 'NONE', *, *, #101233, .F. ) ;
#19960=CARTESIAN_POINT ( 'NONE',  ( 19.61638200451619696, 1.340359594676612611E-15, 0.000000000000000000 ) ) ;
#19968=CARTESIAN_POINT ( 'NONE',  ( 0.000000000000000000, -6.928203230275509661, -3.999999999999999112 ) ) ;
#19971=CARTESIAN_POINT ( 'NONE',  ( 0.06809871960542722424, 7.710219529346608702, -2.645508037661881584 ) ) ;
#19990=VERTEX_POINT ( 'NONE', #103180 ) ;
#20051=LINE ( 'NONE', #52900, #87508 ) ;
#20053=CARTESIAN_POINT ( 'NONE',  ( 35.00384615384614762, 4.172000000000003261, 0.000000000000000000 ) ) ;
#20055=CARTESIAN_POINT ( 'NONE',  ( 41.50669491856072568, 1.482358050883964840E-15, 0.000000000000000000 ) ) ;
#20063=CARTESIAN_POINT ( 'NONE',  ( 43.30868969682389036, 1.340359594676612611E-15, 0.000000000000000000 ) ) ;
#20067=EDGE_LOOP ( 'NONE', ( #38961, #52517, #30654, #8458, #30001 ) ) ;
#20078=CIRCLE ( 'NONE', #87242, 5.000000000000001776 ) ;
#20081=DIRECTION ( 'NONE',  ( 0.000000000000000000, -1.000000000000000000, 0.000000000000000000 ) ) ;
#20128=VERTEX_POINT ( 'NONE', #20053 ) ;
#20137=AXIS2_PLACEMENT_3D ( 'NONE', #22632, #61480, #104030 ) ;
#20145=CIRCLE ( 'NONE', #83843, 5.000000000000001776 ) ;
#20172=DIRECTION ( 'NONE',  ( 0.000000000000000000, 1.000000000000000000, 0.000000000000000000 ) ) ;
#20180=VECTOR ( 'NONE', #7499, 1000.000000000000000 ) ;
#20200=DIRECTION ( 'NONE',  ( -1.000000000000000000, -1.224606353822377258E-16, -0.000000000000000000 ) ) ;
#20229=DIRECTION ( 'NONE',  ( 0.000000000000000000, 0.000000000000000000, -1.000000000000000000 ) ) ;
#20237=EDGE_LOOP ( 'NONE', ( #77700, #54186, #32076 ) ) ;
#20245=CARTESIAN_POINT ( 'NONE',  ( 24.63846153846153797, 1.411358822780289120E-15, 0.000000000000000000 ) ) ;
#20268=CARTESIAN_POINT ( 'NONE',  ( 6.249999999999998224, 0.000000000000000000, 0.000000000000000000 ) ) ;
#20278=DIRECTION ( 'NONE',  ( 0.000000000000000000, -1.000000000000000000, 0.000000000000000000 ) ) ;
#20283=EDGE_CURVE ( 'NONE', #8439, #88628, #104493, .T. ) ;
#20284=ORIENTED_EDGE ( 'NONE', *, *, #38678, .T. ) ;
#20301=CARTESIAN_POINT ( 'NONE',  ( 41.50669491856072568, 1.482358050883964840E-15, 0.000000000000000000 ) ) ;
#20304=CIRCLE ( 'NONE', #96009, 4.172000000000001485 ) ;
#20324=CARTESIAN_POINT ( 'NONE',  ( 6.249999999999998224, -9.237604307034018802, 3.355146209984123968E-17 ) ) ;
#20325=ORIENTED_EDGE ( 'NONE', *, *, #83854, .T. ) ;
#20367=DIRECTION ( 'NONE',  ( -1.000000000000000000, -0.000000000000000000, -0.000000000000000000 ) ) ;
#20386=LINE ( 'NONE', #78030, #70945 ) ;
#20394=CARTESIAN_POINT ( 'NONE',  ( 27.59999999999999787, 4.172000000000003261, 5.109226446042759579E-16 ) ) ;
#20414=CARTESIAN_POINT ( 'NONE',  ( 0.000000000000000000, 0.000000000000000000, 0.000000000000000000 ) ) ;
#20418=EDGE_CURVE ( 'NONE', #96607, #17199, #98565, .T. ) ;
#20419=ORIENTED_EDGE ( 'NONE', *, *, #86848, .T. ) ;
#20424=CARTESIAN_POINT ( 'NONE',  ( 13.69330508143927538, 5.000000000000004441, 6.123233995736770227E-16 ) ) ;
#20433=CARTESIAN_POINT ( 'NONE',  ( 35.00384615384614762, -4.171999999999999709, 5.616230220889763424E-16 ) ) ;
#20441=ORIENTED_EDGE ( 'NONE', *, *, #68612, .T. ) ;
#20442=DIRECTION ( 'NONE',  ( -1.000000000000000000, -1.224606353822377258E-16, -0.000000000000000000 ) ) ;
#20535=DIRECTION ( 'NONE',  ( 1.000000000000000000, 1.224606353822377258E-16, 0.000000000000000000 ) ) ;
#20550=CIRCLE ( 'NONE', #3317, 5.000000000000002665 ) ;
#20558=AXIS2_PLACEMENT_3D ( 'NONE', #81079, #7189, #105372 ) ;
#20562=CARTESIAN_POINT ( 'NONE',  ( 25.21823338009918203, 1.482358050883964840E-15, 0.000000000000000000 ) ) ;
#20573=DIRECTION ( 'NONE',  ( 0.000000000000000000, -1.000000000000000000, 0.000000000000000000 ) ) ;
#20644=ORIENTED_EDGE ( 'NONE', *, *, #39021, .T. ) ;
#20653=AXIS2_PLACEMENT_3D ( 'NONE', #12870, #88382, #94889 ) ;
#20676=CARTESIAN_POINT ( 'NONE',  ( 44.78945892759311675, 1.340359594676612611E-15, 0.000000000000000000 ) ) ;
#20688=ORIENTED_EDGE ( 'NONE', *, *, #42908, .T. ) ;
#20765=DIRECTION ( 'NONE',  ( -1.000000000000000000, -0.000000000000000000, -0.000000000000000000 ) ) ;
#20768=EDGE_CURVE ( 'NONE', #60654, #44784, #89953, .T. ) ;
#20779=AXIS2_PLACEMENT_3D ( 'NONE', #20268, #9989, #42891 ) ;
#20806=FACE_OUTER_BOUND ( 'NONE', #67906, .T. ) ;
#20811=CARTESIAN_POINT ( 'NONE',  ( 6.249999999999998224, 9.237604307034018802, 0.000000000000000000 ) ) ;
#20820=EDGE_CURVE ( 'NONE', #85235, #106160, #67257, .T. ) ;
#20829=EDGE_CURVE ( 'NONE', #77688, #16424, #3958, .T. ) ;
#20851=CARTESIAN_POINT ( 'NONE',  ( 0.000000000000000000, -6.928203230275509661, -3.999999999999999112 ) ) ;
#20871=VERTEX_POINT ( 'NONE', #96177 ) ;
#20878=DIRECTION ( 'NONE',  ( 0.000000000000000000, -1.000000000000000000, 0.000000000000000000 ) ) ;
#20880=ORIENTED_EDGE ( 'NONE', *, *, #28939, .T. ) ;
#20883=EDGE_LOOP ( 'NONE', ( #42773, #102989, #31084, #47960, #76600 ) ) ;
#20926=CONICAL_SURFACE ( 'NONE', #22597, 4.172000000000001485, 0.9599310885968750373 ) ;
#20965=EDGE_CURVE ( 'NONE', #29545, #14796, #31542, .T. ) ;
#20970=DIRECTION ( 'NONE',  ( -1.000000000000000000, -1.224606353822377258E-16, -0.000000000000000000 ) ) ;
#21001=FACE_OUTER_BOUND ( 'NONE', #31405, .T. ) ;
#21028=CIRCLE ( 'NONE', #226, 5.000000000000002665 ) ;
#21081=DIRECTION ( 'NONE',  ( 0.5735764363510468256, 0.8191520442889913545, 0.000000000000000000 ) ) ;
#21199=CARTESIAN_POINT ( 'NONE',  ( 25.53945892759312031, 1.340359594676612611E-15, 0.000000000000000000 ) ) ;
#21258=CARTESIAN_POINT ( 'NONE',  ( 32.62207953394533178, 3.851859888774471706E-31, 5.000000000000001776 ) ) ;
#21266=CARTESIAN_POINT ( 'NONE',  ( 7.770228158362351145, 1.340359594676612611E-15, 0.000000000000000000 ) ) ;
#21298=EDGE_LOOP ( 'NONE', ( #74131, #39104, #80104, #56121, #77221, #56805 ) ) ;
#21306=ORIENTED_EDGE ( 'NONE', *, *, #74149, .T. ) ;
#21320=ORIENTED_EDGE ( 'NONE', *, *, #59750, .T. ) ;
#21331=CIRCLE ( 'NONE', #35105, 5.000000000000001776 ) ;
#21371=DIRECTION ( 'NONE',  ( -1.000000000000000000, -1.224606353822377258E-16, -0.000000000000000000 ) ) ;
#21381=LINE ( 'NONE', #94730, #43274 ) ;
#21396=CARTESIAN_POINT ( 'NONE',  ( 0.000000000000000000, 0.000000000000000000, 5.000000000000002665 ) ) ;
#21402=EDGE_CURVE ( 'NONE', #55161, #79135, #17818, .T. ) ;
#21405=CIRCLE ( 'NONE', #79940, 5.000000000000002665 ) ;
#21456=CARTESIAN_POINT ( 'NONE',  ( 0.000000000000000000, 0.000000000000000000, 0.000000000000000000 ) ) ;
#21475=LINE ( 'NONE', #54310, #103076 ) ;
#21486=EDGE_CURVE ( 'NONE', #50381, #32861, #55654, .T. ) ;
#21507=CARTESIAN_POINT ( 'NONE',  ( 42.40769230769231513, 1.411358822780289120E-15, 0.000000000000000000 ) ) ;
#21509=CARTESIAN_POINT ( 'NONE',  ( 29.66054107240687543, 1.482358050883964840E-15, 0.000000000000000000 ) ) ;
#21531=DIRECTION ( 'NONE',  ( 1.000000000000000000, 0.000000000000000000, -0.000000000000000000 ) ) ;
#21550=EDGE_CURVE ( 'NONE', #63024, #104720, #89970, .T. ) ;
#21622=EDGE_CURVE ( 'NONE', #102923, #16386, #55944, .T. ) ;
#21641=DIRECTION ( 'NONE',  ( 0.000000000000000000, -1.000000000000000000, 0.000000000000000000 ) ) ;
#21669=CIRCLE ( 'NONE', #102632, 5.000000000000002665 ) ;
#21688=DIRECTION ( 'NONE',  ( -1.000000000000000000, -0.000000000000000000, -0.000000000000000000 ) ) ;
#21698=DIRECTION ( 'NONE',  ( 0.5735764363510470476, -0.8191520442889911324, 1.003171929053524007E-16 ) ) ;
#21704=DIRECTION ( 'NONE',  ( -1.000000000000000000, -0.000000000000000000, -0.000000000000000000 ) ) ;
#21706=CARTESIAN_POINT ( 'NONE',  ( 34.42407431220851066, 6.123233995736770227E-16, -5.000000000000002665 ) ) ;
#21716=CIRCLE ( 'NONE', #47539, 5.000000000000002665 ) ;
#21746=ORIENTED_EDGE ( 'NONE', *, *, #63394, .T. ) ;
#21776=AXIS2_PLACEMENT_3D ( 'NONE', #94694, #69869, #12145 ) ;
#21793=CARTESIAN_POINT ( 'NONE',  ( 20.77592568779148863, 1.482358050883964840E-15, 0.000000000000000000 ) ) ;
#21795=ADVANCED_FACE ( 'NONE', ( #14710 ), #79460, .T. ) ;
#21799=ORIENTED_EDGE ( 'NONE', *, *, #59004, .T. ) ;
#21811=ORIENTED_EDGE ( 'NONE', *, *, #49203, .T. ) ;
#21836=VECTOR ( 'NONE', #2235, 1000.000000000000000 ) ;
#21850=VERTEX_POINT ( 'NONE', #46566 ) ;
#21853=CARTESIAN_POINT ( 'NONE',  ( 10.73176661990081371, 1.340359594676612611E-15, 0.000000000000000000 ) ) ;
#21864=DIRECTION ( 'NONE',  ( 0.000000000000000000, -1.000000000000000000, 0.000000000000000000 ) ) ;
#21865=EDGE_CURVE ( 'NONE', #72256, #48691, #88098, .T. ) ;
#21869=CARTESIAN_POINT ( 'NONE',  ( 25.21823338009918203, -5.000000000000000000, 6.123233995736768255E-16 ) ) ;
#21888=CARTESIAN_POINT ( 'NONE',  ( 0.000000000000000000, 9.237604307034018802, 1.301042606982603546E-15 ) ) ;
#21927=FACE_OUTER_BOUND ( 'NONE', #94716, .T. ) ;
#21950=ORIENTED_EDGE ( 'NONE', *, *, #64272, .T. ) ;
#22011=ORIENTED_EDGE ( 'NONE', *, *, #30734, .T. ) ;
#22015=ORIENTED_EDGE ( 'NONE', *, *, #69638, .F. ) ;
#22023=CARTESIAN_POINT ( 'NONE',  ( 0.7145311798163216377, 4.618802153517004960, 7.999999999999998224 ) ) ;
#22052=ORIENTED_EDGE ( 'NONE', *, *, #59439, .F. ) ;
#22054=CARTESIAN_POINT ( 'NONE',  ( 0.000000000000000000, 0.000000000000000000, 5.000000000000002665 ) ) ;
#22076=FACE_OUTER_BOUND ( 'NONE', #18618, .T. ) ;
#22093=LINE ( 'NONE', #31259, #5347 ) ;
#22132=VECTOR ( 'NONE', #97926, 999.9999999999998863 ) ;
#22161=EDGE_CURVE ( 'NONE', #28378, #12793, #52099, .T. ) ;
#22206=ADVANCED_FACE ( 'NONE', ( #68300 ), #57713, .T. ) ;
#22208=VECTOR ( 'NONE', #65161, 1000.000000000000227 ) ;
#22211=CARTESIAN_POINT ( 'NONE',  ( 0.000000000000000000, 6.928203230275506108, 4.000000000000007105 ) ) ;
#22255=DIRECTION ( 'NONE',  ( -1.000000000000000000, -1.224606353822377258E-16, -0.000000000000000000 ) ) ;
#22265=AXIS2_PLACEMENT_3D ( 'NONE', #100859, #28083, #93314 ) ;
#22279=CARTESIAN_POINT ( 'NONE',  ( 40.34715123528543046, 1.340359594676612611E-15, 0.000000000000000000 ) ) ;
#22342=ADVANCED_FACE ( 'NONE', ( #77979 ), #29984, .T. ) ;
#22392=DIRECTION ( 'NONE',  ( 0.5735764363510468256, 0.8191520442889913545, 0.000000000000000000 ) ) ;
#22394=DIRECTION ( 'NONE',  ( -1.000000000000000000, -1.224606353822377258E-16, -0.000000000000000000 ) ) ;
#22420=VERTEX_POINT ( 'NONE', #31060 ) ;
#22430=VERTEX_POINT ( 'NONE', #80613 ) ;
#22442=CARTESIAN_POINT ( 'NONE',  ( 21.67692307692307452, -4.171999999999999709, 5.616230220889763424E-16 ) ) ;
#22444=CARTESIAN_POINT ( 'NONE',  ( 10.41054107240687188, 5.000000000000002665, 0.000000000000000000 ) ) ;
#22466=VECTOR ( 'NONE', #75326, 1000.000000000000000 ) ;
#22474=AXIS2_PLACEMENT_3D ( 'NONE', #36693, #102446, #28591 ) ;
#22490=ORIENTED_EDGE ( 'NONE', *, *, #87474, .T. ) ;
#22491=DIRECTION ( 'NONE',  ( 0.000000000000000000, 1.000000000000000000, 0.000000000000000000 ) ) ;
#22519=ADVANCED_FACE ( 'NONE', ( #75719 ), #2677, .T. ) ;
#22597=AXIS2_PLACEMENT_3D ( 'NONE', #9111, #8051, #49036 ) ;
#22600=PLANE ( 'NONE',  #4487 ) ;
#22627=LINE ( 'NONE', #46854, #61867 ) ;
#22632=CARTESIAN_POINT ( 'NONE',  ( 42.98746414932995208, 1.482358050883964840E-15, 0.000000000000000000 ) ) ;
#22655=CARTESIAN_POINT ( 'NONE',  ( 32.94330508143927716, -4.999999999999990230, 0.000000000000000000 ) ) ;
#22682=CIRCLE ( 'NONE', #82933, 5.000000000000002665 ) ;
#22689=LINE ( 'NONE', #88464, #80205 ) ;
#22698=AXIS2_PLACEMENT_3D ( 'NONE', #61332, #45669, #69420 ) ;
#22755=DIRECTION ( 'NONE',  ( 0.000000000000000000, 0.000000000000000000, 1.000000000000000000 ) ) ;
#22758=DIRECTION ( 'NONE',  ( -1.000000000000000000, -1.224606353822377258E-16, -0.000000000000000000 ) ) ;
#22813=ADVANCED_FACE ( 'NONE', ( #12568 ), #23355, .T. ) ;
#22820=DIRECTION ( 'NONE',  ( -1.000000000000000000, -1.224606353822377258E-16, -0.000000000000000000 ) ) ;
#22836=CARTESIAN_POINT ( 'NONE',  ( 0.4964154566687929981, -8.859816792613649739, 0.6543471694412414941 ) ) ;
#22842=DIRECTION ( 'NONE',  ( 0.000000000000000000, -1.000000000000000000, 0.000000000000000000 ) ) ;
#22844=ORIENTED_EDGE ( 'NONE', *, *, #78575, .T. ) ;
#22846=ORIENTED_EDGE ( 'NONE', *, *, #90793, .F. ) ;
#22852=DIRECTION ( 'NONE',  ( -1.000000000000000000, -0.000000000000000000, -0.000000000000000000 ) ) ;
#22855=ORIENTED_EDGE ( 'NONE', *, *, #35936, .F. ) ;
#22873=EDGE_CURVE ( 'NONE', #30622, #3257, #14685, .T. ) ;
#22892=ORIENTED_EDGE ( 'NONE', *, *, #80971, .T. ) ;
#22896=CARTESIAN_POINT ( 'NONE',  ( 27.59999999999999787, 4.172000000000003261, 0.000000000000000000 ) ) ;
#22898=CARTESIAN_POINT ( 'NONE',  ( 0.7145311798163198613, -4.618802153516998743, 7.999999999999998224 ) ) ;
#22956=DIRECTION ( 'NONE',  ( -1.000000000000000000, -1.224606353822377258E-16, -0.000000000000000000 ) ) ;
#22980=CARTESIAN_POINT ( 'NONE',  ( 20.19615384615384457, 1.411358822780289120E-15, 0.000000000000000000 ) ) ;
#23070=EDGE_LOOP ( 'NONE', ( #69990, #47125, #81763, #100163, #24493 ) ) ;
#23088=ORIENTED_EDGE ( 'NONE', *, *, #47504, .F. ) ;
#23089=STYLED_ITEM ( 'NONE', ( #83582 ), #4890 ) ;
#23100=FACE_OUTER_BOUND ( 'NONE', #3113, .T. ) ;
#23116=VERTEX_POINT ( 'NONE', #57801 ) ;
#23117=CARTESIAN_POINT ( 'NONE',  ( 6.849999999999999645, 9.237604307034018802, 1.301042606982603546E-15 ) ) ;
#23140=LINE ( 'NONE', #63595, #22208 ) ;
#23148=DIRECTION ( 'NONE',  ( 1.000000000000000000, 1.224606353822377258E-16, 0.000000000000000000 ) ) ;
#23157=DIRECTION ( 'NONE',  ( 0.5735764363510468256, 0.8191520442889913545, 0.000000000000000000 ) ) ;
#23161=CONICAL_SURFACE ( 'NONE', #79946, 5.000000000000001776, 0.9599310885968803664 ) ;
#23171=ORIENTED_EDGE ( 'NONE', *, *, #71011, .F. ) ;
#23173=ORIENTED_EDGE ( 'NONE', *, *, #44167, .T. ) ;
#23194=ORIENTED_EDGE ( 'NONE', *, *, #4528, .T. ) ;
#23237=DIRECTION ( 'NONE',  ( 0.000000000000000000, 0.000000000000000000, -1.000000000000000000 ) ) ;
#23254=CARTESIAN_POINT ( 'NONE',  ( 25.53945892759312031, 1.340359594676612611E-15, 0.000000000000000000 ) ) ;
#23273=AXIS2_PLACEMENT_3D ( 'NONE', #26370, #82431, #931 ) ;
#23284=DIRECTION ( 'NONE',  ( 0.000000000000000000, -1.000000000000000000, 0.000000000000000000 ) ) ;
#23294=DIRECTION ( 'NONE',  ( 0.5735764363510468256, 0.8191520442889913545, 0.000000000000000000 ) ) ;
#23324=EDGE_LOOP ( 'NONE', ( #105054, #82435, #86783, #97196, #90671 ) ) ;
#23335=EDGE_CURVE ( 'NONE', #43284, #43900, #88847, .T. ) ;
#23349=CONICAL_SURFACE ( 'NONE', #88771, 4.172000000000001485, 0.9599310885968750373 ) ;
#23355=CONICAL_SURFACE ( 'NONE', #73262, 5.000000000000001776, 0.9599310885968803664 ) ;
#23379=ORIENTED_EDGE ( 'NONE', *, *, #79742, .F. ) ;
#23387=DIRECTION ( 'NONE',  ( 0.000000000000000000, 0.000000000000000000, -1.000000000000000000 ) ) ;
#23416=EDGE_CURVE ( 'NONE', #7097, #2627, #80207, .T. ) ;
#23422=ADVANCED_FACE ( 'NONE', ( #72795 ), #44118, .T. ) ;
#23428=EDGE_CURVE ( 'NONE', #28900, #47541, #94003, .T. ) ;
#23503=VECTOR ( 'NONE', #49623, 999.9999999999998863 ) ;
#23507=DIRECTION ( 'NONE',  ( 0.000000000000000000, 0.000000000000000000, 1.000000000000000000 ) ) ;
#23531=DIRECTION ( 'NONE',  ( 0.000000000000000000, -1.000000000000000000, 0.000000000000000000 ) ) ;
#23561=FACE_OUTER_BOUND ( 'NONE', #63998, .T. ) ;
#23570=CIRCLE ( 'NONE', #28747, 5.000000000000001776 ) ;
#23598=DIRECTION ( 'NONE',  ( -0.5735764363510510444, -0.8191520442889883569, 0.000000000000000000 ) ) ;
#23625=ORIENTED_EDGE ( 'NONE', *, *, #10486, .F. ) ;
#23627=CARTESIAN_POINT ( 'NONE',  ( 45.94900261086841198, -5.000000000000000000, 6.123233995736768255E-16 ) ) ;
#23635=DIRECTION ( 'NONE',  ( -1.000000000000000000, -1.224606353822377258E-16, -0.000000000000000000 ) ) ;
#23643=VERTEX_POINT ( 'NONE', #87693 ) ;
#23651=AXIS2_PLACEMENT_3D ( 'NONE', #106158, #50063, #16640 ) ;
#23659=ORIENTED_EDGE ( 'NONE', *, *, #96773, .T. ) ;
#23674=DIRECTION ( 'NONE',  ( 0.000000000000000000, -1.000000000000000000, 0.000000000000000000 ) ) ;
#23676=ADVANCED_FACE ( 'NONE', ( #79058 ), #86118, .F. ) ;
#23694=ORIENTED_EDGE ( 'NONE', *, *, #11330, .T. ) ;
#23726=EDGE_CURVE ( 'NONE', #39589, #60803, #39042, .T. ) ;
#23738=LINE ( 'NONE', #73844, #20180 ) ;
#23740=LINE ( 'NONE', #58196, #101830 ) ;
#23746=AXIS2_PLACEMENT_3D ( 'NONE', #50489, #85008, #83402 ) ;
#23773=FACE_OUTER_BOUND ( 'NONE', #17023, .T. ) ;
#23780=VERTEX_POINT ( 'NONE', #14835 ) ;
#23788=AXIS2_PLACEMENT_3D ( 'NONE', #83948, #66167, #34907 ) ;
#23846=VERTEX_POINT ( 'NONE', #68181 ) ;
#23847=DIRECTION ( 'NONE',  ( -1.000000000000000000, -0.000000000000000000, -0.000000000000000000 ) ) ;
#23850=CIRCLE ( 'NONE', #80698, 8.000000000000000000 ) ;
#23866=CARTESIAN_POINT ( 'NONE',  ( 9.250997389131581983, -5.000000000000000000, 0.000000000000000000 ) ) ;
#23890=AXIS2_PLACEMENT_3D ( 'NONE', #84642, #33998, #66867 ) ;
#23898=CIRCLE ( 'NONE', #56554, 5.000000000000002665 ) ;
#23899=CARTESIAN_POINT ( 'NONE',  ( 40.02592568779148507, 1.482358050883964840E-15, 0.000000000000000000 ) ) ;
#23961=CARTESIAN_POINT ( 'NONE',  ( 9.830769230769229594, 1.411358822780289120E-15, 0.000000000000000000 ) ) ;
#23980=ORIENTED_EDGE ( 'NONE', *, *, #8754, .F. ) ;
#23988=ORIENTED_EDGE ( 'NONE', *, *, #93691, .F. ) ;
#24001=CYLINDRICAL_SURFACE ( 'NONE', #11296, 5.000000000000002665 ) ;
#24013=ORIENTED_EDGE ( 'NONE', *, *, #97354, .F. ) ;
#24050=ORIENTED_EDGE ( 'NONE', *, *, #1900, .F. ) ;
#24051=DIRECTION ( 'NONE',  ( -1.000000000000000000, -0.000000000000000000, -0.000000000000000000 ) ) ;
#24095=ORIENTED_EDGE ( 'NONE', *, *, #50399, .F. ) ;
#24112=EDGE_CURVE ( 'NONE', #67995, #29093, #17395, .T. ) ;
#24119=CARTESIAN_POINT ( 'NONE',  ( 0.000000000000000000, 0.000000000000000000, 0.000000000000000000 ) ) ;
#24174=EDGE_LOOP ( 'NONE', ( #102724, #74943, #89158, #67615, #2451 ) ) ;
#24208=DIRECTION ( 'NONE',  ( -1.000000000000000000, -0.000000000000000000, -0.000000000000000000 ) ) ;
#24226=CARTESIAN_POINT ( 'NONE',  ( 7.770228158362351145, 6.123233995736769241E-16, -5.000000000000002665 ) ) ;
#24238=DIRECTION ( 'NONE',  ( 1.000000000000000000, 1.224606353822377258E-16, 0.000000000000000000 ) ) ;
#24240=CARTESIAN_POINT ( 'NONE',  ( 8.929771841637641927, 1.482358050883964840E-15, 0.000000000000000000 ) ) ;
#24250=VERTEX_POINT ( 'NONE', #101491 ) ;
#24259=DIRECTION ( 'NONE',  ( -0.000000000000000000, 0.8660254037844387076, 0.4999999999999999445 ) ) ;
#24284=ORIENTED_EDGE ( 'NONE', *, *, #58934, .F. ) ;
#24310=CARTESIAN_POINT ( 'NONE',  ( 6.849999999999999645, 0.000000000000000000, 0.000000000000000000 ) ) ;
#24330=FACE_OUTER_BOUND ( 'NONE', #96446, .T. ) ;
#24343=AXIS2_PLACEMENT_3D ( 'NONE', #55421, #88354, #14430 ) ;
#24382=CARTESIAN_POINT ( 'NONE',  ( 11.89131030317610183, -5.000000000000000000, 6.123233995736768255E-16 ) ) ;
#24393=ORIENTED_EDGE ( 'NONE', *, *, #58112, .F. ) ;
#24404=CARTESIAN_POINT ( 'NONE',  ( 8.349999999999999645, 4.172000000000003261, 0.000000000000000000 ) ) ;
#24454=DIRECTION ( 'NONE',  ( -1.000000000000000000, -1.224606353822377258E-16, -0.000000000000000000 ) ) ;
#24478=VECTOR ( 'NONE', #98960, 1000.000000000000000 ) ;
#24480=ORIENTED_EDGE ( 'NONE', *, *, #9803, .F. ) ;
#24489=CARTESIAN_POINT ( 'NONE',  ( 34.42407431220851066, 4.999999999999994671, 6.123233995736758394E-16 ) ) ;
#24492=CIRCLE ( 'NONE', #105376, 5.000000000000002665 ) ;
#24493=ORIENTED_EDGE ( 'NONE', *, *, #55132, .F. ) ;
#24563=AXIS2_PLACEMENT_3D ( 'NONE', #99161, #51141, #58180 ) ;
#24565=ORIENTED_EDGE ( 'NONE', *, *, #94745, .T. ) ;
#24578=DIRECTION ( 'NONE',  ( 0.000000000000000000, -1.000000000000000000, 0.000000000000000000 ) ) ;
#24591=DIRECTION ( 'NONE',  ( -1.000000000000000000, -1.224606353822377258E-16, -0.000000000000000000 ) ) ;
#24625=EDGE_CURVE ( 'NONE', #33590, #106160, #1266, .T. ) ;
#24645=ORIENTED_EDGE ( 'NONE', *, *, #17107, .F. ) ;
#24663=LINE ( 'NONE', #57516, #98761 ) ;
#24668=AXIS2_PLACEMENT_3D ( 'NONE', #77574, #36620, #87264 ) ;
#24669=DIRECTION ( 'NONE',  ( 0.000000000000000000, -1.000000000000000000, 0.000000000000000000 ) ) ;
#24678=DIRECTION ( 'NONE',  ( 0.000000000000000000, -1.000000000000000000, 0.000000000000000000 ) ) ;
#24683=DIRECTION ( 'NONE',  ( -1.000000000000000000, -1.224606353822377258E-16, -0.000000000000000000 ) ) ;
#24684=VERTEX_POINT ( 'NONE', #74027 ) ;
#24694=VERTEX_POINT ( 'NONE', #59466 ) ;
#24721=CARTESIAN_POINT ( 'NONE',  ( 38.54515645702225868, 6.123233995736772199E-16, -5.000000000000001776 ) ) ;
#24744=ORIENTED_EDGE ( 'NONE', *, *, #59478, .F. ) ;
#24750=DIRECTION ( 'NONE',  ( 0.000000000000000000, -1.000000000000000000, 0.000000000000000000 ) ) ;
#24756=CARTESIAN_POINT ( 'NONE',  ( 6.249999999999998224, 4.618802153517001408, -8.000000000000000000 ) ) ;
#24803=DIRECTION ( 'NONE',  ( -1.000000000000000000, -1.224606353822377258E-16, -0.000000000000000000 ) ) ;
#24824=CARTESIAN_POINT ( 'NONE',  ( 0.000000000000000000, 0.000000000000000000, 0.000000000000000000 ) ) ;
#24845=CARTESIAN_POINT ( 'NONE',  ( 0.000000000000000000, 6.123233995736770227E-16, -5.000000000000002665 ) ) ;
#24848=CARTESIAN_POINT ( 'NONE',  ( 22.57792046605466041, 1.340359594676612611E-15, 0.000000000000000000 ) ) ;
#24851=CARTESIAN_POINT ( 'NONE',  ( 6.849999999999999645, 0.000000000000000000, 8.000000000000000000 ) ) ;
#24868=EDGE_CURVE ( 'NONE', #94292, #24694, #44878, .T. ) ;
#24872=ORIENTED_EDGE ( 'NONE', *, *, #63117, .T. ) ;
#24873=CARTESIAN_POINT ( 'NONE',  ( 0.000000000000000000, 6.123233995736770227E-16, -5.000000000000002665 ) ) ;
#24882=AXIS2_PLACEMENT_3D ( 'NONE', #4351, #62085, #79293 ) ;
#24897=ORIENTED_EDGE ( 'NONE', *, *, #86985, .F. ) ;
#25025=EDGE_CURVE ( 'NONE', #53057, #49120, #90628, .T. ) ;
#25032=VERTEX_POINT ( 'NONE', #9850 ) ;
#25034=DIRECTION ( 'NONE',  ( 1.000000000000000000, 1.224606353822377258E-16, 0.000000000000000000 ) ) ;
#25051=VECTOR ( 'NONE', #42541, 999.9999999999998863 ) ;
#25097=EDGE_CURVE ( 'NONE', #84262, #73855, #83738, .T. ) ;
#25172=DIRECTION ( 'NONE',  ( -1.000000000000000000, -1.224606353822377258E-16, -0.000000000000000000 ) ) ;
#25179=CIRCLE ( 'NONE', #6199, 5.000000000000001776 ) ;
#25186=CIRCLE ( 'NONE', #2746, 5.000000000000001776 ) ;
#25224=CARTESIAN_POINT ( 'NONE',  ( 0.1317522424410015880, 1.959574484677831130, -8.000000000000001776 ) ) ;
#25225=DIRECTION ( 'NONE',  ( 0.5735764363510470476, -0.8191520442889911324, 1.003171929053524007E-16 ) ) ;
#25226=DIRECTION ( 'NONE',  ( -1.000000000000000000, -1.224606353822377258E-16, -0.000000000000000000 ) ) ;
#25244=CARTESIAN_POINT ( 'NONE',  ( 0.000000000000000000, 0.000000000000000000, 0.000000000000000000 ) ) ;
#25249=CARTESIAN_POINT ( 'NONE',  ( 18.13561277374696701, 6.123233995736770227E-16, -5.000000000000002665 ) ) ;
#25262=DIRECTION ( 'NONE',  ( 0.000000000000000000, -1.000000000000000000, 0.000000000000000000 ) ) ;
#25285=VECTOR ( 'NONE', #29416, 999.9999999999998863 ) ;
#25306=ORIENTED_EDGE ( 'NONE', *, *, #75200, .T. ) ;
#25331=AXIS2_PLACEMENT_3D ( 'NONE', #94620, #20765, #70326 ) ;
#25343=EDGE_LOOP ( 'NONE', ( #13007, #43080, #87794, #2256, #3148 ) ) ;
#25349=ORIENTED_EDGE ( 'NONE', *, *, #60644, .T. ) ;
#25351=ORIENTED_EDGE ( 'NONE', *, *, #106243, .F. ) ;
#25357=CONICAL_SURFACE ( 'NONE', #85628, 5.000000000000001776, 0.9599310885968803664 ) ;
#25382=CARTESIAN_POINT ( 'NONE',  ( 34.42407431220851066, 1.340359594676612611E-15, 0.000000000000000000 ) ) ;
#25400=CARTESIAN_POINT ( 'NONE',  ( 26.69900261086841198, 1.482358050883964840E-15, 0.000000000000000000 ) ) ;
#25402=AXIS2_PLACEMENT_3D ( 'NONE', #103053, #94439, #52355 ) ;
#25469=VERTEX_POINT ( 'NONE', #64787 ) ;
#25480=CARTESIAN_POINT ( 'NONE',  ( 12.79230769230769305, 4.172000000000003261, 5.109226446042759579E-16 ) ) ;
#25491=DIRECTION ( 'NONE',  ( -1.000000000000000000, -0.000000000000000000, -0.000000000000000000 ) ) ;
#25507=VERTEX_POINT ( 'NONE', #49111 ) ;
#25515=CARTESIAN_POINT ( 'NONE',  ( 10.41054107240687188, 1.482358050883964840E-15, 0.000000000000000000 ) ) ;
#25561=EDGE_CURVE ( 'NONE', #33830, #39671, #60446, .T. ) ;
#25564=DIRECTION ( 'NONE',  ( 0.000000000000000000, -1.000000000000000000, 0.000000000000000000 ) ) ;
#25570=CONICAL_SURFACE ( 'NONE', #99580, 4.172000000000001485, 0.9599310885968750373 ) ;
#25584=CIRCLE ( 'NONE', #85864, 5.000000000000002665 ) ;
#25596=AXIS2_PLACEMENT_3D ( 'NONE', #57830, #90218, #49753 ) ;
#25642=DIRECTION ( 'NONE',  ( -1.000000000000000000, -1.224606353822377258E-16, -0.000000000000000000 ) ) ;
#25653=DIRECTION ( 'NONE',  ( -1.000000000000000000, -1.224606353822377258E-16, -0.000000000000000000 ) ) ;
#25696=CONICAL_SURFACE ( 'NONE', #94588, 8.000000000000000000, 1.047197551196600296 ) ;
#25726=ORIENTED_EDGE ( 'NONE', *, *, #102568, .T. ) ;
#25763=DIRECTION ( 'NONE',  ( 0.000000000000000000, -1.000000000000000000, 0.000000000000000000 ) ) ;
#25785=VERTEX_POINT ( 'NONE', #96511 ) ;
#25794=EDGE_CURVE ( 'NONE', #86992, #82401, #5878, .T. ) ;
#25808=DIRECTION ( 'NONE',  ( 0.5735764363510468256, 0.8191520442889913545, 0.000000000000000000 ) ) ;
#25816=DIRECTION ( 'NONE',  ( 0.000000000000000000, -1.000000000000000000, 0.000000000000000000 ) ) ;
#25826=DIRECTION ( 'NONE',  ( 0.000000000000000000, 0.000000000000000000, -1.000000000000000000 ) ) ;
#25860=ADVANCED_FACE ( 'NONE', ( #88939 ), #96001, .T. ) ;
#25866=DIRECTION ( 'NONE',  ( 0.000000000000000000, 0.000000000000000000, 1.000000000000000000 ) ) ;
#25886=AXIS2_PLACEMENT_3D ( 'NONE', #101685, #11591, #86057 ) ;
#25892=CARTESIAN_POINT ( 'NONE',  ( 27.59999999999999787, 1.411358822780289120E-15, 0.000000000000000000 ) ) ;
#25918=DIRECTION ( 'NONE',  ( -1.000000000000000000, -1.224606353822377258E-16, -0.000000000000000000 ) ) ;
#25956=CARTESIAN_POINT ( 'NONE',  ( 23.73746414932995208, 5.000000000000002665, 0.000000000000000000 ) ) ;
#25964=CARTESIAN_POINT ( 'NONE',  ( 26.11923076923076792, 1.411358822780289120E-15, 0.000000000000000000 ) ) ;
#25982=ADVANCED_FACE ( 'NONE', ( #17189 ), #89995, .T. ) ;
#25988=CARTESIAN_POINT ( 'NONE',  ( 0.000000000000000000, 0.000000000000000000, 5.000000000000002665 ) ) ;
#26038=ORIENTED_EDGE ( 'NONE', *, *, #39443, .T. ) ;
#26062=DIRECTION ( 'NONE',  ( -1.000000000000000000, -1.224606353822377258E-16, -0.000000000000000000 ) ) ;
#26091=AXIS2_PLACEMENT_3D ( 'NONE', #65803, #84112, #34536 ) ;
#26151=VERTEX_POINT ( 'NONE', #52185 ) ;
#26162=DIRECTION ( 'NONE',  ( 0.000000000000000000, 0.000000000000000000, 1.000000000000000000 ) ) ;
#26183=DIRECTION ( 'NONE',  ( 0.000000000000000000, -1.000000000000000000, 0.000000000000000000 ) ) ;
#26188=CIRCLE ( 'NONE', #86441, 5.000000000000002665 ) ;
#26189=VERTEX_POINT ( 'NONE', #59775 ) ;
#26212=DIRECTION ( 'NONE',  ( -1.000000000000000000, -0.000000000000000000, -0.000000000000000000 ) ) ;
#26294=VERTEX_POINT ( 'NONE', #20424 ) ;
#26327=DIRECTION ( 'NONE',  ( 0.000000000000000000, -0.5000000000000009992, -0.8660254037844380415 ) ) ;
#26339=ORIENTED_EDGE ( 'NONE', *, *, #102337, .F. ) ;
#26370=CARTESIAN_POINT ( 'NONE',  ( 28.17977184163764193, 1.482358050883964840E-15, 0.000000000000000000 ) ) ;
#26372=ORIENTED_EDGE ( 'NONE', *, *, #103652, .F. ) ;
#26377=EDGE_CURVE ( 'NONE', #44516, #13812, #35828, .T. ) ;
#26396=CARTESIAN_POINT ( 'NONE',  ( 0.4964154566687637438, -4.996589667937443302, -7.345652830558661250 ) ) ;
#26481=CARTESIAN_POINT ( 'NONE',  ( 0.4973051450695264442, -3.866309095700703136, 8.000000000000000000 ) ) ;
#26492=CIRCLE ( 'NONE', #84811, 5.000000000000002665 ) ;
#26495=CARTESIAN_POINT ( 'NONE',  ( 14.85284876471456350, 5.000000000000002665, 0.000000000000000000 ) ) ;
#26510=ORIENTED_EDGE ( 'NONE', *, *, #5663, .F. ) ;
#26512=CARTESIAN_POINT ( 'NONE',  ( 43.88846153846154152, 1.411358822780289120E-15, 0.000000000000000000 ) ) ;
#26522=CARTESIAN_POINT ( 'NONE',  ( 16.33361799548379523, 3.851859888774471706E-31, 5.000000000000001776 ) ) ;
#26609=CARTESIAN_POINT ( 'NONE',  ( 17.81438722625302518, 6.123233995736772199E-16, -5.000000000000001776 ) ) ;
#26625=LINE ( 'NONE', #59497, #18577 ) ;
#26666=VECTOR ( 'NONE', #25225, 999.9999999999998863 ) ;
#26672=EDGE_LOOP ( 'NONE', ( #16760, #28835, #84390, #16937, #103359 ) ) ;
#26682=AXIS2_PLACEMENT_3D ( 'NONE', #17491, #19651, #9900 ) ;
#26683=CIRCLE ( 'NONE', #73109, 5.000000000000002665 ) ;
#26688=ORIENTED_EDGE ( 'NONE', *, *, #84570, .T. ) ;
#26695=EDGE_CURVE ( 'NONE', #61495, #39668, #42624, .T. ) ;
#26741=DIRECTION ( 'NONE',  ( 0.000000000000000000, -1.000000000000000000, 0.000000000000000000 ) ) ;
#26745=ORIENTED_EDGE ( 'NONE', *, *, #92950, .T. ) ;
#26746=CARTESIAN_POINT ( 'NONE',  ( 33.52307692307692122, 4.172000000000003261, 0.000000000000000000 ) ) ;
#26762=DIRECTION ( 'NONE',  ( -1.000000000000000000, -1.224606353822377258E-16, -0.000000000000000000 ) ) ;
#26798=ORIENTED_EDGE ( 'NONE', *, *, #8144, .T. ) ;
#26838=EDGE_LOOP ( 'NONE', ( #33974, #56124, #38211, #100969, #87317 ) ) ;
#26850=ORIENTED_EDGE ( 'NONE', *, *, #97959, .T. ) ;
#26863=EDGE_CURVE ( 'NONE', #58211, #84262, #11739, .T. ) ;
#26868=ORIENTED_EDGE ( 'NONE', *, *, #104609, .F. ) ;
#26879=FACE_OUTER_BOUND ( 'NONE', #73309, .T. ) ;
#26907=AXIS2_PLACEMENT_3D ( 'NONE', #80575, #22394, #79525 ) ;
#26925=CONICAL_SURFACE ( 'NONE', #104410, 4.172000000000001485, 0.9599310885968750373 ) ;
#26965=VERTEX_POINT ( 'NONE', #48478 ) ;
#26967=EDGE_CURVE ( 'NONE', #31421, #81027, #16927, .T. ) ;
#26982=AXIS2_PLACEMENT_3D ( 'NONE', #65707, #82948, #16081 ) ;
#26987=DIRECTION ( 'NONE',  ( -1.000000000000000000, -0.000000000000000000, -0.000000000000000000 ) ) ;
#26992=DIRECTION ( 'NONE',  ( 0.000000000000000000, -1.000000000000000000, 0.000000000000000000 ) ) ;
#27022=ADVANCED_FACE ( 'NONE', ( #61388 ), #1334, .T. ) ;
#27034=AXIS2_PLACEMENT_3D ( 'NONE', #78013, #102825, #62378 ) ;
#27038=ORIENTED_EDGE ( 'NONE', *, *, #65516, .F. ) ;
#27040=FACE_OUTER_BOUND ( 'NONE', #68109, .T. ) ;
#27049=DIRECTION ( 'NONE',  ( 1.000000000000000000, 1.224606353822377258E-16, 0.000000000000000000 ) ) ;
#27083=DIRECTION ( 'NONE',  ( -1.000000000000000000, -1.224606353822377258E-16, -0.000000000000000000 ) ) ;
#27110=EDGE_CURVE ( 'NONE', #67362, #24694, #32420, .T. ) ;
#27124=DIRECTION ( 'NONE',  ( -1.000000000000000000, -1.224606353822377258E-16, -0.000000000000000000 ) ) ;
#27137=VECTOR ( 'NONE', #103783, 999.9999999999998863 ) ;
#27148=CYLINDRICAL_SURFACE ( 'NONE', #61895, 5.000000000000002665 ) ;
#27180=ORIENTED_EDGE ( 'NONE', *, *, #71883, .F. ) ;
#27220=CARTESIAN_POINT ( 'NONE',  ( 6.249999999999998224, 0.000000000000000000, 0.000000000000000000 ) ) ;
#27244=EDGE_LOOP ( 'NONE', ( #99171, #63795, #100668, #97545, #49668 ) ) ;
#27250=CARTESIAN_POINT ( 'NONE',  ( 0.000000000000000000, 0.000000000000000000, 0.000000000000000000 ) ) ;
#27280=ORIENTED_EDGE ( 'NONE', *, *, #57168, .T. ) ;
#27331=ORIENTED_EDGE ( 'NONE', *, *, #80971, .F. ) ;
#27353=DIRECTION ( 'NONE',  ( 0.5735764363510470476, -0.8191520442889911324, 1.003171929053524007E-16 ) ) ;
#27368=ORIENTED_EDGE ( 'NONE', *, *, #74195, .F. ) ;
#27425=EDGE_CURVE ( 'NONE', #95837, #85235, #87199, .T. ) ;
#27428=EDGE_LOOP ( 'NONE', ( #42154, #51118, #79452, #47330, #27331, #27038 ) ) ;
#27470=VERTEX_POINT ( 'NONE', #86083 ) ;
#27473=CONICAL_SURFACE ( 'NONE', #44618, 4.171999999999999709, 0.7853981633974708165 ) ;
#27508=ORIENTED_EDGE ( 'NONE', *, *, #84282, .T. ) ;
#27514=DIRECTION ( 'NONE',  ( -1.000000000000000000, -1.224606353822377258E-16, -0.000000000000000000 ) ) ;
#27529=CARTESIAN_POINT ( 'NONE',  ( 34.42407431220851066, 0.000000000000000000, 5.000000000000002665 ) ) ;
#27594=EDGE_LOOP ( 'NONE', ( #67751, #17113, #90300, #38816, #74497 ) ) ;
#27649=ADVANCED_FACE ( 'NONE', ( #85404 ), #69689, .T. ) ;
#27717=CIRCLE ( 'NONE', #50062, 5.000000000000001776 ) ;
#27729=CIRCLE ( 'NONE', #96519, 5.000000000000002665 ) ;
#27735=CARTESIAN_POINT ( 'NONE',  ( 20.77592568779148863, 5.000000000000002665, 0.000000000000000000 ) ) ;
#27742=CARTESIAN_POINT ( 'NONE',  ( 43.88846153846154152, -4.171999999999999709, 5.616230220889763424E-16 ) ) ;
#27747=DIRECTION ( 'NONE',  ( 0.5735764363510470476, -0.8191520442889911324, 1.003171929053524007E-16 ) ) ;
#27759=DIRECTION ( 'NONE',  ( -1.000000000000000000, -0.000000000000000000, -0.000000000000000000 ) ) ;
#27772=AXIS2_PLACEMENT_3D ( 'NONE', #12170, #94170, #70429 ) ;
#27775=CYLINDRICAL_SURFACE ( 'NONE', #55671, 5.000000000000002665 ) ;
#27786=DIRECTION ( 'NONE',  ( 1.000000000000000000, 0.000000000000000000, 0.000000000000000000 ) ) ;
#27822=AXIS2_PLACEMENT_3D ( 'NONE', #69623, #5409, #14005 ) ;
#27834=CARTESIAN_POINT ( 'NONE',  ( 34.10284876471455817, 1.482358050883964840E-15, 0.000000000000000000 ) ) ;
#27839=ORIENTED_EDGE ( 'NONE', *, *, #61779, .T. ) ;
#27855=CARTESIAN_POINT ( 'NONE',  ( 15.75384615384615294, 1.411358822780289120E-15, 0.000000000000000000 ) ) ;
#27894=ORIENTED_EDGE ( 'NONE', *, *, #103917, .T. ) ;
#27924=CARTESIAN_POINT ( 'NONE',  ( 12.79230769230769305, 1.411358822780289120E-15, 0.000000000000000000 ) ) ;
#27928=VERTEX_POINT ( 'NONE', #56724 ) ;
#27937=DIRECTION ( 'NONE',  ( 0.000000000000000000, -1.000000000000000000, 0.000000000000000000 ) ) ;
#27984=EDGE_CURVE ( 'NONE', #97763, #86992, #4244, .T. ) ;
#27988=DIRECTION ( 'NONE',  ( 0.000000000000000000, -1.000000000000000000, 0.000000000000000000 ) ) ;
#28014=DIRECTION ( 'NONE',  ( 0.5735764363510470476, -0.8191520442889911324, 1.003171929053524007E-16 ) ) ;
#28015=VERTEX_POINT ( 'NONE', #29722 ) ;
#28023=EDGE_CURVE ( 'NONE', #21850, #99464, #71434, .T. ) ;
#28036=ADVANCED_FACE ( 'NONE', ( #70683 ), #29213, .T. ) ;
#28048=CARTESIAN_POINT ( 'NONE',  ( 36.48461538461538822, 1.411358822780289120E-15, 0.000000000000000000 ) ) ;
#28079=FACE_OUTER_BOUND ( 'NONE', #10869, .T. ) ;
#28082=ORIENTED_EDGE ( 'NONE', *, *, #89521, .F. ) ;
#28083=DIRECTION ( 'NONE',  ( -1.000000000000000000, -0.000000000000000000, -0.000000000000000000 ) ) ;
#28102=ORIENTED_EDGE ( 'NONE', *, *, #93067, .T. ) ;
#28119=ORIENTED_EDGE ( 'NONE', *, *, #88580, .F. ) ;
#28162=EDGE_CURVE ( 'NONE', #28989, #32993, #55856, .T. ) ;
#28174=DIRECTION ( 'NONE',  ( -1.000000000000000000, -1.224606353822377258E-16, -0.000000000000000000 ) ) ;
#28188=CIRCLE ( 'NONE', #59187, 5.000000000000002665 ) ;
#28200=CARTESIAN_POINT ( 'NONE',  ( 34.10284876471455817, -5.000000000000000000, 6.123233995736768255E-16 ) ) ;
#28201=CYLINDRICAL_SURFACE ( 'NONE', #37859, 5.000000000000002665 ) ;
#28208=EDGE_CURVE ( 'NONE', #17199, #28900, #66544, .T. ) ;
#28212=DIRECTION ( 'NONE',  ( 0.000000000000000000, 0.000000000000000000, 1.000000000000000000 ) ) ;
#28246=ORIENTED_EDGE ( 'NONE', *, *, #70013, .F. ) ;
#28251=CARTESIAN_POINT ( 'NONE',  ( 38.54515645702225868, 1.482358050883964840E-15, 0.000000000000000000 ) ) ;
#28278=FACE_OUTER_BOUND ( 'NONE', #94851, .T. ) ;
#28316=DIRECTION ( 'NONE',  ( -1.000000000000000000, -1.224606353822377258E-16, -0.000000000000000000 ) ) ;
#28325=CARTESIAN_POINT ( 'NONE',  ( 31.46253585067004721, -4.999999999999990230, 0.000000000000000000 ) ) ;
#28346=ORIENTED_EDGE ( 'NONE', *, *, #59568, .T. ) ;
#28378=VERTEX_POINT ( 'NONE', #33261 ) ;
#28414=ORIENTED_EDGE ( 'NONE', *, *, #4528, .F. ) ;
#28417=ORIENTED_EDGE ( 'NONE', *, *, #53965, .F. ) ;
#28428=CARTESIAN_POINT ( 'NONE',  ( 0.000000000000000000, 0.000000000000000000, 8.000000000000000000 ) ) ;
#28433=EDGE_LOOP ( 'NONE', ( #63270, #527, #90316, #75731, #55245, #91788 ) ) ;
#28448=EDGE_CURVE ( 'NONE', #63004, #80882, #104417, .T. ) ;
#28452=AXIS2_PLACEMENT_3D ( 'NONE', #94675, #86053, #3522 ) ;
#28463=DIRECTION ( 'NONE',  ( -1.000000000000000000, -0.000000000000000000, -0.000000000000000000 ) ) ;
#28515=FACE_OUTER_BOUND ( 'NONE', #86087, .T. ) ;
#28539=EDGE_LOOP ( 'NONE', ( #104291, #45055, #39155, #85816, #58873, #95227 ) ) ;
#28545=DIRECTION ( 'NONE',  ( 0.000000000000000000, -1.000000000000000000, 0.000000000000000000 ) ) ;
#28569=ADVANCED_FACE ( 'NONE', ( #76344 ), #28927, .T. ) ;
#28591=DIRECTION ( 'NONE',  ( 0.000000000000000000, 1.000000000000000000, 0.000000000000000000 ) ) ;
#28608=AXIS2_PLACEMENT_3D ( 'NONE', #77235, #86418, #53998 ) ;
#28614=DIRECTION ( 'NONE',  ( -1.000000000000000000, -0.000000000000000000, -0.000000000000000000 ) ) ;
#28616=ORIENTED_EDGE ( 'NONE', *, *, #60694, .F. ) ;
#28619=DIRECTION ( 'NONE',  ( 0.5735764363510470476, -0.8191520442889911324, 1.003171929053524007E-16 ) ) ;
#28710=AXIS2_PLACEMENT_3D ( 'NONE', #17101, #55523, #88463 ) ;
#28725=LINE ( 'NONE', #5471, #18352 ) ;
#28726=DIRECTION ( 'NONE',  ( -1.000000000000000000, -1.224606353822377258E-16, -0.000000000000000000 ) ) ;
#28742=AXIS2_PLACEMENT_3D ( 'NONE', #2545, #99101, #25262 ) ;
#28747=AXIS2_PLACEMENT_3D ( 'NONE', #4053, #54697, #87108 ) ;
#28767=VECTOR ( 'NONE', #54152, 1000.000000000000227 ) ;
#28789=ADVANCED_FACE ( 'NONE', ( #87651 ), #102824, .T. ) ;
#28810=DIRECTION ( 'NONE',  ( 0.000000000000000000, 0.000000000000000000, 1.000000000000000000 ) ) ;
#28835=ORIENTED_EDGE ( 'NONE', *, *, #28023, .F. ) ;
#28842=VECTOR ( 'NONE', #36855, 999.9999999999998863 ) ;
#28851=VECTOR ( 'NONE', #12124, 999.9999999999998863 ) ;
#28900=VERTEX_POINT ( 'NONE', #106457 ) ;
#28927=CYLINDRICAL_SURFACE ( 'NONE', #21776, 5.000000000000002665 ) ;
#28939=EDGE_CURVE ( 'NONE', #98966, #42513, #83252, .T. ) ;
#28953=CARTESIAN_POINT ( 'NONE',  ( 42.40769230769231513, 4.172000000000003261, 5.109226446042759579E-16 ) ) ;
#28989=VERTEX_POINT ( 'NONE', #41205 ) ;
#28991=CARTESIAN_POINT ( 'NONE',  ( 35.58361799548379167, 1.482358050883964840E-15, 0.000000000000000000 ) ) ;
#29031=CIRCLE ( 'NONE', #49662, 4.172000000000001485 ) ;
#29038=ORIENTED_EDGE ( 'NONE', *, *, #14582, .T. ) ;
#29046=EDGE_LOOP ( 'NONE', ( #752, #98944, #42281, #80518, #48238, #15966 ) ) ;
#29071=CIRCLE ( 'NONE', #23890, 5.000000000000002665 ) ;
#29078=AXIS2_PLACEMENT_3D ( 'NONE', #23254, #31874, #65813 ) ;
#29090=CARTESIAN_POINT ( 'NONE',  ( 6.249999999999998224, 0.000000000000000000, 0.000000000000000000 ) ) ;
#29091=ORIENTED_EDGE ( 'NONE', *, *, #15124, .F. ) ;
#29093=VERTEX_POINT ( 'NONE', #34212 ) ;
#29141=AXIS2_PLACEMENT_3D ( 'NONE', #75343, #43533, #26327 ) ;
#29142=LINE ( 'NONE', #104557, #82709 ) ;
#29147=LINE ( 'NONE', #62017, #49335 ) ;
#29154=DIRECTION ( 'NONE',  ( 0.000000000000000000, 0.000000000000000000, 1.000000000000000000 ) ) ;
#29169=DIRECTION ( 'NONE',  ( -1.000000000000000000, -1.224606353822377258E-16, -0.000000000000000000 ) ) ;
#29180=DIRECTION ( 'NONE',  ( -1.000000000000000000, -1.224606353822377258E-16, -0.000000000000000000 ) ) ;
#29185=CARTESIAN_POINT ( 'NONE',  ( 32.94330508143927716, 6.123233995736770227E-16, -5.000000000000002665 ) ) ;
#29213=CYLINDRICAL_SURFACE ( 'NONE', #24882, 5.000000000000002665 ) ;
#29250=CARTESIAN_POINT ( 'NONE',  ( 46.85000000000000142, 0.000000000000000000, 4.171999999999999709 ) ) ;
#29302=CARTESIAN_POINT ( 'NONE',  ( 9.830769230769229594, -4.171999999999999709, 0.000000000000000000 ) ) ;
#29313=VERTEX_POINT ( 'NONE', #71838 ) ;
#29368=ORIENTED_EDGE ( 'NONE', *, *, #46650, .F. ) ;
#29384=DIRECTION ( 'NONE',  ( 0.000000000000000000, -1.000000000000000000, 0.000000000000000000 ) ) ;
#29416=DIRECTION ( 'NONE',  ( 0.000000000000000000, -0.5000000000000008882, 0.8660254037844382635 ) ) ;
#29441=DIRECTION ( 'NONE',  ( -1.000000000000000000, -1.224606353822377258E-16, -0.000000000000000000 ) ) ;
#29452=VERTEX_POINT ( 'NONE', #23866 ) ;
#29468=VERTEX_POINT ( 'NONE', #52347 ) ;
#29484=AXIS2_PLACEMENT_3D ( 'NONE', #62933, #102856, #94784 ) ;
#29485=VERTEX_POINT ( 'NONE', #76621 ) ;
#29501=DIRECTION ( 'NONE',  ( -1.000000000000000000, -0.000000000000000000, -0.000000000000000000 ) ) ;
#29535=EDGE_CURVE ( 'NONE', #39668, #61495, #78776, .T. ) ;
#29545=VERTEX_POINT ( 'NONE', #12943 ) ;
#29601=VERTEX_POINT ( 'NONE', #37274 ) ;
#29689=AXIS2_PLACEMENT_3D ( 'NONE', #40881, #83461, #51624 ) ;
#29690=EDGE_LOOP ( 'NONE', ( #2432, #75539, #67378, #7214, #18256, #19957 ) ) ;
#29722=CARTESIAN_POINT ( 'NONE',  ( 22.57792046605466041, 5.000000000000004441, 6.123233995736770227E-16 ) ) ;
#29767=ORIENTED_EDGE ( 'NONE', *, *, #72401, .T. ) ;
#29786=EDGE_CURVE ( 'NONE', #73528, #88469, #3026, .T. ) ;
#29790=ORIENTED_EDGE ( 'NONE', *, *, #44073, .F. ) ;
#29791=EDGE_CURVE ( 'NONE', #39953, #60654, #44689, .T. ) ;
#29800=CIRCLE ( 'NONE', #72786, 5.000000000000002665 ) ;
#29867=ORIENTED_EDGE ( 'NONE', *, *, #4626, .F. ) ;
#29871=CARTESIAN_POINT ( 'NONE',  ( 23.73746414932995208, 5.000000000000003553, 0.000000000000000000 ) ) ;
#29887=ORIENTED_EDGE ( 'NONE', *, *, #92312, .F. ) ;
#29890=ORIENTED_EDGE ( 'NONE', *, *, #17342, .F. ) ;
#29906=CIRCLE ( 'NONE', #497, 5.000000000000002665 ) ;
#29909=ORIENTED_EDGE ( 'NONE', *, *, #18802, .F. ) ;
#29913=CARTESIAN_POINT ( 'NONE',  ( 42.98746414932995208, 6.123233995736772199E-16, -5.000000000000001776 ) ) ;
#29917=CARTESIAN_POINT ( 'NONE',  ( 6.249999999999998224, 0.000000000000000000, 0.000000000000000000 ) ) ;
#29942=CARTESIAN_POINT ( 'NONE',  ( 0.000000000000000000, 6.123233995736770227E-16, -5.000000000000002665 ) ) ;
#29984=CYLINDRICAL_SURFACE ( 'NONE', #49093, 5.000000000000002665 ) ;
#29993=CONICAL_SURFACE ( 'NONE', #59226, 5.000000000000001776, 0.9599310885968803664 ) ;
#29999=EDGE_LOOP ( 'NONE', ( #23988, #73292, #59447, #61387, #35532 ) ) ;
#30001=ORIENTED_EDGE ( 'NONE', *, *, #17288, .F. ) ;
#30018=ORIENTED_EDGE ( 'NONE', *, *, #5663, .T. ) ;
#30023=CARTESIAN_POINT ( 'NONE',  ( 29.98176661990081371, 6.123233995736770227E-16, -5.000000000000002665 ) ) ;
#30039=LINE ( 'NONE', #20394, #80012 ) ;
#30052=AXIS2_PLACEMENT_3D ( 'NONE', #51470, #84915, #84385 ) ;
#30074=ORIENTED_EDGE ( 'NONE', *, *, #10619, .T. ) ;
#30102=CARTESIAN_POINT ( 'NONE',  ( 17.81438722625302518, 3.851859888774471706E-31, 5.000000000000001776 ) ) ;
#30106=ORIENTED_EDGE ( 'NONE', *, *, #34154, .F. ) ;
#30164=DIRECTION ( 'NONE',  ( 0.000000000000000000, 0.000000000000000000, -1.000000000000000000 ) ) ;
#30176=DIRECTION ( 'NONE',  ( 0.000000000000000000, -1.000000000000000000, 0.000000000000000000 ) ) ;
#30186=DIRECTION ( 'NONE',  ( -1.000000000000000000, -1.224606353822377258E-16, -0.000000000000000000 ) ) ;
#30197=CARTESIAN_POINT ( 'NONE',  ( 27.02022815836235026, -5.000000000000000000, 0.000000000000000000 ) ) ;
#30203=CIRCLE ( 'NONE', #93952, 5.000000000000002665 ) ;
#30207=CARTESIAN_POINT ( 'NONE',  ( 38.54515645702225868, -5.000000000000000888, 6.123233995736769241E-16 ) ) ;
#30241=EDGE_LOOP ( 'NONE', ( #7754, #26372, #75671, #84316, #84461 ) ) ;
#30252=CARTESIAN_POINT ( 'NONE',  ( 0.000000000000000000, 0.000000000000000000, 0.000000000000000000 ) ) ;
#30286=ORIENTED_EDGE ( 'NONE', *, *, #29786, .T. ) ;
#30297=CARTESIAN_POINT ( 'NONE',  ( 0.06809871960542752956, 6.146186931204407067, 5.354491962338127742 ) ) ;
#30306=DIRECTION ( 'NONE',  ( -1.000000000000000000, -1.224606353822377258E-16, -0.000000000000000000 ) ) ;
#30310=DIRECTION ( 'NONE',  ( -1.000000000000000000, -1.224606353822377258E-16, -0.000000000000000000 ) ) ;
#30316=ADVANCED_FACE ( 'NONE', ( #101986 ), #37294, .T. ) ;
#30380=EDGE_CURVE ( 'NONE', #36732, #12690, #29031, .T. ) ;
#30385=DIRECTION ( 'NONE',  ( 0.000000000000000000, -1.000000000000000000, 0.000000000000000000 ) ) ;
#30414=ORIENTED_EDGE ( 'NONE', *, *, #55995, .F. ) ;
#30449=VERTEX_POINT ( 'NONE', #104103 ) ;
#30460=CARTESIAN_POINT ( 'NONE',  ( 32.04230769230768772, 4.172000000000003261, 5.109226446042759579E-16 ) ) ;
#30471=CARTESIAN_POINT ( 'NONE',  ( 31.14131030317610538, 5.000000000000003553, 0.000000000000000000 ) ) ;
#30504=CARTESIAN_POINT ( 'NONE',  ( 0.08224679563971343255, 7.710515798486365036, 2.644994884459111351 ) ) ;
#30515=AXIS2_PLACEMENT_3D ( 'NONE', #18944, #2706, #68533 ) ;
#30541=CARTESIAN_POINT ( 'NONE',  ( 0.000000000000000000, 0.000000000000000000, 0.000000000000000000 ) ) ;
#30606=ORIENTED_EDGE ( 'NONE', *, *, #83581, .T. ) ;
#30622=VERTEX_POINT ( 'NONE', #85700 ) ;
#30633=AXIS2_PLACEMENT_3D ( 'NONE', #100904, #59955, #92822 ) ;
#30653=LINE ( 'NONE', #45749, #65590 ) ;
#30654=ORIENTED_EDGE ( 'NONE', *, *, #99863, .T. ) ;
#30707=CIRCLE ( 'NONE', #92648, 5.000000000000002665 ) ;
#30709=DIRECTION ( 'NONE',  ( -1.000000000000000000, -1.224606353822377258E-16, -0.000000000000000000 ) ) ;
#30734=EDGE_CURVE ( 'NONE', #2627, #7097, #32456, .T. ) ;
#30738=ORIENTED_EDGE ( 'NONE', *, *, #100360, .T. ) ;
#30741=CIRCLE ( 'NONE', #25596, 5.000000000000001776 ) ;
#30743=DIRECTION ( 'NONE',  ( -1.000000000000000000, -1.224606353822377258E-16, -0.000000000000000000 ) ) ;
#30754=DIRECTION ( 'NONE',  ( -1.000000000000000000, -0.000000000000000000, -0.000000000000000000 ) ) ;
#30756=CARTESIAN_POINT ( 'NONE',  ( 37.06438722625302518, 1.482358050883964840E-15, 0.000000000000000000 ) ) ;
#30779=CARTESIAN_POINT ( 'NONE',  ( 15.17407431220850533, 5.000000000000004441, 6.123233995736770227E-16 ) ) ;
#30839=CARTESIAN_POINT ( 'NONE',  ( 41.82792046605465686, 0.000000000000000000, 5.000000000000002665 ) ) ;
#30858=DIRECTION ( 'NONE',  ( -0.5735764363510512664, 0.8191520442889881348, 1.003171929053520309E-16 ) ) ;
#30905=DIRECTION ( 'NONE',  ( 0.000000000000000000, 0.000000000000000000, -1.000000000000000000 ) ) ;
#30909=FACE_OUTER_BOUND ( 'NONE', #18329, .T. ) ;
#30910=EDGE_CURVE ( 'NONE', #16452, #36720, #99555, .T. ) ;
#30967=DIRECTION ( 'NONE',  ( -1.000000000000000000, -1.224606353822377258E-16, -0.000000000000000000 ) ) ;
#30968=CIRCLE ( 'NONE', #53346, 4.172000000000001485 ) ;
#30978=FACE_OUTER_BOUND ( 'NONE', #36924, .T. ) ;
#30987=CARTESIAN_POINT ( 'NONE',  ( 22.25669491856071858, 1.482358050883964840E-15, 0.000000000000000000 ) ) ;
#30988=ADVANCED_FACE ( 'NONE', ( #99604 ), #7401, .T. ) ;
#30998=CARTESIAN_POINT ( 'NONE',  ( 0.3173508448886502298, -5.375634714784614410, 6.689127551062007626 ) ) ;
#31008=VECTOR ( 'NONE', #94721, 1000.000000000000227 ) ;
#31014=AXIS2_PLACEMENT_3D ( 'NONE', #20245, #28316, #29384 ) ;
#31017=ORIENTED_EDGE ( 'NONE', *, *, #94440, .T. ) ;
#31031=VECTOR ( 'NONE', #37520, 1000.000000000000227 ) ;
#31060=CARTESIAN_POINT ( 'NONE',  ( 15.17407431220850533, -5.000000000000000000, 0.000000000000000000 ) ) ;
#31075=VERTEX_POINT ( 'NONE', #54762 ) ;
#31084=ORIENTED_EDGE ( 'NONE', *, *, #106243, .T. ) ;
#31088=DIRECTION ( 'NONE',  ( -1.000000000000000000, -1.224606353822377258E-16, -0.000000000000000000 ) ) ;
#31096=LINE ( 'NONE', #56363, #74701 ) ;
#31099=ORIENTED_EDGE ( 'NONE', *, *, #11140, .F. ) ;
#31117=CARTESIAN_POINT ( 'NONE',  ( 20.19615384615384457, -4.171999999999999709, 0.000000000000000000 ) ) ;
#31149=DIRECTION ( 'NONE',  ( -1.000000000000000000, -1.224606353822377258E-16, -0.000000000000000000 ) ) ;
#31206=FACE_OUTER_BOUND ( 'NONE', #44685, .T. ) ;
#31251=DIRECTION ( 'NONE',  ( 0.000000000000000000, 1.000000000000000000, 0.000000000000000000 ) ) ;
#31259=CARTESIAN_POINT ( 'NONE',  ( 45.94900261086841198, 5.000000000000003553, 0.000000000000000000 ) ) ;
#31272=CARTESIAN_POINT ( 'NONE',  ( 15.75384615384615294, 1.411358822780289120E-15, 0.000000000000000000 ) ) ;
#31276=EDGE_LOOP ( 'NONE', ( #55176, #20284, #39911, #19259, #91932, #16105 ) ) ;
#31278=CARTESIAN_POINT ( 'NONE',  ( 30.56153846153846132, 4.172000000000003261, 5.109226446042759579E-16 ) ) ;
#31294=EDGE_LOOP ( 'NONE', ( #3514, #75984, #95786, #19747, #42106 ) ) ;
#31302=AXIS2_PLACEMENT_3D ( 'NONE', #83611, #92231, #34583 ) ;
#31308=CARTESIAN_POINT ( 'NONE',  ( 29.98176661990081371, -5.000000000000000000, 0.000000000000000000 ) ) ;
#31325=ORIENTED_EDGE ( 'NONE', *, *, #33297, .T. ) ;
#31331=LINE ( 'NONE', #55017, #46087 ) ;
#31343=FACE_OUTER_BOUND ( 'NONE', #21298, .T. ) ;
#31405=EDGE_LOOP ( 'NONE', ( #61621, #45841, #106475, #86722, #31997 ) ) ;
#31407=DIRECTION ( 'NONE',  ( -1.000000000000000000, -0.000000000000000000, -0.000000000000000000 ) ) ;
#31408=ADVANCED_FACE ( 'NONE', ( #49677 ), #39377, .T. ) ;
#31421=VERTEX_POINT ( 'NONE', #84714 ) ;
#31508=ORIENTED_EDGE ( 'NONE', *, *, #100761, .F. ) ;
#31542=CIRCLE ( 'NONE', #93510, 5.000000000000001776 ) ;
#31546=DIRECTION ( 'NONE',  ( 0.000000000000000000, -1.000000000000000000, 0.000000000000000000 ) ) ;
#31549=VERTEX_POINT ( 'NONE', #42393 ) ;
#31570=CARTESIAN_POINT ( 'NONE',  ( 0.3173508448886549482, 8.480771745766404024, 1.310872448937998813 ) ) ;
#31575=CARTESIAN_POINT ( 'NONE',  ( 29.66054107240687543, 6.123233995736772199E-16, -5.000000000000001776 ) ) ;
#31580=LINE ( 'NONE', #80089, #55129 ) ;
#31612=CONICAL_SURFACE ( 'NONE', #52280, 5.000000000000001776, 0.9599310885968803664 ) ;
#31632=EDGE_CURVE ( 'NONE', #82401, #61254, #68790, .T. ) ;
#31635=LINE ( 'NONE', #31117, #50295 ) ;
#31639=ADVANCED_FACE ( 'NONE', ( #51550 ), #84463, .T. ) ;
#31687=PRODUCT_DEFINITION_CONTEXT ( 'detailed design', #95471, 'design' ) ;
#31760=EDGE_LOOP ( 'NONE', ( #40946, #70928, #22844, #28119, #61898, #101341 ) ) ;
#31767=ADVANCED_FACE ( 'NONE', ( #77963 ), #27473, .T. ) ;
#31772=CONICAL_SURFACE ( 'NONE', #11108, 4.172000000000001485, 0.9599310885968750373 ) ;
#31785=FACE_OUTER_BOUND ( 'NONE', #67558, .T. ) ;
#31819=DIRECTION ( 'NONE',  ( 0.000000000000000000, -0.5000000000000013323, -0.8660254037844379305 ) ) ;
#31859=ORIENTED_EDGE ( 'NONE', *, *, #31632, .F. ) ;
#31874=DIRECTION ( 'NONE',  ( -1.000000000000000000, -1.224606353822377258E-16, -0.000000000000000000 ) ) ;
#31879=CARTESIAN_POINT ( 'NONE',  ( 43.30868969682389036, 0.000000000000000000, 5.000000000000002665 ) ) ;
#31895=DIRECTION ( 'NONE',  ( -0.5735764363510512664, 0.8191520442889881348, 1.003171929053520309E-16 ) ) ;
#31922=ORIENTED_EDGE ( 'NONE', *, *, #68612, .F. ) ;
#31934=ORIENTED_EDGE ( 'NONE', *, *, #32278, .T. ) ;
#31968=ORIENTED_EDGE ( 'NONE', *, *, #94161, .F. ) ;
#31980=VECTOR ( 'NONE', #36003, 1000.000000000000000 ) ;
#31983=CARTESIAN_POINT ( 'NONE',  ( 8.929771841637641927, 1.482358050883964840E-15, 0.000000000000000000 ) ) ;
#31997=ORIENTED_EDGE ( 'NONE', *, *, #46986, .T. ) ;
#32003=ORIENTED_EDGE ( 'NONE', *, *, #34555, .F. ) ;
#32016=ADVANCED_FACE ( 'NONE', ( #76761 ), #46445, .T. ) ;
#32045=AXIS2_PLACEMENT_3D ( 'NONE', #28251, #94012, #20172 ) ;
#32070=ORIENTED_EDGE ( 'NONE', *, *, #807, .T. ) ;
#32076=ORIENTED_EDGE ( 'NONE', *, *, #15158, .T. ) ;
#32118=EDGE_LOOP ( 'NONE', ( #101199, #67593, #33934, #9507, #23173 ) ) ;
#32123=LINE ( 'NONE', #50395, #100694 ) ;
#32124=AXIS2_PLACEMENT_3D ( 'NONE', #69757, #44419, #36370 ) ;
#32144=CARTESIAN_POINT ( 'NONE',  ( 0.000000000000000000, 6.123233995736770227E-16, -5.000000000000002665 ) ) ;
#32180=EDGE_CURVE ( 'NONE', #48676, #83974, #103267, .T. ) ;
#32192=DIRECTION ( 'NONE',  ( -1.000000000000000000, -1.224606353822377258E-16, -0.000000000000000000 ) ) ;
#32195=ORIENTED_EDGE ( 'NONE', *, *, #76053, .F. ) ;
#32197=AXIS2_PLACEMENT_3D ( 'NONE', #24119, #72627, #47806 ) ;
#32250=CONICAL_SURFACE ( 'NONE', #40851, 4.172000000000001485, 0.9599310885968750373 ) ;
#32251=FACE_OUTER_BOUND ( 'NONE', #80810, .T. ) ;
#32252=CONICAL_SURFACE ( 'NONE', #92505, 5.000000000000001776, 0.9599310885968803664 ) ;
#32270=EDGE_CURVE ( 'NONE', #29313, #98120, #47572, .T. ) ;
#32278=EDGE_CURVE ( 'NONE', #89827, #79740, #10246, .T. ) ;
#32287=AXIS2_PLACEMENT_3D ( 'NONE', #68803, #61236, #62304 ) ;
#32324=DIRECTION ( 'NONE',  ( 0.000000000000000000, 0.000000000000000000, 1.000000000000000000 ) ) ;
#32329=ORIENTED_EDGE ( 'NONE', *, *, #25561, .F. ) ;
#32345=PLANE ( 'NONE',  #17546 ) ;
#32378=DIRECTION ( 'NONE',  ( 0.000000000000000000, -1.000000000000000000, 0.000000000000000000 ) ) ;
#32389=CYLINDRICAL_SURFACE ( 'NONE', #37205, 5.000000000000002665 ) ;
#32417=DIRECTION ( 'NONE',  ( -1.000000000000000000, -0.000000000000000000, -0.000000000000000000 ) ) ;
#32420=CIRCLE ( 'NONE', #6508, 5.000000000000002665 ) ;
#32442=ORIENTED_EDGE ( 'NONE', *, *, #94820, .T. ) ;
#32444=( NAMED_UNIT ( * ) PLANE_ANGLE_UNIT ( ) SI_UNIT ( $, .RADIAN. ) );
#32456=CIRCLE ( 'NONE', #92715, 4.172000000000001485 ) ;
#32505=ORIENTED_EDGE ( 'NONE', *, *, #8473, .F. ) ;
#32604=CIRCLE ( 'NONE', #80763, 5.000000000000002665 ) ;
#32639=CARTESIAN_POINT ( 'NONE',  ( 38.54515645702225868, 1.482358050883964840E-15, 0.000000000000000000 ) ) ;
#32654=ORIENTED_EDGE ( 'NONE', *, *, #52312, .T. ) ;
#32669=CARTESIAN_POINT ( 'NONE',  ( 9.250997389131581983, 1.340359594676612611E-15, 0.000000000000000000 ) ) ;
#32697=DIRECTION ( 'NONE',  ( 0.000000000000000000, 1.000000000000000000, 0.000000000000000000 ) ) ;
#32699=CIRCLE ( 'NONE', #32779, 5.000000000000002665 ) ;
#32704=CIRCLE ( 'NONE', #92965, 5.000000000000001776 ) ;
#32710=CIRCLE ( 'NONE', #65412, 5.000000000000001776 ) ;
#32715=DIRECTION ( 'NONE',  ( 0.000000000000000000, 0.5000000000000013323, 0.8660254037844378194 ) ) ;
#32720=VERTEX_POINT ( 'NONE', #31308 ) ;
#32757=AXIS2_PLACEMENT_3D ( 'NONE', #2014, #81857, #7980 ) ;
#32778=ORIENTED_EDGE ( 'NONE', *, *, #79709, .T. ) ;
#32779=AXIS2_PLACEMENT_3D ( 'NONE', #11958, #28726, #85333 ) ;
#32795=CARTESIAN_POINT ( 'NONE',  ( 29.98176661990081371, 1.340359594676612611E-15, 0.000000000000000000 ) ) ;
#32844=ORIENTED_EDGE ( 'NONE', *, *, #92693, .F. ) ;
#32848=ADVANCED_FACE ( 'NONE', ( #66712 ), #18765, .T. ) ;
#32857=DIRECTION ( 'NONE',  ( -1.000000000000000000, -1.224606353822377258E-16, -0.000000000000000000 ) ) ;
#32861=VERTEX_POINT ( 'NONE', #41893 ) ;
#32887=EDGE_CURVE ( 'NONE', #57077, #86773, #75771, .T. ) ;
#32896=DIRECTION ( 'NONE',  ( -1.000000000000000000, -1.224606353822377258E-16, -0.000000000000000000 ) ) ;
#32898=AXIS2_PLACEMENT_3D ( 'NONE', #29090, #54337, #87279 ) ;
#32923=ADVANCED_FACE ( 'NONE', ( #28278 ), #98018, .T. ) ;
#32929=CYLINDRICAL_SURFACE ( 'NONE', #26091, 5.000000000000002665 ) ;
#32968=AXIS2_PLACEMENT_3D ( 'NONE', #90454, #24683, #57532 ) ;
#32993=VERTEX_POINT ( 'NONE', #37965 ) ;
#32996=CYLINDRICAL_SURFACE ( 'NONE', #101246, 5.000000000000002665 ) ;
#33026=CARTESIAN_POINT ( 'NONE',  ( 10.41054107240687188, 1.482358050883964840E-15, 0.000000000000000000 ) ) ;
#33035=CIRCLE ( 'NONE', #27822, 5.000000000000002665 ) ;
#33037=VERTEX_POINT ( 'NONE', #44975 ) ;
#33087=DIRECTION ( 'NONE',  ( -1.000000000000000000, -0.000000000000000000, -0.000000000000000000 ) ) ;
#33108=EDGE_CURVE ( 'NONE', #12693, #82401, #63548, .T. ) ;
#33126=VERTEX_POINT ( 'NONE', #97732 ) ;
#33138=FACE_OUTER_BOUND ( 'NONE', #62097, .T. ) ;
#33159=VERTEX_POINT ( 'NONE', #105833 ) ;
#33184=CIRCLE ( 'NONE', #83052, 5.000000000000002665 ) ;
#33202=EDGE_CURVE ( 'NONE', #29452, #2025, #32604, .T. ) ;
#33222=DIRECTION ( 'NONE',  ( -1.000000000000000000, -1.224606353822377258E-16, -0.000000000000000000 ) ) ;
#33240=AXIS2_PLACEMENT_3D ( 'NONE', #66048, #100005, #42836 ) ;
#33255=CARTESIAN_POINT ( 'NONE',  ( 40.02592568779148507, -5.000000000000000888, 6.123233995736769241E-16 ) ) ;
#33261=CARTESIAN_POINT ( 'NONE',  ( 17.23461538461538467, -4.171999999999999709, 5.616230220889763424E-16 ) ) ;
#33297=EDGE_CURVE ( 'NONE', #96464, #65523, #91109, .T. ) ;
#33299=CARTESIAN_POINT ( 'NONE',  ( 40.92692307692308162, 1.411358822780289120E-15, 0.000000000000000000 ) ) ;
#33307=DIRECTION ( 'NONE',  ( 0.000000000000000000, 0.000000000000000000, 1.000000000000000000 ) ) ;
#33330=ORIENTED_EDGE ( 'NONE', *, *, #87196, .F. ) ;
#33367=CARTESIAN_POINT ( 'NONE',  ( 32.62207953394533178, -5.000000000000000888, 6.123233995736769241E-16 ) ) ;
#33370=DIRECTION ( 'NONE',  ( -1.000000000000000000, -1.224606353822377258E-16, -0.000000000000000000 ) ) ;
#33371=ADVANCED_FACE ( 'NONE', ( #10842 ), #25696, .T. ) ;
#33378=EDGE_LOOP ( 'NONE', ( #89416, #66032, #106020, #64226, #90462 ) ) ;
#33464=CARTESIAN_POINT ( 'NONE',  ( 19.61638200451619696, -5.000000000000000000, 0.000000000000000000 ) ) ;
#33492=CARTESIAN_POINT ( 'NONE',  ( 17.23461538461538467, 4.172000000000003261, 5.109226446042759579E-16 ) ) ;
#33502=MECHANICAL_DESIGN_GEOMETRIC_PRESENTATION_REPRESENTATION('',(#61073),#62770);
#33516=LINE ( 'NONE', #7606, #69769 ) ;
#33519=EDGE_CURVE ( 'NONE', #4042, #35042, #66992, .T. ) ;
#33590=VERTEX_POINT ( 'NONE', #3848 ) ;
#33622=CARTESIAN_POINT ( 'NONE',  ( 31.46253585067004721, 1.340359594676612611E-15, 0.000000000000000000 ) ) ;
#33633=DIRECTION ( 'NONE',  ( 1.000000000000000000, 0.000000000000000000, 0.000000000000000000 ) ) ;
#33639=ORIENTED_EDGE ( 'NONE', *, *, #21622, .F. ) ;
#33671=EDGE_CURVE ( 'NONE', #26189, #98844, #66855, .T. ) ;
#33693=DIRECTION ( 'NONE',  ( 0.000000000000000000, -1.000000000000000000, 0.000000000000000000 ) ) ;
#33706=ORIENTED_EDGE ( 'NONE', *, *, #82143, .F. ) ;
#33718=EDGE_CURVE ( 'NONE', #28989, #48371, #87294, .T. ) ;
#33744=VECTOR ( 'NONE', #23847, 1000.000000000000000 ) ;
#33748=CARTESIAN_POINT ( 'NONE',  ( 19.29515645702225868, 6.123233995736772199E-16, -5.000000000000001776 ) ) ;
#33752=DIRECTION ( 'NONE',  ( 0.000000000000000000, -1.000000000000000000, 0.000000000000000000 ) ) ;
#33830=VERTEX_POINT ( 'NONE', #60061 ) ;
#33871=CARTESIAN_POINT ( 'NONE',  ( 29.08076923076923137, 4.172000000000003261, 5.109226446042759579E-16 ) ) ;
#33903=AXIS2_PLACEMENT_3D ( 'NONE', #65711, #7988, #48445 ) ;
#33908=ORIENTED_EDGE ( 'NONE', *, *, #20768, .F. ) ;
#33920=CARTESIAN_POINT ( 'NONE',  ( 19.29515645702225868, 1.482358050883964840E-15, 0.000000000000000000 ) ) ;
#33934=ORIENTED_EDGE ( 'NONE', *, *, #1070, .T. ) ;
#33949=ADVANCED_FACE ( 'NONE', ( #102580 ), #28201, .T. ) ;
#33962=CARTESIAN_POINT ( 'NONE',  ( 22.25669491856071858, -5.000000000000000000, 6.123233995736768255E-16 ) ) ;
#33968=ORIENTED_EDGE ( 'NONE', *, *, #78143, .F. ) ;
#33974=ORIENTED_EDGE ( 'NONE', *, *, #51604, .F. ) ;
#33991=CARTESIAN_POINT ( 'NONE',  ( 12.79230769230769305, 1.411358822780289120E-15, 0.000000000000000000 ) ) ;
#33994=EDGE_LOOP ( 'NONE', ( #23980, #77848, #20644, #97111, #91416, #16030 ) ) ;
#33998=DIRECTION ( 'NONE',  ( -1.000000000000000000, -1.224606353822377258E-16, -0.000000000000000000 ) ) ;
#34000=CARTESIAN_POINT ( 'NONE',  ( 6.249999999999998224, -4.618802153517012954, -8.000000000000001776 ) ) ;
#34020=FILL_AREA_STYLE_COLOUR ( '', #61039 ) ;
#34052=VECTOR ( 'NONE', #57781, 1000.000000000000000 ) ;
#34154=EDGE_CURVE ( 'NONE', #98655, #34834, #66223, .T. ) ;
#34168=B_SPLINE_CURVE_WITH_KNOTS ( 'NONE', 3,
 ( #39266, #87810, #96952, #78626, #37698, #79168, #104504, #22023 ),
 .UNSPECIFIED., .F., .F.,
 ( 4, 2, 2, 4 ),
 ( 0.01336725832182608306, 0.01453745201803765055, 0.01570764571424921457, 0.01804803310667234956 ),
 .UNSPECIFIED. ) ;
#34188=EDGE_CURVE ( 'NONE', #75560, #99927, #3564, .T. ) ;
#34198=AXIS2_PLACEMENT_3D ( 'NONE', #58781, #17792, #100807 ) ;
#34199=EDGE_CURVE ( 'NONE', #23846, #19012, #36165, .T. ) ;
#34200=DIRECTION ( 'NONE',  ( -1.000000000000000000, -1.224606353822377258E-16, -0.000000000000000000 ) ) ;
#34209=CIRCLE ( 'NONE', #29078, 5.000000000000002665 ) ;
#34212=CARTESIAN_POINT ( 'NONE',  ( 41.50669491856072568, 3.851859888774471706E-31, 5.000000000000001776 ) ) ;
#34222=ADVANCED_FACE ( 'NONE', ( #26879 ), #102857, .T. ) ;
#34229=EDGE_CURVE ( 'NONE', #54320, #58994, #70614, .T. ) ;
#34232=ORIENTED_EDGE ( 'NONE', *, *, #87196, .T. ) ;
#34293=ADVANCED_FACE ( 'NONE', ( #44091 ), #67152, .T. ) ;
#34325=VECTOR ( 'NONE', #92864, 1000.000000000000000 ) ;
#34445=LINE ( 'NONE', #51096, #73501 ) ;
#34470=AXIS2_PLACEMENT_3D ( 'NONE', #33299, #106624, #24678 ) ;
#34492=DIRECTION ( 'NONE',  ( -1.000000000000000000, -1.224606353822377258E-16, -0.000000000000000000 ) ) ;
#34496=EDGE_CURVE ( 'NONE', #5037, #106154, #63765, .T. ) ;
#34514=AXIS2_PLACEMENT_3D ( 'NONE', #47638, #96224, #7707 ) ;
#34526=FACE_OUTER_BOUND ( 'NONE', #90308, .T. ) ;
#34530=DIRECTION ( 'NONE',  ( -1.000000000000000000, -1.224606353822377258E-16, -0.000000000000000000 ) ) ;
#34532=VECTOR ( 'NONE', #16824, 1000.000000000000000 ) ;
#34536=DIRECTION ( 'NONE',  ( 0.000000000000000000, 0.000000000000000000, 1.000000000000000000 ) ) ;
#34555=EDGE_CURVE ( 'NONE', #75282, #39269, #57458, .T. ) ;
#34556=CIRCLE ( 'NONE', #101662, 8.000000000000000000 ) ;
#34566=CARTESIAN_POINT ( 'NONE',  ( 40.02592568779148507, -5.000000000000000000, 6.123233995736768255E-16 ) ) ;
#34583=DIRECTION ( 'NONE',  ( 0.000000000000000000, -1.000000000000000000, 0.000000000000000000 ) ) ;
#34584=CIRCLE ( 'NONE', #94860, 5.000000000000001776 ) ;
#34614=DIRECTION ( 'NONE',  ( -1.000000000000000000, -1.224606353822377258E-16, -0.000000000000000000 ) ) ;
#34629=CARTESIAN_POINT ( 'NONE',  ( 42.98746414932995208, 1.482358050883964840E-15, 0.000000000000000000 ) ) ;
#34653=DIRECTION ( 'NONE',  ( 0.000000000000000000, 0.000000000000000000, -1.000000000000000000 ) ) ;
#34660=AXIS2_PLACEMENT_3D ( 'NONE', #9853, #33633, #66513 ) ;
#34663=CYLINDRICAL_SURFACE ( 'NONE', #54498, 8.000000000000000000 ) ;
#34676=DIRECTION ( 'NONE',  ( 0.000000000000000000, -1.000000000000000000, 0.000000000000000000 ) ) ;
#34681=DIRECTION ( 'NONE',  ( 0.000000000000000000, -1.000000000000000000, 0.000000000000000000 ) ) ;
#34689=EDGE_CURVE ( 'NONE', #27470, #95088, #44841, .T. ) ;
#34697=ORIENTED_EDGE ( 'NONE', *, *, #12344, .T. ) ;
#34702=LINE ( 'NONE', #2276, #1563 ) ;
#34703=EDGE_CURVE ( 'NONE', #79952, #60839, #3482, .T. ) ;
#34786=ORIENTED_EDGE ( 'NONE', *, *, #40339, .F. ) ;
#34794=DIRECTION ( 'NONE',  ( -1.000000000000000000, -1.224606353822377258E-16, -0.000000000000000000 ) ) ;
#34813=CIRCLE ( 'NONE', #3756, 5.000000000000002665 ) ;
#34825=CYLINDRICAL_SURFACE ( 'NONE', #60735, 5.000000000000002665 ) ;
#34834=VERTEX_POINT ( 'NONE', #42499 ) ;
#34888=DIRECTION ( 'NONE',  ( 0.000000000000000000, -1.000000000000000000, 0.000000000000000000 ) ) ;
#34907=DIRECTION ( 'NONE',  ( 0.000000000000000000, -1.000000000000000000, 0.000000000000000000 ) ) ;
#34933=CARTESIAN_POINT ( 'NONE',  ( 6.849999999999999645, -9.237604307034018802, 3.355146209984123968E-17 ) ) ;
#34934=ADVANCED_FACE ( 'NONE', ( #403 ), #72366, .T. ) ;
#34942=EDGE_CURVE ( 'NONE', #39671, #30449, #12085, .T. ) ;
#34960=CARTESIAN_POINT ( 'NONE',  ( 13.37207953394533355, 1.482358050883964840E-15, 0.000000000000000000 ) ) ;
#34962=CARTESIAN_POINT ( 'NONE',  ( 0.7145311798161616545, -4.618802153517262532, -8.000000000000001776 ) ) ;
#34995=AXIS2_PLACEMENT_3D ( 'NONE', #59098, #76320, #20278 ) ;
#34998=DIRECTION ( 'NONE',  ( -1.000000000000000000, -0.000000000000000000, -0.000000000000000000 ) ) ;
#35016=ORIENTED_EDGE ( 'NONE', *, *, #59568, .F. ) ;
#35031=VECTOR ( 'NONE', #41950, 1000.000000000000227 ) ;
#35042=VERTEX_POINT ( 'NONE', #95843 ) ;
#35071=ORIENTED_EDGE ( 'NONE', *, *, #65428, .T. ) ;
#35105=AXIS2_PLACEMENT_3D ( 'NONE', #51741, #69542, #85740 ) ;
#35145=CARTESIAN_POINT ( 'NONE',  ( 22.25669491856071858, 1.482358050883964840E-15, 0.000000000000000000 ) ) ;
#35231=FACE_OUTER_BOUND ( 'NONE', #60779, .T. ) ;
#35294=DIRECTION ( 'NONE',  ( 1.000000000000000000, 0.000000000000000000, 0.000000000000000000 ) ) ;
#35297=CIRCLE ( 'NONE', #28452, 5.000000000000002665 ) ;
#35331=B_SPLINE_CURVE_WITH_KNOTS ( 'NONE', 3,
 ( #45418, #12482, #38912, #30297, #96080, #22211 ),
 .UNSPECIFIED., .F., .F.,
 ( 4, 2, 4 ),
 ( 2.380731629582122378E-07, 0.002336973833157553367, 0.004673709593152147908 ),
 .UNSPECIFIED. ) ;
#35333=ORIENTED_EDGE ( 'NONE', *, *, #100360, .F. ) ;
#35352=EDGE_CURVE ( 'NONE', #9677, #42925, #59458, .T. ) ;
#35362=AXIS2_PLACEMENT_3D ( 'NONE', #96180, #5559, #22842 ) ;
#35384=FACE_OUTER_BOUND ( 'NONE', #23070, .T. ) ;
#35415=CARTESIAN_POINT ( 'NONE',  ( 41.50669491856072568, -5.000000000000000888, 6.123233995736769241E-16 ) ) ;
#35447=EDGE_LOOP ( 'NONE', ( #48164, #73508, #61997, #3280, #83153 ) ) ;
#35458=CIRCLE ( 'NONE', #11214, 5.000000000000001776 ) ;
#35464=VERTEX_POINT ( 'NONE', #57882 ) ;
#35469=PLANE ( 'NONE',  #29141 ) ;
#35497=CARTESIAN_POINT ( 'NONE',  ( 37.96538461538461462, 4.172000000000003261, 0.000000000000000000 ) ) ;
#35514=ORIENTED_EDGE ( 'NONE', *, *, #80825, .F. ) ;
#35529=ORIENTED_EDGE ( 'NONE', *, *, #83581, .F. ) ;
#35531=CIRCLE ( 'NONE', #49258, 5.000000000000001776 ) ;
#35532=ORIENTED_EDGE ( 'NONE', *, *, #97424, .F. ) ;
#35574=ORIENTED_EDGE ( 'NONE', *, *, #3686, .F. ) ;
#35591=CARTESIAN_POINT ( 'NONE',  ( 44.46823338009918558, 1.482358050883964840E-15, 0.000000000000000000 ) ) ;
#35595=DIRECTION ( 'NONE',  ( -1.000000000000000000, -1.224606353822377258E-16, -0.000000000000000000 ) ) ;
#35630=EDGE_CURVE ( 'NONE', #2025, #16424, #59505, .T. ) ;
#35631=ORIENTED_EDGE ( 'NONE', *, *, #91993, .F. ) ;
#35649=DIRECTION ( 'NONE',  ( -1.000000000000000000, -1.224606353822377258E-16, -0.000000000000000000 ) ) ;
#35650=DIRECTION ( 'NONE',  ( 0.000000000000000000, 0.000000000000000000, 1.000000000000000000 ) ) ;
#35656=CIRCLE ( 'NONE', #66643, 5.000000000000001776 ) ;
#35663=CARTESIAN_POINT ( 'NONE',  ( 32.62207953394533178, 5.000000000000003553, 0.000000000000000000 ) ) ;
#35673=CIRCLE ( 'NONE', #14903, 5.000000000000002665 ) ;
#35687=DIRECTION ( 'NONE',  ( -1.000000000000000000, -1.224606353822377258E-16, -0.000000000000000000 ) ) ;
#35689=EDGE_LOOP ( 'NONE', ( #47554, #69333, #75486, #70395, #95452, #51971 ) ) ;
#35774=AXIS2_PLACEMENT_3D ( 'NONE', #33920, #2974, #4584 ) ;
#35790=ORIENTED_EDGE ( 'NONE', *, *, #52053, .T. ) ;
#35828=CIRCLE ( 'NONE', #61605, 8.000000000000000000 ) ;
#35868=VERTEX_POINT ( 'NONE', #99817 ) ;
#35936=EDGE_CURVE ( 'NONE', #96494, #2234, #74468, .T. ) ;
#35945=DIRECTION ( 'NONE',  ( -1.000000000000000000, -0.000000000000000000, -0.000000000000000000 ) ) ;
#35962=ORIENTED_EDGE ( 'NONE', *, *, #78940, .F. ) ;
#36003=DIRECTION ( 'NONE',  ( -1.000000000000000000, -0.000000000000000000, -0.000000000000000000 ) ) ;
#36024=CARTESIAN_POINT ( 'NONE',  ( 39.44615384615384812, 1.411358822780289120E-15, 0.000000000000000000 ) ) ;
#36057=EDGE_LOOP ( 'NONE', ( #47104, #27894, #57878, #14585, #81280 ) ) ;
#36061=EDGE_CURVE ( 'NONE', #19012, #23643, #21669, .T. ) ;
#36062=CARTESIAN_POINT ( 'NONE',  ( 24.05868969682389036, 1.340359594676612611E-15, 0.000000000000000000 ) ) ;
#36071=ORIENTED_EDGE ( 'NONE', *, *, #30380, .T. ) ;
#36080=DIRECTION ( 'NONE',  ( -1.000000000000000000, -1.224606353822377258E-16, -0.000000000000000000 ) ) ;
#36101=EDGE_LOOP ( 'NONE', ( #104597, #26850, #40317, #933, #81264 ) ) ;
#36110=AXIS2_PLACEMENT_3D ( 'NONE', #10496, #57978, #82798 ) ;
#36133=ORIENTED_EDGE ( 'NONE', *, *, #87171, .T. ) ;
#36155=ADVANCED_FACE ( 'NONE', ( #67470 ), #92302, .T. ) ;
#36165=CIRCLE ( 'NONE', #32757, 5.000000000000002665 ) ;
#36222=DIRECTION ( 'NONE',  ( 0.000000000000000000, -1.000000000000000000, 0.000000000000000000 ) ) ;
#36242=DIRECTION ( 'NONE',  ( 0.5735764363510470476, -0.8191520442889911324, 1.003171929053524007E-16 ) ) ;
#36261=ORIENTED_EDGE ( 'NONE', *, *, #8110, .F. ) ;
#36274=CIRCLE ( 'NONE', #56909, 5.000000000000001776 ) ;
#36280=DIRECTION ( 'NONE',  ( -1.000000000000000000, -1.224606353822377258E-16, -0.000000000000000000 ) ) ;
#36284=CARTESIAN_POINT ( 'NONE',  ( 40.92692307692308162, -4.171999999999999709, 0.000000000000000000 ) ) ;
#36290=ORIENTED_EDGE ( 'NONE', *, *, #103347, .T. ) ;
#36304=APPLICATION_CONTEXT ( 'automotive_design' ) ;
#36306=DIRECTION ( 'NONE',  ( -1.000000000000000000, -1.224606353822377258E-16, -0.000000000000000000 ) ) ;
#36370=DIRECTION ( 'NONE',  ( 0.000000000000000000, -1.000000000000000000, 0.000000000000000000 ) ) ;
#36403=CARTESIAN_POINT ( 'NONE',  ( 0.000000000000000000, 0.000000000000000000, 0.000000000000000000 ) ) ;
#36405=ORIENTED_EDGE ( 'NONE', *, *, #55096, .F. ) ;
#36409=CARTESIAN_POINT ( 'NONE',  ( 28.50099738913158376, 5.000000000000004441, 6.123233995736770227E-16 ) ) ;
#36417=EDGE_LOOP ( 'NONE', ( #23194, #18955, #78875, #87151, #18867 ) ) ;
#36491=DIRECTION ( 'NONE',  ( 0.000000000000000000, -1.000000000000000000, 0.000000000000000000 ) ) ;
#36547=CARTESIAN_POINT ( 'NONE',  ( 39.44615384615384812, 1.411358822780289120E-15, 0.000000000000000000 ) ) ;
#36551=EDGE_CURVE ( 'NONE', #45751, #98120, #106072, .T. ) ;
#36580=ORIENTED_EDGE ( 'NONE', *, *, #60700, .F. ) ;
#36585=ORIENTED_EDGE ( 'NONE', *, *, #82608, .T. ) ;
#36592=DIRECTION ( 'NONE',  ( 0.000000000000000000, -1.000000000000000000, 0.000000000000000000 ) ) ;
#36620=DIRECTION ( 'NONE',  ( -1.000000000000000000, -1.224606353822377258E-16, -0.000000000000000000 ) ) ;
#36635=ADVANCED_FACE ( 'NONE', ( #57889 ), #69983, .T. ) ;
#36693=CARTESIAN_POINT ( 'NONE',  ( 45.94900261086841198, 1.482358050883964840E-15, 0.000000000000000000 ) ) ;
#36697=CARTESIAN_POINT ( 'NONE',  ( 22.25669491856071858, 1.482358050883964840E-15, 0.000000000000000000 ) ) ;
#36720=VERTEX_POINT ( 'NONE', #51926 ) ;
#36732=VERTEX_POINT ( 'NONE', #10923 ) ;
#36760=FACE_OUTER_BOUND ( 'NONE', #20067, .T. ) ;
#36763=DIRECTION ( 'NONE',  ( -1.000000000000000000, -1.224606353822377258E-16, -0.000000000000000000 ) ) ;
#36764=DIRECTION ( 'NONE',  ( 0.000000000000000000, -1.000000000000000000, 0.000000000000000000 ) ) ;
#36820=DIRECTION ( 'NONE',  ( 0.000000000000000000, 0.000000000000000000, 1.000000000000000000 ) ) ;
#36831=EDGE_CURVE ( 'NONE', #27928, #58498, #85558, .T. ) ;
#36855=DIRECTION ( 'NONE',  ( 0.5735764363510468256, 0.8191520442889913545, 0.000000000000000000 ) ) ;
#36869=DIRECTION ( 'NONE',  ( -1.000000000000000000, -1.224606353822377258E-16, -0.000000000000000000 ) ) ;
#36894=EDGE_CURVE ( 'NONE', #72287, #70974, #13144, .T. ) ;
#36902=CARTESIAN_POINT ( 'NONE',  ( 0.000000000000000000, 0.000000000000000000, 0.000000000000000000 ) ) ;
#36911=EDGE_CURVE ( 'NONE', #86664, #94186, #14114, .T. ) ;
#36924=EDGE_LOOP ( 'NONE', ( #100427, #36133, #29038, #100674, #59823 ) ) ;
#36949=VERTEX_POINT ( 'NONE', #95073 ) ;
#36984=CARTESIAN_POINT ( 'NONE',  ( 45.36923076923077502, -4.171999999999999709, 0.000000000000000000 ) ) ;
#36996=DIRECTION ( 'NONE',  ( 1.000000000000000000, 1.224606353822377258E-16, 0.000000000000000000 ) ) ;
#37009=DIRECTION ( 'NONE',  ( -1.000000000000000000, -0.000000000000000000, -0.000000000000000000 ) ) ;
#37011=CARTESIAN_POINT ( 'NONE',  ( 0.4969600502617528281, -8.860760056385748484, -0.6527133886630291926 ) ) ;
#37062=DIRECTION ( 'NONE',  ( -1.000000000000000000, -1.224606353822377258E-16, -0.000000000000000000 ) ) ;
#37070=CARTESIAN_POINT ( 'NONE',  ( 41.82792046605465686, 1.340359594676612611E-15, 0.000000000000000000 ) ) ;
#37072=EDGE_CURVE ( 'NONE', #39953, #25507, #61458, .T. ) ;
#37099=CARTESIAN_POINT ( 'NONE',  ( 32.62207953394533178, 5.000000000000002665, 0.000000000000000000 ) ) ;
#37137=AXIS2_PLACEMENT_3D ( 'NONE', #103977, #14422, #38221 ) ;
#37182=ORIENTED_EDGE ( 'NONE', *, *, #4236, .F. ) ;
#37194=ORIENTED_EDGE ( 'NONE', *, *, #33108, .F. ) ;
#37205=AXIS2_PLACEMENT_3D ( 'NONE', #24824, #57677, #66319 ) ;
#37240=CARTESIAN_POINT ( 'NONE',  ( 0.000000000000000000, 0.000000000000000000, 5.000000000000002665 ) ) ;
#37251=ORIENTED_EDGE ( 'NONE', *, *, #64545, .F. ) ;
#37274=CARTESIAN_POINT ( 'NONE',  ( 31.14131030317610538, 5.000000000000002665, 0.000000000000000000 ) ) ;
#37288=CONICAL_SURFACE ( 'NONE', #95776, 4.172000000000001485, 0.9599310885968750373 ) ;
#37291=ORIENTED_EDGE ( 'NONE', *, *, #47870, .F. ) ;
#37294=CYLINDRICAL_SURFACE ( 'NONE', #103046, 5.000000000000002665 ) ;
#37336=CARTESIAN_POINT ( 'NONE',  ( 32.94330508143927716, 1.340359594676612611E-15, 0.000000000000000000 ) ) ;
#37353=CIRCLE ( 'NONE', #16671, 5.000000000000002665 ) ;
#37359=DIRECTION ( 'NONE',  ( 0.000000000000000000, -1.000000000000000000, 0.000000000000000000 ) ) ;
#37442=ORIENTED_EDGE ( 'NONE', *, *, #79650, .F. ) ;
#37450=AXIS2_PLACEMENT_3D ( 'NONE', #38804, #30186, #79776 ) ;
#37520=DIRECTION ( 'NONE',  ( -0.5735764363510512664, 0.8191520442889881348, 1.003171929053520309E-16 ) ) ;
#37534=AXIS2_PLACEMENT_3D ( 'NONE', #12636, #38032, #45570 ) ;
#37579=CIRCLE ( 'NONE', #6551, 4.172000000000001485 ) ;
#37586=EDGE_CURVE ( 'NONE', #72256, #89827, #78606, .T. ) ;
#37609=AXIS2_PLACEMENT_3D ( 'NONE', #16657, #42521, #91624 ) ;
#37651=DIRECTION ( 'NONE',  ( -1.000000000000000000, -1.224606353822377258E-16, -0.000000000000000000 ) ) ;
#37663=ORIENTED_EDGE ( 'NONE', *, *, #96954, .F. ) ;
#37664=ORIENTED_EDGE ( 'NONE', *, *, #3776, .F. ) ;
#37698=CARTESIAN_POINT ( 'NONE',  ( 0.1317522424472098164, 1.959574484719855292, 7.999999999999998224 ) ) ;
#37762=CARTESIAN_POINT ( 'NONE',  ( 38.54515645702225868, 5.000000000000002665, 0.000000000000000000 ) ) ;
#37772=DIRECTION ( 'NONE',  ( -1.000000000000000000, -0.000000000000000000, -0.000000000000000000 ) ) ;
#37781=DIRECTION ( 'NONE',  ( 0.5735764363510468256, 0.8191520442889913545, 0.000000000000000000 ) ) ;
#37791=ORIENTED_EDGE ( 'NONE', *, *, #92950, .F. ) ;
#37808=ORIENTED_EDGE ( 'NONE', *, *, #78575, .F. ) ;
#37859=AXIS2_PLACEMENT_3D ( 'NONE', #3888, #79353, #36820 ) ;
#37868=DIRECTION ( 'NONE',  ( 0.000000000000000000, -1.000000000000000000, 0.000000000000000000 ) ) ;
#37888=CARTESIAN_POINT ( 'NONE',  ( 24.05868969682389036, 1.340359594676612611E-15, 0.000000000000000000 ) ) ;
#37902=CARTESIAN_POINT ( 'NONE',  ( 6.849999999999999645, 9.797174393178825657E-16, -8.000000000000000000 ) ) ;
#37909=ORIENTED_EDGE ( 'NONE', *, *, #62711, .F. ) ;
#37929=ADVANCED_FACE ( 'NONE', ( #61684 ), #42635, .T. ) ;
#37958=ORIENTED_EDGE ( 'NONE', *, *, #6227, .T. ) ;
#37965=CARTESIAN_POINT ( 'NONE',  ( 32.94330508143927716, 4.999999999999994671, 6.123233995736758394E-16 ) ) ;
#37967=CARTESIAN_POINT ( 'NONE',  ( 8.929771841637641927, 1.482358050883964840E-15, 0.000000000000000000 ) ) ;
#37971=DIRECTION ( 'NONE',  ( -1.000000000000000000, -1.224606353822377258E-16, -0.000000000000000000 ) ) ;
#37991=VERTEX_POINT ( 'NONE', #27742 ) ;
#37997=DIRECTION ( 'NONE',  ( 0.000000000000000000, -1.000000000000000000, 0.000000000000000000 ) ) ;
#38032=DIRECTION ( 'NONE',  ( -1.000000000000000000, -1.224606353822377258E-16, -0.000000000000000000 ) ) ;
#38051=CIRCLE ( 'NONE', #51775, 5.000000000000002665 ) ;
#38087=ORIENTED_EDGE ( 'NONE', *, *, #49370, .F. ) ;
#38103=ADVANCED_FACE ( 'NONE', ( #16274 ), #65044, .T. ) ;
#38113=DIRECTION ( 'NONE',  ( -1.000000000000000000, -0.000000000000000000, -0.000000000000000000 ) ) ;
#38120=FACE_OUTER_BOUND ( 'NONE', #23324, .T. ) ;
#38130=EDGE_CURVE ( 'NONE', #85882, #83030, #105814, .T. ) ;
#38211=ORIENTED_EDGE ( 'NONE', *, *, #8544, .T. ) ;
#38221=DIRECTION ( 'NONE',  ( 0.000000000000000000, -1.000000000000000000, 0.000000000000000000 ) ) ;
#38228=ORIENTED_EDGE ( 'NONE', *, *, #13122, .F. ) ;
#38237=AXIS2_PLACEMENT_3D ( 'NONE', #94213, #10615, #69415 ) ;
#38247=FACE_BOUND ( 'NONE', #82341, .T. ) ;
#38299=CARTESIAN_POINT ( 'NONE',  ( 35.90484354297773706, 6.123233995736770227E-16, -5.000000000000002665 ) ) ;
#38334=DIRECTION ( 'NONE',  ( 0.000000000000000000, 1.000000000000000000, 0.000000000000000000 ) ) ;
#38370=FACE_OUTER_BOUND ( 'NONE', #77844, .T. ) ;
#38405=VECTOR ( 'NONE', #26212, 1000.000000000000000 ) ;
#38421=DIRECTION ( 'NONE',  ( 0.000000000000000000, 0.000000000000000000, -1.000000000000000000 ) ) ;
#38484=VECTOR ( 'NONE', #25808, 999.9999999999998863 ) ;
#38499=DIRECTION ( 'NONE',  ( 0.000000000000000000, 0.000000000000000000, -1.000000000000000000 ) ) ;
#38527=PRODUCT_CONTEXT ( 'NONE', #36304, 'mechanical' ) ;
#38554=DIRECTION ( 'NONE',  ( 0.000000000000000000, -1.000000000000000000, 0.000000000000000000 ) ) ;
#38566=CARTESIAN_POINT ( 'NONE',  ( 43.88846153846154152, 1.411358822780289120E-15, 0.000000000000000000 ) ) ;
#38678=EDGE_CURVE ( 'NONE', #33126, #4002, #13376, .T. ) ;
#38695=CONICAL_SURFACE ( 'NONE', #11103, 5.000000000000001776, 0.9599310885968803664 ) ;
#38713=DIRECTION ( 'NONE',  ( 0.000000000000000000, 0.000000000000000000, 1.000000000000000000 ) ) ;
#38721=ORIENTED_EDGE ( 'NONE', *, *, #39569, .F. ) ;
#38723=EDGE_CURVE ( 'NONE', #44784, #79740, #45657, .T. ) ;
#38751=DIRECTION ( 'NONE',  ( -1.000000000000000000, -1.224606353822377258E-16, -0.000000000000000000 ) ) ;
#38758=LINE ( 'NONE', #12857, #16816 ) ;
#38759=CARTESIAN_POINT ( 'NONE',  ( 6.249999999999998224, 0.000000000000000000, 8.000000000000000000 ) ) ;
#38779=CONICAL_SURFACE ( 'NONE', #16350, 4.172000000000001485, 0.9599310885968750373 ) ;
#38795=CARTESIAN_POINT ( 'NONE',  ( 0.000000000000000000, 9.797174393178825657E-16, -8.000000000000000000 ) ) ;
#38801=ORIENTED_EDGE ( 'NONE', *, *, #96255, .F. ) ;
#38804=CARTESIAN_POINT ( 'NONE',  ( 23.15769230769230802, 1.411358822780289120E-15, 0.000000000000000000 ) ) ;
#38816=ORIENTED_EDGE ( 'NONE', *, *, #64195, .T. ) ;
#38894=AXIS2_PLACEMENT_3D ( 'NONE', #62740, #45504, #3966 ) ;
#38909=EDGE_LOOP ( 'NONE', ( #101966, #34232, #94801, #627, #83231 ) ) ;
#38912=CARTESIAN_POINT ( 'NONE',  ( 0.3167204509598363082, 5.377136764700156668, 6.686525924292793022 ) ) ;
#38935=FACE_OUTER_BOUND ( 'NONE', #88724, .T. ) ;
#38961=ORIENTED_EDGE ( 'NONE', *, *, #47647, .F. ) ;
#39010=CARTESIAN_POINT ( 'NONE',  ( 0.000000000000000000, 0.000000000000000000, 5.000000000000002665 ) ) ;
#39021=EDGE_CURVE ( 'NONE', #58994, #52182, #23898, .T. ) ;
#39042=CIRCLE ( 'NONE', #71733, 5.000000000000002665 ) ;
#39055=CARTESIAN_POINT ( 'NONE',  ( 35.90484354297773706, 1.340359594676612611E-15, 0.000000000000000000 ) ) ;
#39056=AXIS2_PLACEMENT_3D ( 'NONE', #87239, #72100, #105007 ) ;
#39062=FACE_OUTER_BOUND ( 'NONE', #48657, .T. ) ;
#39070=CARTESIAN_POINT ( 'NONE',  ( 0.1306530452038068557, -5.952467836904147269, 5.690023276062396107 ) ) ;
#39084=EDGE_CURVE ( 'NONE', #57394, #1686, #89162, .T. ) ;
#39100=CONICAL_SURFACE ( 'NONE', #68354, 4.172000000000001485, 0.9599310885968750373 ) ;
#39104=ORIENTED_EDGE ( 'NONE', *, *, #51335, .T. ) ;
#39106=DIRECTION ( 'NONE',  ( -1.000000000000000000, -1.224606353822377258E-16, -0.000000000000000000 ) ) ;
#39111=EDGE_CURVE ( 'NONE', #33159, #30622, #30741, .T. ) ;
#39151=DIRECTION ( 'NONE',  ( -1.000000000000000000, -0.000000000000000000, -0.000000000000000000 ) ) ;
#39155=ORIENTED_EDGE ( 'NONE', *, *, #89521, .T. ) ;
#39164=AXIS2_PLACEMENT_3D ( 'NONE', #21509, #13898, #88874 ) ;
#39189=AXIS2_PLACEMENT_3D ( 'NONE', #48728, #81619, #72490 ) ;
#39216=DIRECTION ( 'NONE',  ( 0.000000000000000000, 1.000000000000000000, 0.000000000000000000 ) ) ;
#39222=CYLINDRICAL_SURFACE ( 'NONE', #55031, 8.000000000000000000 ) ;
#39266=CARTESIAN_POINT ( 'NONE',  ( 0.000000000000000000, 0.000000000000000000, 8.000000000000000000 ) ) ;
#39269=VERTEX_POINT ( 'NONE', #51872 ) ;
#39289=ADVANCED_FACE ( 'NONE', ( #50799 ), #61055, .T. ) ;
#39290=DIRECTION ( 'NONE',  ( -1.000000000000000000, -1.224606353822377258E-16, -0.000000000000000000 ) ) ;
#39314=AXIS2_PLACEMENT_3D ( 'NONE', #88008, #70756, #96096 ) ;
#39342=CIRCLE ( 'NONE', #77216, 5.000000000000002665 ) ;
#39350=DIRECTION ( 'NONE',  ( -1.000000000000000000, -0.000000000000000000, -0.000000000000000000 ) ) ;
#39377=CONICAL_SURFACE ( 'NONE', #13553, 5.000000000000001776, 0.9599310885968803664 ) ;
#39428=EDGE_CURVE ( 'NONE', #70645, #28989, #54794, .T. ) ;
#39443=EDGE_CURVE ( 'NONE', #8540, #87039, #34209, .T. ) ;
#39489=DIRECTION ( 'NONE',  ( 0.000000000000000000, -1.000000000000000000, 0.000000000000000000 ) ) ;
#39494=ORIENTED_EDGE ( 'NONE', *, *, #24625, .F. ) ;
#39541=DIRECTION ( 'NONE',  ( 1.000000000000000000, 1.224606353822377258E-16, 0.000000000000000000 ) ) ;
#39551=DIRECTION ( 'NONE',  ( -1.000000000000000000, -0.000000000000000000, -0.000000000000000000 ) ) ;
#39569=EDGE_CURVE ( 'NONE', #48676, #40649, #498, .T. ) ;
#39584=ADVANCED_FACE ( 'NONE', ( #57697 ), #83062, .T. ) ;
#39589=VERTEX_POINT ( 'NONE', #80927 ) ;
#39646=DIRECTION ( 'NONE',  ( 0.000000000000000000, -1.000000000000000000, 0.000000000000000000 ) ) ;
#39668=VERTEX_POINT ( 'NONE', #4146 ) ;
#39671=VERTEX_POINT ( 'NONE', #69942 ) ;
#39682=DIRECTION ( 'NONE',  ( -1.000000000000000000, -0.000000000000000000, -0.000000000000000000 ) ) ;
#39690=ORIENTED_EDGE ( 'NONE', *, *, #11672, .T. ) ;
#39776=CIRCLE ( 'NONE', #87973, 5.000000000000002665 ) ;
#39793=ORIENTED_EDGE ( 'NONE', *, *, #106607, .T. ) ;
#39796=DIRECTION ( 'NONE',  ( -1.000000000000000000, -1.224606353822377258E-16, -0.000000000000000000 ) ) ;
#39804=DIRECTION ( 'NONE',  ( -1.000000000000000000, -1.224606353822377258E-16, -0.000000000000000000 ) ) ;
#39806=DIRECTION ( 'NONE',  ( -1.000000000000000000, -0.000000000000000000, -0.000000000000000000 ) ) ;
#39819=LINE ( 'NONE', #22054, #1048 ) ;
#39842=CARTESIAN_POINT ( 'NONE',  ( 37.96538461538461462, 1.411358822780289120E-15, 0.000000000000000000 ) ) ;
#39851=CARTESIAN_POINT ( 'NONE',  ( 32.04230769230768772, -4.171999999999999709, 0.000000000000000000 ) ) ;
#39856=CARTESIAN_POINT ( 'NONE',  ( 0.1306530452038086043, 5.952467836904148157, -5.690023276062398772 ) ) ;
#39860=AXIS2_PLACEMENT_3D ( 'NONE', #94399, #61504, #96906 ) ;
#39911=ORIENTED_EDGE ( 'NONE', *, *, #13163, .T. ) ;
#39924=DIRECTION ( 'NONE',  ( 0.000000000000000000, -1.000000000000000000, 0.000000000000000000 ) ) ;
#39953=VERTEX_POINT ( 'NONE', #35497 ) ;
#39966=DIRECTION ( 'NONE',  ( -1.000000000000000000, -1.224606353822377258E-16, -0.000000000000000000 ) ) ;
#39999=DIRECTION ( 'NONE',  ( -1.000000000000000000, -1.224606353822377258E-16, -0.000000000000000000 ) ) ;
#40022=ORIENTED_EDGE ( 'NONE', *, *, #51003, .F. ) ;
#40047=DIRECTION ( 'NONE',  ( 0.000000000000000000, 1.000000000000000000, 0.000000000000000000 ) ) ;
#40050=CARTESIAN_POINT ( 'NONE',  ( 0.06809871960542614178, -7.710219529346607814, 2.645508037661882472 ) ) ;
#40066=CARTESIAN_POINT ( 'NONE',  ( 46.85000000000000142, 0.000000000000000000, 0.000000000000000000 ) ) ;
#40133=DIRECTION ( 'NONE',  ( -1.000000000000000000, -1.224606353822377258E-16, -0.000000000000000000 ) ) ;
#40157=CARTESIAN_POINT ( 'NONE',  ( 0.000000000000000000, 6.928203230275506108, 4.000000000000007105 ) ) ;
#40171=ORIENTED_EDGE ( 'NONE', *, *, #75007, .T. ) ;
#40218=CIRCLE ( 'NONE', #100500, 4.172000000000001485 ) ;
#40226=AXIS2_PLACEMENT_3D ( 'NONE', #17562, #66089, #42345 ) ;
#40228=DIRECTION ( 'NONE',  ( 0.000000000000000000, 1.000000000000000000, 0.000000000000000000 ) ) ;
#40295=DIRECTION ( 'NONE',  ( -1.000000000000000000, -1.224606353822377258E-16, -0.000000000000000000 ) ) ;
#40317=ORIENTED_EDGE ( 'NONE', *, *, #5278, .T. ) ;
#40339=EDGE_CURVE ( 'NONE', #36732, #88469, #104706, .T. ) ;
#40345=FACE_OUTER_BOUND ( 'NONE', #52076, .T. ) ;
#40383=FACE_OUTER_BOUND ( 'NONE', #106508, .T. ) ;
#40399=CARTESIAN_POINT ( 'NONE',  ( 37.38561277374697056, 5.000000000000004441, 6.123233995736770227E-16 ) ) ;
#40409=CIRCLE ( 'NONE', #92075, 4.172000000000001485 ) ;
#40415=EDGE_CURVE ( 'NONE', #79740, #49120, #104948, .T. ) ;
#40431=ORIENTED_EDGE ( 'NONE', *, *, #74666, .F. ) ;
#40466=ORIENTED_EDGE ( 'NONE', *, *, #74666, .T. ) ;
#40470=ORIENTED_EDGE ( 'NONE', *, *, #12855, .T. ) ;
#40505=EDGE_LOOP ( 'NONE', ( #99461, #78337, #10472, #77205, #83021, #755 ) ) ;
#40512=LINE ( 'NONE', #55607, #1877 ) ;
#40518=ORIENTED_EDGE ( 'NONE', *, *, #62201, .T. ) ;
#40524=EDGE_CURVE ( 'NONE', #33126, #33037, #98720, .T. ) ;
#40552=CARTESIAN_POINT ( 'NONE',  ( 0.000000000000000000, 0.000000000000000000, 5.000000000000002665 ) ) ;
#40567=ORIENTED_EDGE ( 'NONE', *, *, #34703, .T. ) ;
#40592=FACE_OUTER_BOUND ( 'NONE', #38909, .T. ) ;
#40610=DIRECTION ( 'NONE',  ( 0.000000000000000000, 0.000000000000000000, 1.000000000000000000 ) ) ;
#40619=VECTOR ( 'NONE', #31895, 1000.000000000000227 ) ;
#40626=DIRECTION ( 'NONE',  ( -1.000000000000000000, -1.224606353822377258E-16, -0.000000000000000000 ) ) ;
#40633=EDGE_CURVE ( 'NONE', #33590, #42859, #68769, .T. ) ;
#40649=VERTEX_POINT ( 'NONE', #51229 ) ;
#40685=EDGE_LOOP ( 'NONE', ( #4965, #72789, #40171, #37664, #95233 ) ) ;
#40688=DIRECTION ( 'NONE',  ( -1.000000000000000000, -1.224606353822377258E-16, -0.000000000000000000 ) ) ;
#40724=CIRCLE ( 'NONE', #70059, 5.000000000000001776 ) ;
#40778=AXIS2_PLACEMENT_3D ( 'NONE', #4585, #103281, #13182 ) ;
#40797=ORIENTED_EDGE ( 'NONE', *, *, #99863, .F. ) ;
#40832=CIRCLE ( 'NONE', #94272, 5.000000000000001776 ) ;
#40839=CARTESIAN_POINT ( 'NONE',  ( 0.3194001229792609031, 3.115132258397515397, -7.999999999999996447 ) ) ;
#40842=ORIENTED_EDGE ( 'NONE', *, *, #81339, .T. ) ;
#40848=DIRECTION ( 'NONE',  ( 1.000000000000000000, 0.000000000000000000, -0.000000000000000000 ) ) ;
#40851=AXIS2_PLACEMENT_3D ( 'NONE', #68087, #36306, #17958 ) ;
#40881=CARTESIAN_POINT ( 'NONE',  ( 0.000000000000000000, 0.000000000000000000, 0.000000000000000000 ) ) ;
#40883=VECTOR ( 'NONE', #39551, 1000.000000000000000 ) ;
#40894=CONICAL_SURFACE ( 'NONE', #106310, 5.000000000000001776, 0.9599310885968803664 ) ;
#40902=AXIS2_PLACEMENT_3D ( 'NONE', #84198, #35687, #36222 ) ;
#40928=EDGE_LOOP ( 'NONE', ( #42277, #94814, #64362, #9100, #106709, #104763 ) ) ;
#40932=CARTESIAN_POINT ( 'NONE',  ( 0.000000000000000000, 6.123233995736770227E-16, -5.000000000000002665 ) ) ;
#40938=DIRECTION ( 'NONE',  ( 0.000000000000000000, -0.4999999999999998890, 0.8660254037844385966 ) ) ;
#40946=ORIENTED_EDGE ( 'NONE', *, *, #49370, .T. ) ;
#40956=LINE ( 'NONE', #33962, #25051 ) ;
#41014=CARTESIAN_POINT ( 'NONE',  ( 43.30868969682389036, 1.340359594676612611E-15, 0.000000000000000000 ) ) ;
#41086=DIRECTION ( 'NONE',  ( 0.000000000000000000, 1.000000000000000000, 0.000000000000000000 ) ) ;
#41088=EDGE_CURVE ( 'NONE', #95530, #84621, #94478, .T. ) ;
#41133=EDGE_CURVE ( 'NONE', #67995, #103302, #25584, .T. ) ;
#41165=ORIENTED_EDGE ( 'NONE', *, *, #13122, .T. ) ;
#41203=DIRECTION ( 'NONE',  ( -1.000000000000000000, -0.000000000000000000, -0.000000000000000000 ) ) ;
#41205=CARTESIAN_POINT ( 'NONE',  ( 32.94330508143927716, 0.000000000000000000, 5.000000000000002665 ) ) ;
#41211=ADVANCED_FACE ( 'NONE', ( #89226 ), #51394, .T. ) ;
#41214=ORIENTED_EDGE ( 'NONE', *, *, #516, .T. ) ;
#41287=VECTOR ( 'NONE', #50814, 1000.000000000000000 ) ;
#41313=CONICAL_SURFACE ( 'NONE', #101624, 4.172000000000001485, 0.9599310885968750373 ) ;
#41315=CARTESIAN_POINT ( 'NONE',  ( 10.41054107240687188, 6.123233995736772199E-16, -5.000000000000001776 ) ) ;
#41363=CARTESIAN_POINT ( 'NONE',  ( 37.38561277374697056, 1.340359594676612611E-15, 0.000000000000000000 ) ) ;
#41452=ORIENTED_EDGE ( 'NONE', *, *, #3109, .T. ) ;
#41458=EDGE_CURVE ( 'NONE', #73449, #29452, #103157, .T. ) ;
#41461=CARTESIAN_POINT ( 'NONE',  ( -9.232659125071873696E-16, -6.534749472788166536, -4.681481898396976149 ) ) ;
#41487=DIRECTION ( 'NONE',  ( -1.000000000000000000, -1.224606353822377258E-16, -0.000000000000000000 ) ) ;
#41512=AXIS2_PLACEMENT_3D ( 'NONE', #64484, #6760, #23507 ) ;
#41516=DIRECTION ( 'NONE',  ( 0.000000000000000000, 0.000000000000000000, 1.000000000000000000 ) ) ;
#41518=CIRCLE ( 'NONE', #67406, 5.000000000000002665 ) ;
#41532=ORIENTED_EDGE ( 'NONE', *, *, #5946, .T. ) ;
#41540=SURFACE_STYLE_USAGE ( .BOTH. , #58255 ) ;
#41566=LINE ( 'NONE', #33492, #96213 ) ;
#41591=DIRECTION ( 'NONE',  ( -1.000000000000000000, -1.224606353822377258E-16, -0.000000000000000000 ) ) ;
#41600=CONICAL_SURFACE ( 'NONE', #53695, 4.172000000000001485, 0.9599310885968750373 ) ;
#41603=VERTEX_POINT ( 'NONE', #35415 ) ;
#41611=ORIENTED_EDGE ( 'NONE', *, *, #36061, .T. ) ;
#41627=AXIS2_PLACEMENT_3D ( 'NONE', #48606, #90146, #39489 ) ;
#41688=ORIENTED_EDGE ( 'NONE', *, *, #8544, .F. ) ;
#41743=EDGE_CURVE ( 'NONE', #70219, #26294, #43887, .T. ) ;
#41756=DIRECTION ( 'NONE',  ( -1.000000000000000000, -1.224606353822377258E-16, -0.000000000000000000 ) ) ;
#41769=EDGE_LOOP ( 'NONE', ( #29890, #59382, #73331, #36585, #24393 ) ) ;
#41783=VERTEX_POINT ( 'NONE', #76893 ) ;
#41786=CARTESIAN_POINT ( 'NONE',  ( 17.23461538461538467, 1.411358822780289120E-15, 0.000000000000000000 ) ) ;
#41803=VECTOR ( 'NONE', #15599, 999.9999999999998863 ) ;
#41858=CARTESIAN_POINT ( 'NONE',  ( 22.25669491856071858, 1.482358050883964840E-15, 0.000000000000000000 ) ) ;
#41861=DIRECTION ( 'NONE',  ( -1.000000000000000000, -1.224606353822377258E-16, -0.000000000000000000 ) ) ;
#41869=ORIENTED_EDGE ( 'NONE', *, *, #87460, .F. ) ;
#41893=CARTESIAN_POINT ( 'NONE',  ( 12.21253585067004543, 5.000000000000004441, 6.123233995736770227E-16 ) ) ;
#41944=DIRECTION ( 'NONE',  ( 0.000000000000000000, -1.000000000000000000, 0.000000000000000000 ) ) ;
#41950=DIRECTION ( 'NONE',  ( -0.5735764363510512664, 0.8191520442889881348, 1.003171929053520309E-16 ) ) ;
#41954=DIRECTION ( 'NONE',  ( 1.000000000000000000, 1.224606353822377258E-16, 0.000000000000000000 ) ) ;
#41959=ORIENTED_EDGE ( 'NONE', *, *, #76773, .F. ) ;
#41992=AXIS2_PLACEMENT_3D ( 'NONE', #9800, #91809, #43779 ) ;
#42013=CARTESIAN_POINT ( 'NONE',  ( 9.250997389131581983, 0.000000000000000000, 5.000000000000002665 ) ) ;
#42028=VERTEX_POINT ( 'NONE', #17492 ) ;
#42063=CIRCLE ( 'NONE', #14475, 5.000000000000001776 ) ;
#42088=EDGE_LOOP ( 'NONE', ( #101201, #21306, #44538, #28417, #82383 ) ) ;
#42092=EDGE_CURVE ( 'NONE', #35042, #42028, #96101, .T. ) ;
#42100=DIRECTION ( 'NONE',  ( 0.000000000000000000, -1.000000000000000000, 0.000000000000000000 ) ) ;
#42106=ORIENTED_EDGE ( 'NONE', *, *, #89195, .F. ) ;
#42109=ORIENTED_EDGE ( 'NONE', *, *, #76115, .T. ) ;
#42113=ORIENTED_EDGE ( 'NONE', *, *, #84282, .F. ) ;
#42116=DIRECTION ( 'NONE',  ( 0.000000000000000000, -1.000000000000000000, 0.000000000000000000 ) ) ;
#42154=ORIENTED_EDGE ( 'NONE', *, *, #26967, .T. ) ;
#42207=CARTESIAN_POINT ( 'NONE',  ( 6.849999999999999645, 4.618802153517004960, 7.999999999999998224 ) ) ;
#42225=CARTESIAN_POINT ( 'NONE',  ( 23.15769230769230802, 1.411358822780289120E-15, 0.000000000000000000 ) ) ;
#42240=AXIS2_PLACEMENT_3D ( 'NONE', #106090, #90458, #33307 ) ;
#42244=CARTESIAN_POINT ( 'NONE',  ( 8.349999999999999645, 1.411358822780289120E-15, 0.000000000000000000 ) ) ;
#42277=ORIENTED_EDGE ( 'NONE', *, *, #19505, .T. ) ;
#42278=ADVANCED_FACE ( 'NONE', ( #30909 ), #51271, .T. ) ;
#42281=ORIENTED_EDGE ( 'NONE', *, *, #13425, .T. ) ;
#42345=DIRECTION ( 'NONE',  ( 0.000000000000000000, -1.000000000000000000, 0.000000000000000000 ) ) ;
#42361=EDGE_CURVE ( 'NONE', #5164, #70645, #58886, .T. ) ;
#42365=CARTESIAN_POINT ( 'NONE',  ( 6.849999999999999645, -9.237604307034018802, 3.355146209984123968E-17 ) ) ;
#42393=CARTESIAN_POINT ( 'NONE',  ( 6.249999999999998224, -9.237604307034018802, 0.000000000000000000 ) ) ;
#42453=FACE_OUTER_BOUND ( 'NONE', #26672, .T. ) ;
#42455=ORIENTED_EDGE ( 'NONE', *, *, #97354, .T. ) ;
#42460=CARTESIAN_POINT ( 'NONE',  ( 32.94330508143927716, 1.340359594676612611E-15, 0.000000000000000000 ) ) ;
#42472=EDGE_CURVE ( 'NONE', #61957, #85320, #4869, .T. ) ;
#42475=CARTESIAN_POINT ( 'NONE',  ( 27.02022815836235026, 1.340359594676612611E-15, 0.000000000000000000 ) ) ;
#42499=CARTESIAN_POINT ( 'NONE',  ( 34.10284876471455817, 3.851859888774471706E-31, 5.000000000000001776 ) ) ;
#42513=VERTEX_POINT ( 'NONE', #12954 ) ;
#42521=DIRECTION ( 'NONE',  ( -1.000000000000000000, -1.224606353822377258E-16, -0.000000000000000000 ) ) ;
#42541=DIRECTION ( 'NONE',  ( 0.5735764363510470476, -0.8191520442889911324, 1.003171929053524007E-16 ) ) ;
#42564=CIRCLE ( 'NONE', #2992, 5.000000000000002665 ) ;
#42572=AXIS2_PLACEMENT_3D ( 'NONE', #85511, #69330, #45584 ) ;
#42589=CYLINDRICAL_SURFACE ( 'NONE', #54977, 5.000000000000002665 ) ;
#42601=ADVANCED_FACE ( 'NONE', ( #72265 ), #49654, .T. ) ;
#42603=CARTESIAN_POINT ( 'NONE',  ( 30.56153846153846132, 4.172000000000003261, 0.000000000000000000 ) ) ;
#42613=LINE ( 'NONE', #67442, #45043 ) ;
#42616=CARTESIAN_POINT ( 'NONE',  ( 0.7145311798163198613, -4.618802153516998743, 7.999999999999998224 ) ) ;
#42621=ORIENTED_EDGE ( 'NONE', *, *, #20965, .F. ) ;
#42623=CARTESIAN_POINT ( 'NONE',  ( 24.05868969682389036, 6.123233995736770227E-16, -5.000000000000002665 ) ) ;
#42624=CIRCLE ( 'NONE', #75352, 4.172000000000001485 ) ;
#42635=CONICAL_SURFACE ( 'NONE', #70216, 4.172000000000001485, 0.9599310885968750373 ) ;
#42644=ORIENTED_EDGE ( 'NONE', *, *, #55966, .T. ) ;
#42702=DIRECTION ( 'NONE',  ( -1.000000000000000000, -1.224606353822377258E-16, -0.000000000000000000 ) ) ;
#42710=EDGE_LOOP ( 'NONE', ( #53840, #20880, #34697 ) ) ;
#42718=CARTESIAN_POINT ( 'NONE',  ( 0.000000000000000000, 0.000000000000000000, 0.000000000000000000 ) ) ;
#42719=CIRCLE ( 'NONE', #11742, 5.000000000000001776 ) ;
#42724=VECTOR ( 'NONE', #52665, 1000.000000000000000 ) ;
#42728=DIRECTION ( 'NONE',  ( -0.5735764363510510444, -0.8191520442889883569, 0.000000000000000000 ) ) ;
#42730=EDGE_LOOP ( 'NONE', ( #33639, #47337, #2772, #103749, #59504, #87987 ) ) ;
#42737=DIRECTION ( 'NONE',  ( -1.000000000000000000, -1.224606353822377258E-16, -0.000000000000000000 ) ) ;
#42753=DIRECTION ( 'NONE',  ( -1.000000000000000000, -0.000000000000000000, -0.000000000000000000 ) ) ;
#42760=EDGE_CURVE ( 'NONE', #32993, #85882, #66923, .T. ) ;
#42773=ORIENTED_EDGE ( 'NONE', *, *, #84570, .F. ) ;
#42806=DIRECTION ( 'NONE',  ( -1.000000000000000000, -1.224606353822377258E-16, -0.000000000000000000 ) ) ;
#42826=DIRECTION ( 'NONE',  ( 0.000000000000000000, 0.000000000000000000, 1.000000000000000000 ) ) ;
#42829=ORIENTED_EDGE ( 'NONE', *, *, #43845, .T. ) ;
#42836=DIRECTION ( 'NONE',  ( 0.000000000000000000, -1.000000000000000000, 0.000000000000000000 ) ) ;
#42842=DIRECTION ( 'NONE',  ( 0.000000000000000000, -1.000000000000000000, 0.000000000000000000 ) ) ;
#42848=ORIENTED_EDGE ( 'NONE', *, *, #72420, .F. ) ;
#42852=CARTESIAN_POINT ( 'NONE',  ( 0.000000000000000000, 0.000000000000000000, 5.000000000000002665 ) ) ;
#42859=VERTEX_POINT ( 'NONE', #78504 ) ;
#42861=DIRECTION ( 'NONE',  ( -1.000000000000000000, -1.224606353822377258E-16, -0.000000000000000000 ) ) ;
#42886=ORIENTED_EDGE ( 'NONE', *, *, #102744, .T. ) ;
#42891=DIRECTION ( 'NONE',  ( 0.000000000000000000, 0.000000000000000000, 1.000000000000000000 ) ) ;
#42908=EDGE_CURVE ( 'NONE', #36732, #88025, #8381, .T. ) ;
#42925=VERTEX_POINT ( 'NONE', #7844 ) ;
#42926=CARTESIAN_POINT ( 'NONE',  ( 0.000000000000000000, 0.000000000000000000, 0.000000000000000000 ) ) ;
#42943=CARTESIAN_POINT ( 'NONE',  ( 36.48461538461538822, 1.411358822780289120E-15, 0.000000000000000000 ) ) ;
#42975=CONICAL_SURFACE ( 'NONE', #6776, 4.172000000000001485, 0.9599310885968750373 ) ;
#42992=AXIS2_PLACEMENT_3D ( 'NONE', #88581, #8183, #73437 ) ;
#42993=ADVANCED_FACE ( 'NONE', ( #106542 ), #13549, .T. ) ;
#43008=AXIS2_PLACEMENT_3D ( 'NONE', #63396, #54192, #39646 ) ;
#43025=CARTESIAN_POINT ( 'NONE',  ( 0.3157512944461042803, -3.097794232780332724, -8.000000000000001776 ) ) ;
#43080=ORIENTED_EDGE ( 'NONE', *, *, #28023, .T. ) ;
#43108=DIRECTION ( 'NONE',  ( -1.000000000000000000, -0.000000000000000000, -0.000000000000000000 ) ) ;
#43139=CIRCLE ( 'NONE', #50045, 5.000000000000001776 ) ;
#43143=DIRECTION ( 'NONE',  ( -1.000000000000000000, -1.224606353822377258E-16, -0.000000000000000000 ) ) ;
#43146=AXIS2_PLACEMENT_3D ( 'NONE', #58131, #48959, #25826 ) ;
#43182=EDGE_LOOP ( 'NONE', ( #45733, #65861, #105927, #105840, #57941 ) ) ;
#43184=VERTEX_POINT ( 'NONE', #3496 ) ;
#43261=VERTEX_POINT ( 'NONE', #70355 ) ;
#43274=VECTOR ( 'NONE', #20878, 1000.000000000000000 ) ;
#43284=VERTEX_POINT ( 'NONE', #29913 ) ;
#43301=DIRECTION ( 'NONE',  ( 0.000000000000000000, -1.000000000000000000, 0.000000000000000000 ) ) ;
#43315=CONICAL_SURFACE ( 'NONE', #82895, 5.000000000000001776, 0.9599310885968803664 ) ;
#43383=CARTESIAN_POINT ( 'NONE',  ( 10.41054107240687188, 1.482358050883964840E-15, 0.000000000000000000 ) ) ;
#43392=EDGE_LOOP ( 'NONE', ( #73838, #24645, #83057, #52066, #32654 ) ) ;
#43401=CARTESIAN_POINT ( 'NONE',  ( 44.46823338009918558, 1.482358050883964840E-15, 0.000000000000000000 ) ) ;
#43427=DIRECTION ( 'NONE',  ( -1.000000000000000000, -1.224606353822377258E-16, -0.000000000000000000 ) ) ;
#43450=EDGE_CURVE ( 'NONE', #51711, #84725, #97935, .T. ) ;
#43533=DIRECTION ( 'NONE',  ( 0.000000000000000000, -0.8660254037844380415, 0.5000000000000009992 ) ) ;
#43536=LINE ( 'NONE', #33871, #17833 ) ;
#43537=B_SPLINE_CURVE_WITH_KNOTS ( 'NONE', 3,
 ( #42616, #26481, #85208, #58823, #10249, #67964 ),
 .UNSPECIFIED., .F., .F.,
 ( 4, 2, 4 ),
 ( 0.008690415895085790154, 0.01102883710845593661, 0.01336725832182608306 ),
 .UNSPECIFIED. ) ;
#43543=FACE_OUTER_BOUND ( 'NONE', #95640, .T. ) ;
#43578=CIRCLE ( 'NONE', #50415, 5.000000000000002665 ) ;
#43585=CONICAL_SURFACE ( 'NONE', #3951, 5.000000000000001776, 0.9599310885968803664 ) ;
#43593=CARTESIAN_POINT ( 'NONE',  ( 23.73746414932995208, 1.482358050883964840E-15, 0.000000000000000000 ) ) ;
#43612=AXIS2_PLACEMENT_3D ( 'NONE', #92605, #10094, #101244 ) ;
#43622=CONICAL_SURFACE ( 'NONE', #59111, 5.000000000000001776, 0.9599310885968803664 ) ;
#43659=AXIS2_PLACEMENT_3D ( 'NONE', #16770, #75532, #35650 ) ;
#43661=CARTESIAN_POINT ( 'NONE',  ( -3.828588921589437533E-15, 7.321656987762870550, -3.318518101603011861 ) ) ;
#43668=AXIS2_PLACEMENT_3D ( 'NONE', #63828, #55170, #38499 ) ;
#43712=LINE ( 'NONE', #35663, #11218 ) ;
#43713=EDGE_LOOP ( 'NONE', ( #50516, #105508, #81098, #41452, #66727 ) ) ;
#43754=ORIENTED_EDGE ( 'NONE', *, *, #87637, .F. ) ;
#43769=EDGE_LOOP ( 'NONE', ( #15075, #21746, #14890, #12310, #12939 ) ) ;
#43770=EDGE_CURVE ( 'NONE', #56015, #68447, #8239, .T. ) ;
#43773=AXIS2_PLACEMENT_3D ( 'NONE', #106240, #97620, #56082 ) ;
#43777=CARTESIAN_POINT ( 'NONE',  ( 0.000000000000000000, 0.000000000000000000, 0.000000000000000000 ) ) ;
#43779=DIRECTION ( 'NONE',  ( 0.000000000000000000, -1.000000000000000000, 0.000000000000000000 ) ) ;
#43787=CARTESIAN_POINT ( 'NONE',  ( 43.88846153846154152, -4.171999999999999709, 0.000000000000000000 ) ) ;
#43801=DIRECTION ( 'NONE',  ( 0.5735764363510470476, -0.8191520442889911324, 1.003171929053524007E-16 ) ) ;
#43802=EDGE_CURVE ( 'NONE', #73449, #104380, #62670, .T. ) ;
#43845=EDGE_CURVE ( 'NONE', #64182, #57394, #79885, .T. ) ;
#43887=CIRCLE ( 'NONE', #52503, 5.000000000000002665 ) ;
#43900=VERTEX_POINT ( 'NONE', #13019 ) ;
#43914=ORIENTED_EDGE ( 'NONE', *, *, #48765, .T. ) ;
#44072=SHAPE_REPRESENTATION ( 'hex screw gradec_din_DIN EN 24018 - M10 x 40-WS', ( #10728 ), #54068 ) ;
#44073=EDGE_CURVE ( 'NONE', #23116, #33590, #43537, .T. ) ;
#44091=FACE_OUTER_BOUND ( 'NONE', #76512, .T. ) ;
#44115=DIRECTION ( 'NONE',  ( -1.000000000000000000, -1.224606353822377258E-16, -0.000000000000000000 ) ) ;
#44116=ORIENTED_EDGE ( 'NONE', *, *, #39021, .F. ) ;
#44118=CONICAL_SURFACE ( 'NONE', #2763, 4.172000000000001485, 0.9599310885968750373 ) ;
#44126=ADVANCED_FACE ( 'NONE', ( #92764 ), #77150, .T. ) ;
#44140=CARTESIAN_POINT ( 'NONE',  ( 24.05868969682389036, -5.000000000000000000, 0.000000000000000000 ) ) ;
#44149=AXIS2_PLACEMENT_3D ( 'NONE', #41858, #10025, #49410 ) ;
#44150=EDGE_LOOP ( 'NONE', ( #105427, #9113 ) ) ;
#44163=ORIENTED_EDGE ( 'NONE', *, *, #101544, .T. ) ;
#44167=EDGE_CURVE ( 'NONE', #91513, #12793, #58275, .T. ) ;
#44188=DIRECTION ( 'NONE',  ( 0.000000000000000000, -1.000000000000000000, 0.000000000000000000 ) ) ;
#44209=DIRECTION ( 'NONE',  ( 0.000000000000000000, -1.000000000000000000, 0.000000000000000000 ) ) ;
#44328=DIRECTION ( 'NONE',  ( 0.000000000000000000, -1.000000000000000000, 0.000000000000000000 ) ) ;
#44350=CIRCLE ( 'NONE', #101250, 5.000000000000001776 ) ;
#44388=CIRCLE ( 'NONE', #25402, 5.000000000000002665 ) ;
#44393=EDGE_LOOP ( 'NONE', ( #62737, #40466, #72047, #62462, #56207, #50543 ) ) ;
#44419=DIRECTION ( 'NONE',  ( -1.000000000000000000, -1.224606353822377258E-16, -0.000000000000000000 ) ) ;
#44443=AXIS2_PLACEMENT_3D ( 'NONE', #25964, #2686, #50176 ) ;
#44451=CARTESIAN_POINT ( 'NONE',  ( 27.02022815836235026, 0.000000000000000000, 5.000000000000002665 ) ) ;
#44452=DIRECTION ( 'NONE',  ( 0.000000000000000000, 0.000000000000000000, 1.000000000000000000 ) ) ;
#44468=ORIENTED_EDGE ( 'NONE', *, *, #20418, .F. ) ;
#44489=DIRECTION ( 'NONE',  ( -1.000000000000000000, -1.224606353822377258E-16, -0.000000000000000000 ) ) ;
#44490=ORIENTED_EDGE ( 'NONE', *, *, #74293, .F. ) ;
#44503=LINE ( 'NONE', #95181, #27137 ) ;
#44516=VERTEX_POINT ( 'NONE', #37902 ) ;
#44522=ORIENTED_EDGE ( 'NONE', *, *, #86180, .F. ) ;
#44538=ORIENTED_EDGE ( 'NONE', *, *, #39443, .F. ) ;
#44542=ORIENTED_EDGE ( 'NONE', *, *, #69410, .T. ) ;
#44587=AXIS2_PLACEMENT_3D ( 'NONE', #50527, #59725, #19311 ) ;
#44592=ORIENTED_EDGE ( 'NONE', *, *, #78940, .T. ) ;
#44613=ADVANCED_FACE ( 'NONE', ( #38935 ), #94500, .T. ) ;
#44618=AXIS2_PLACEMENT_3D ( 'NONE', #70410, #37009, #47169 ) ;
#44621=ORIENTED_EDGE ( 'NONE', *, *, #53359, .F. ) ;
#44628=AXIS2_PLACEMENT_3D ( 'NONE', #102017, #36280, #44328 ) ;
#44637=DIRECTION ( 'NONE',  ( 0.000000000000000000, -1.877893248421449036E-16, 1.000000000000000000 ) ) ;
#44651=ORIENTED_EDGE ( 'NONE', *, *, #4016, .F. ) ;
#44685=EDGE_LOOP ( 'NONE', ( #47956, #70088, #52629, #68134, #22846, #99045 ) ) ;
#44689=LINE ( 'NONE', #3696, #9948 ) ;
#44784=VERTEX_POINT ( 'NONE', #3250 ) ;
#44810=EDGE_CURVE ( 'NONE', #13133, #11758, #99626, .T. ) ;
#44825=CARTESIAN_POINT ( 'NONE',  ( 26.69900261086841198, -5.000000000000000000, 6.123233995736768255E-16 ) ) ;
#44841=CIRCLE ( 'NONE', #20779, 8.000000000000000000 ) ;
#44843=ORIENTED_EDGE ( 'NONE', *, *, #73375, .F. ) ;
#44858=ORIENTED_EDGE ( 'NONE', *, *, #61082, .T. ) ;
#44878=LINE ( 'NONE', #36284, #75355 ) ;
#44889=PLANE ( 'NONE',  #92376 ) ;
#44928=LINE ( 'NONE', #5509, #28842 ) ;
#44956=CARTESIAN_POINT ( 'NONE',  ( 16.65484354297773351, 1.340359594676612611E-15, 0.000000000000000000 ) ) ;
#44965=AXIS2_PLACEMENT_3D ( 'NONE', #74220, #41861, #74748 ) ;
#44971=CARTESIAN_POINT ( 'NONE',  ( 20.19615384615384457, 4.172000000000003261, 0.000000000000000000 ) ) ;
#44975=CARTESIAN_POINT ( 'NONE',  ( 26.69900261086841198, 6.123233995736772199E-16, -5.000000000000001776 ) ) ;
#45008=EDGE_CURVE ( 'NONE', #58498, #73855, #51501, .T. ) ;
#45027=DIRECTION ( 'NONE',  ( 0.000000000000000000, -1.000000000000000000, 0.000000000000000000 ) ) ;
#45043=VECTOR ( 'NONE', #89726, 1000.000000000000227 ) ;
#45055=ORIENTED_EDGE ( 'NONE', *, *, #69071, .T. ) ;
#45086=CARTESIAN_POINT ( 'NONE',  ( 0.08224679563971615259, -7.710515798486368588, -2.644994884459107354 ) ) ;
#45096=AXIS2_PLACEMENT_3D ( 'NONE', #2935, #12610, #54125 ) ;
#45134=CYLINDRICAL_SURFACE ( 'NONE', #27034, 5.000000000000002665 ) ;
#45170=DIRECTION ( 'NONE',  ( 0.000000000000000000, -1.000000000000000000, -1.877893248421449036E-16 ) ) ;
#45184=ORIENTED_EDGE ( 'NONE', *, *, #59621, .F. ) ;
#45185=CIRCLE ( 'NONE', #24563, 5.000000000000002665 ) ;
#45199=EDGE_CURVE ( 'NONE', #55144, #2494, #20550, .T. ) ;
#45202=ORIENTED_EDGE ( 'NONE', *, *, #101544, .F. ) ;
#45204=ADVANCED_FACE ( 'NONE', ( #9594 ), #68398, .T. ) ;
#45207=ORIENTED_EDGE ( 'NONE', *, *, #2275, .F. ) ;
#45208=CARTESIAN_POINT ( 'NONE',  ( 40.34715123528543046, 1.340359594676612611E-15, 0.000000000000000000 ) ) ;
#45291=EDGE_LOOP ( 'NONE', ( #9181, #54943, #52849, #6960, #53842 ) ) ;
#45293=VECTOR ( 'NONE', #101776, 1000.000000000000000 ) ;
#45298=DIRECTION ( 'NONE',  ( -1.000000000000000000, -1.224606353822377258E-16, -0.000000000000000000 ) ) ;
#45310=ORIENTED_EDGE ( 'NONE', *, *, #25097, .T. ) ;
#45317=EDGE_LOOP ( 'NONE', ( #79161, #105696, #76365, #18540, #33908 ) ) ;
#45319=VERTEX_POINT ( 'NONE', #69979 ) ;
#45322=CONICAL_SURFACE ( 'NONE', #100433, 5.000000000000001776, 0.9599310885968803664 ) ;
#45326=ORIENTED_EDGE ( 'NONE', *, *, #51664, .F. ) ;
#45343=ORIENTED_EDGE ( 'NONE', *, *, #33297, .F. ) ;
#45365=ORIENTED_EDGE ( 'NONE', *, *, #24868, .T. ) ;
#45388=CARTESIAN_POINT ( 'NONE',  ( 0.000000000000000000, 6.123233995736770227E-16, -5.000000000000002665 ) ) ;
#45418=CARTESIAN_POINT ( 'NONE',  ( 0.7145311798163216377, 4.618802153517004960, 7.999999999999998224 ) ) ;
#45482=ADVANCED_FACE ( 'NONE', ( #80178 ), #39222, .T. ) ;
#45492=MECHANICAL_DESIGN_GEOMETRIC_PRESENTATION_REPRESENTATION('',(#23089),#16201);
#45504=DIRECTION ( 'NONE',  ( -1.000000000000000000, -1.224606353822377258E-16, -0.000000000000000000 ) ) ;
#45519=DIRECTION ( 'NONE',  ( 0.000000000000000000, -1.000000000000000000, 0.000000000000000000 ) ) ;
#45531=DIRECTION ( 'NONE',  ( 0.000000000000000000, -1.000000000000000000, 0.000000000000000000 ) ) ;
#45532=VERTEX_POINT ( 'NONE', #9470 ) ;
#45570=DIRECTION ( 'NONE',  ( 0.000000000000000000, -1.000000000000000000, 0.000000000000000000 ) ) ;
#45572=LINE ( 'NONE', #30460, #28767 ) ;
#45584=DIRECTION ( 'NONE',  ( 0.000000000000000000, -1.000000000000000000, 0.000000000000000000 ) ) ;
#45592=ADVANCED_FACE ( 'NONE', ( #51538 ), #42975, .T. ) ;
#45629=ORIENTED_EDGE ( 'NONE', *, *, #69466, .T. ) ;
#45647=CARTESIAN_POINT ( 'NONE',  ( 35.90484354297773706, -5.000000000000000000, 0.000000000000000000 ) ) ;
#45657=LINE ( 'NONE', #19308, #42724 ) ;
#45665=FACE_OUTER_BOUND ( 'NONE', #33378, .T. ) ;
#45669=DIRECTION ( 'NONE',  ( -1.000000000000000000, -1.224606353822377258E-16, -0.000000000000000000 ) ) ;
#45702=CARTESIAN_POINT ( 'NONE',  ( 15.17407431220850533, 1.340359594676612611E-15, 0.000000000000000000 ) ) ;
#45733=ORIENTED_EDGE ( 'NONE', *, *, #102924, .F. ) ;
#45749=CARTESIAN_POINT ( 'NONE',  ( 6.849999999999999645, -4.618802153517012954, -8.000000000000001776 ) ) ;
#45751=VERTEX_POINT ( 'NONE', #33255 ) ;
#45758=EDGE_CURVE ( 'NONE', #48079, #72287, #49941, .T. ) ;
#45760=DIRECTION ( 'NONE',  ( 0.5735764363510470476, -0.8191520442889911324, 1.003171929053524007E-16 ) ) ;
#45773=EDGE_CURVE ( 'NONE', #12690, #36732, #10230, .T. ) ;
#45790=ORIENTED_EDGE ( 'NONE', *, *, #61001, .F. ) ;
#45841=ORIENTED_EDGE ( 'NONE', *, *, #74446, .F. ) ;
#45851=CARTESIAN_POINT ( 'NONE',  ( 44.46823338009918558, 6.123233995736772199E-16, -5.000000000000001776 ) ) ;
#45856=EDGE_CURVE ( 'NONE', #36720, #53278, #53667, .T. ) ;
#45889=VERTEX_POINT ( 'NONE', #91108 ) ;
#45909=EDGE_LOOP ( 'NONE', ( #4301, #1153, #19297, #100147, #98476 ) ) ;
#45926=DIRECTION ( 'NONE',  ( -1.000000000000000000, -1.224606353822377258E-16, -0.000000000000000000 ) ) ;
#45941=DIRECTION ( 'NONE',  ( 0.000000000000000000, -1.000000000000000000, 0.000000000000000000 ) ) ;
#45947=DIRECTION ( 'NONE',  ( -0.000000000000000000, 0.5000000000000009992, 0.8660254037844380415 ) ) ;
#45964=CONICAL_SURFACE ( 'NONE', #9830, 5.000000000000001776, 0.9599310885968803664 ) ;
#45972=AXIS2_PLACEMENT_3D ( 'NONE', #75821, #35945, #52598 ) ;
#45996=VECTOR ( 'NONE', #91881, 1000.000000000000000 ) ;
#46059=AXIS2_PLACEMENT_3D ( 'NONE', #57082, #91081, #82438 ) ;
#46087=VECTOR ( 'NONE', #56615, 1000.000000000000000 ) ;
#46141=VECTOR ( 'NONE', #21698, 999.9999999999998863 ) ;
#46142=FACE_OUTER_BOUND ( 'NONE', #302, .T. ) ;
#46149=AXIS2_PLACEMENT_3D ( 'NONE', #74099, #67632, #8309 ) ;
#46156=AXIS2_PLACEMENT_3D ( 'NONE', #59274, #84068, #77577 ) ;
#46169=CARTESIAN_POINT ( 'NONE',  ( 12.21253585067004543, 1.340359594676612611E-15, 0.000000000000000000 ) ) ;
#46208=ADVANCED_FACE ( 'NONE', ( #28515 ), #54317, .T. ) ;
#46274=DIRECTION ( 'NONE',  ( 0.000000000000000000, -1.000000000000000000, 0.000000000000000000 ) ) ;
#46311=DIRECTION ( 'NONE',  ( -1.000000000000000000, -0.000000000000000000, -0.000000000000000000 ) ) ;
#46345=ORIENTED_EDGE ( 'NONE', *, *, #36831, .T. ) ;
#46351=ORIENTED_EDGE ( 'NONE', *, *, #80293, .T. ) ;
#46363=DIRECTION ( 'NONE',  ( 0.5735764363510470476, -0.8191520442889911324, 1.003171929053524007E-16 ) ) ;
#46423=DIRECTION ( 'NONE',  ( 0.000000000000000000, 0.000000000000000000, 1.000000000000000000 ) ) ;
#46435=ORIENTED_EDGE ( 'NONE', *, *, #85508, .F. ) ;
#46444=CARTESIAN_POINT ( 'NONE',  ( 0.000000000000000000, 0.000000000000000000, 5.000000000000002665 ) ) ;
#46445=CONICAL_SURFACE ( 'NONE', #11939, 5.000000000000001776, 0.9599310885968803664 ) ;
#46447=VERTEX_POINT ( 'NONE', #78360 ) ;
#46483=CARTESIAN_POINT ( 'NONE',  ( 32.04230769230768772, 4.172000000000003261, 0.000000000000000000 ) ) ;
#46527=EDGE_CURVE ( 'NONE', #3051, #95088, #52094, .T. ) ;
#46545=CARTESIAN_POINT ( 'NONE',  ( 32.62207953394533178, 1.482358050883964840E-15, 0.000000000000000000 ) ) ;
#46550=VECTOR ( 'NONE', #22392, 999.9999999999998863 ) ;
#46561=CARTESIAN_POINT ( 'NONE',  ( 42.98746414932995208, 5.000000000000003553, 0.000000000000000000 ) ) ;
#46566=CARTESIAN_POINT ( 'NONE',  ( 39.44615384615384812, 4.172000000000003261, 0.000000000000000000 ) ) ;
#46587=VECTOR ( 'NONE', #14488, 999.9999999999998863 ) ;
#46592=DIRECTION ( 'NONE',  ( 0.000000000000000000, -1.000000000000000000, 0.000000000000000000 ) ) ;
#46603=DIRECTION ( 'NONE',  ( 1.000000000000000000, 1.224606353822377258E-16, 0.000000000000000000 ) ) ;
#46606=AXIS2_PLACEMENT_3D ( 'NONE', #104168, #30310, #96093 ) ;
#46607=CARTESIAN_POINT ( 'NONE',  ( 13.37207953394533355, -5.000000000000000888, 6.123233995736769241E-16 ) ) ;
#46636=CARTESIAN_POINT ( 'NONE',  ( 42.40769230769231513, -4.171999999999999709, 0.000000000000000000 ) ) ;
#46650=EDGE_CURVE ( 'NONE', #24684, #32861, #49163, .T. ) ;
#46686=CARTESIAN_POINT ( 'NONE',  ( 6.849999999999999645, 9.237604307034018802, 0.000000000000000000 ) ) ;
#46696=DIRECTION ( 'NONE',  ( -1.000000000000000000, -1.224606353822377258E-16, -0.000000000000000000 ) ) ;
#46712=AXIS2_PLACEMENT_3D ( 'NONE', #90291, #16400, #82186 ) ;
#46713=EDGE_CURVE ( 'NONE', #47940, #28900, #9771, .T. ) ;
#46749=CONICAL_SURFACE ( 'NONE', #60555, 4.172000000000001485, 0.9599310885968750373 ) ;
#46756=CIRCLE ( 'NONE', #55359, 5.000000000000002665 ) ;
#46759=DIRECTION ( 'NONE',  ( 0.000000000000000000, -1.000000000000000000, 0.000000000000000000 ) ) ;
#46784=DIRECTION ( 'NONE',  ( -1.000000000000000000, -1.224606353822377258E-16, -0.000000000000000000 ) ) ;
#46854=CARTESIAN_POINT ( 'NONE',  ( 0.000000000000000000, 0.000000000000000000, 5.000000000000002665 ) ) ;
#46870=ORIENTED_EDGE ( 'NONE', *, *, #65308, .T. ) ;
#46893=CARTESIAN_POINT ( 'NONE',  ( 0.000000000000000000, 6.123233995736770227E-16, -5.000000000000002665 ) ) ;
#46901=EDGE_CURVE ( 'NONE', #58211, #25469, #47972, .T. ) ;
#46922=DIRECTION ( 'NONE',  ( -0.5735764363510510444, -0.8191520442889883569, 0.000000000000000000 ) ) ;
#46931=ORIENTED_EDGE ( 'NONE', *, *, #36911, .T. ) ;
#46949=ORIENTED_EDGE ( 'NONE', *, *, #88378, .T. ) ;
#46968=DIRECTION ( 'NONE',  ( 0.000000000000000000, 1.000000000000000000, 0.000000000000000000 ) ) ;
#46986=EDGE_CURVE ( 'NONE', #93494, #7084, #98225, .T. ) ;
#47017=CARTESIAN_POINT ( 'NONE',  ( 25.21823338009918203, 1.482358050883964840E-15, 0.000000000000000000 ) ) ;
#47040=FACE_OUTER_BOUND ( 'NONE', #36101, .T. ) ;
#47041=ADVANCED_FACE ( 'NONE', ( #58204 ), #20926, .T. ) ;
#47044=ADVANCED_FACE ( 'NONE', ( #73853 ), #56947, .T. ) ;
#47104=ORIENTED_EDGE ( 'NONE', *, *, #76115, .F. ) ;
#47113=VECTOR ( 'NONE', #88816, 1000.000000000000000 ) ;
#47125=ORIENTED_EDGE ( 'NONE', *, *, #58949, .T. ) ;
#47169=DIRECTION ( 'NONE',  ( 0.000000000000000000, 0.000000000000000000, 1.000000000000000000 ) ) ;
#47172=CARTESIAN_POINT ( 'NONE',  ( -9.215718466126777828E-16, -7.124194613927628872, -3.660532965668816363 ) ) ;
#47190=CARTESIAN_POINT ( 'NONE',  ( 37.06438722625302518, -5.000000000000000888, 6.123233995736769241E-16 ) ) ;
#47199=CARTESIAN_POINT ( 'NONE',  ( 9.250997389131581983, 5.000000000000004441, 6.123233995736770227E-16 ) ) ;
#47201=EDGE_CURVE ( 'NONE', #68161, #93742, #3629, .T. ) ;
#47215=DIRECTION ( 'NONE',  ( -1.000000000000000000, -1.224606353822377258E-16, -0.000000000000000000 ) ) ;
#47233=CARTESIAN_POINT ( 'NONE',  ( 40.34715123528543046, 6.123233995736770227E-16, -5.000000000000002665 ) ) ;
#47294=EDGE_CURVE ( 'NONE', #36720, #43900, #51700, .T. ) ;
#47307=DIRECTION ( 'NONE',  ( -1.000000000000000000, -0.000000000000000000, -0.000000000000000000 ) ) ;
#47328=EDGE_CURVE ( 'NONE', #98966, #99927, #30653, .T. ) ;
#47330=ORIENTED_EDGE ( 'NONE', *, *, #59750, .F. ) ;
#47337=ORIENTED_EDGE ( 'NONE', *, *, #94575, .T. ) ;
#47340=DIRECTION ( 'NONE',  ( -1.000000000000000000, -1.224606353822377258E-16, -0.000000000000000000 ) ) ;
#47350=AXIS2_PLACEMENT_3D ( 'NONE', #30756, #71693, #63642 ) ;
#47383=EDGE_CURVE ( 'NONE', #33590, #71421, #34168, .T. ) ;
#47388=CIRCLE ( 'NONE', #28742, 5.000000000000001776 ) ;
#47402=ORIENTED_EDGE ( 'NONE', *, *, #39111, .F. ) ;
#47426=FACE_OUTER_BOUND ( 'NONE', #3591, .T. ) ;
#47462=CARTESIAN_POINT ( 'NONE',  ( 21.09715123528542691, 1.340359594676612611E-15, 0.000000000000000000 ) ) ;
#47501=AXIS2_PLACEMENT_3D ( 'NONE', #16883, #49763, #91830 ) ;
#47504=EDGE_CURVE ( 'NONE', #45889, #64182, #96623, .T. ) ;
#47539=AXIS2_PLACEMENT_3D ( 'NONE', #36062, #44115, #36592 ) ;
#47541=VERTEX_POINT ( 'NONE', #106626 ) ;
#47554=ORIENTED_EDGE ( 'NONE', *, *, #80421, .F. ) ;
#47568=AXIS2_PLACEMENT_3D ( 'NONE', #54000, #86420, #79351 ) ;
#47572=LINE ( 'NONE', #40552, #5105 ) ;
#47589=CARTESIAN_POINT ( 'NONE',  ( 9.830769230769229594, 1.411358822780289120E-15, 0.000000000000000000 ) ) ;
#47595=AXIS2_PLACEMENT_3D ( 'NONE', #80338, #71713, #25763 ) ;
#47597=FACE_OUTER_BOUND ( 'NONE', #90264, .T. ) ;
#47603=ORIENTED_EDGE ( 'NONE', *, *, #5586, .F. ) ;
#47604=LINE ( 'NONE', #39010, #86633 ) ;
#47608=LINE ( 'NONE', #80503, #40883 ) ;
#47610=DIRECTION ( 'NONE',  ( 0.000000000000000000, -1.000000000000000000, 0.000000000000000000 ) ) ;
#47627=VECTOR ( 'NONE', #13438, 1000.000000000000000 ) ;
#47638=CARTESIAN_POINT ( 'NONE',  ( 16.33361799548379523, 1.482358050883964840E-15, 0.000000000000000000 ) ) ;
#47643=ORIENTED_EDGE ( 'NONE', *, *, #84968, .F. ) ;
#47647=EDGE_CURVE ( 'NONE', #48268, #18270, #60541, .T. ) ;
#47710=ORIENTED_EDGE ( 'NONE', *, *, #9543, .T. ) ;
#47718=DIRECTION ( 'NONE',  ( 0.000000000000000000, -1.000000000000000000, 0.000000000000000000 ) ) ;
#47729=ORIENTED_EDGE ( 'NONE', *, *, #41458, .F. ) ;
#47730=ORIENTED_EDGE ( 'NONE', *, *, #76256, .F. ) ;
#47737=FACE_OUTER_BOUND ( 'NONE', #70773, .T. ) ;
#47740=VERTEX_POINT ( 'NONE', #47199 ) ;
#47792=ORIENTED_EDGE ( 'NONE', *, *, #8110, .T. ) ;
#47806=DIRECTION ( 'NONE',  ( 0.000000000000000000, 0.000000000000000000, 1.000000000000000000 ) ) ;
#47851=ORIENTED_EDGE ( 'NONE', *, *, #88966, .F. ) ;
#47858=VERTEX_POINT ( 'NONE', #22444 ) ;
#47861=FACE_OUTER_BOUND ( 'NONE', #18116, .T. ) ;
#47870=EDGE_CURVE ( 'NONE', #95088, #85724, #21381, .T. ) ;
#47878=DIRECTION ( 'NONE',  ( 1.000000000000000000, 0.000000000000000000, 0.000000000000000000 ) ) ;
#47885=EDGE_LOOP ( 'NONE', ( #5460, #42886, #95604, #37182, #99813, #47851 ) ) ;
#47902=CONICAL_SURFACE ( 'NONE', #15186, 4.172000000000001485, 0.9599310885968750373 ) ;
#47913=CARTESIAN_POINT ( 'NONE',  ( 0.000000000000000000, 6.928203230275505220, -4.000000000000007994 ) ) ;
#47940=VERTEX_POINT ( 'NONE', #56875 ) ;
#47956=ORIENTED_EDGE ( 'NONE', *, *, #79742, .T. ) ;
#47960=ORIENTED_EDGE ( 'NONE', *, *, #11413, .T. ) ;
#47972=LINE ( 'NONE', #96026, #84467 ) ;
#47974=AXIS2_PLACEMENT_3D ( 'NONE', #67452, #90117, #83089 ) ;
#48048=VERTEX_POINT ( 'NONE', #16978 ) ;
#48079=VERTEX_POINT ( 'NONE', #66579 ) ;
#48083=ORIENTED_EDGE ( 'NONE', *, *, #83854, .F. ) ;
#48143=CIRCLE ( 'NONE', #1622, 5.000000000000002665 ) ;
#48164=ORIENTED_EDGE ( 'NONE', *, *, #93691, .T. ) ;
#48211=VECTOR ( 'NONE', #70147, 999.9999999999998863 ) ;
#48220=CONICAL_SURFACE ( 'NONE', #1723, 4.172000000000001485, 0.9599310885968750373 ) ;
#48221=CARTESIAN_POINT ( 'NONE',  ( 18.71538461538461462, 1.411358822780289120E-15, 0.000000000000000000 ) ) ;
#48222=EDGE_LOOP ( 'NONE', ( #21799, #70442, #90967, #102896, #4455 ) ) ;
#48238=ORIENTED_EDGE ( 'NONE', *, *, #14487, .F. ) ;
#48248=ORIENTED_EDGE ( 'NONE', *, *, #96255, .T. ) ;
#48266=CARTESIAN_POINT ( 'NONE',  ( 0.000000000000000000, 0.000000000000000000, 5.000000000000002665 ) ) ;
#48267=AXIS2_PLACEMENT_3D ( 'NONE', #75788, #59627, #1882 ) ;
#48268=VERTEX_POINT ( 'NONE', #69260 ) ;
#48326=ORIENTED_EDGE ( 'NONE', *, *, #34703, .F. ) ;
#48371=VERTEX_POINT ( 'NONE', #21258 ) ;
#48420=ADVANCED_FACE ( 'NONE', ( #34526 ), #40894, .T. ) ;
#48445=DIRECTION ( 'NONE',  ( 0.000000000000000000, 0.000000000000000000, 1.000000000000000000 ) ) ;
#48465=EDGE_CURVE ( 'NONE', #24684, #8257, #15012, .T. ) ;
#48472=VERTEX_POINT ( 'NONE', #55157 ) ;
#48478=CARTESIAN_POINT ( 'NONE',  ( 28.17977184163764193, 5.000000000000002665, 0.000000000000000000 ) ) ;
#48503=CARTESIAN_POINT ( 'NONE',  ( 32.94330508143927716, 1.340359594676612611E-15, 0.000000000000000000 ) ) ;
#48521=CYLINDRICAL_SURFACE ( 'NONE', #3494, 5.000000000000002665 ) ;
#48548=ORIENTED_EDGE ( 'NONE', *, *, #70282, .F. ) ;
#48569=ORIENTED_EDGE ( 'NONE', *, *, #18802, .T. ) ;
#48572=AXIS2_PLACEMENT_3D ( 'NONE', #52952, #19579, #85881 ) ;
#48606=CARTESIAN_POINT ( 'NONE',  ( 16.33361799548379523, 1.482358050883964840E-15, 0.000000000000000000 ) ) ;
#48620=CARTESIAN_POINT ( 'NONE',  ( 8.929771841637641927, -5.000000000000000000, 6.123233995736768255E-16 ) ) ;
#48637=ORIENTED_EDGE ( 'NONE', *, *, #89402, .T. ) ;
#48657=EDGE_LOOP ( 'NONE', ( #81157, #86220, #39690, #26745, #77895 ) ) ;
#48658=EDGE_CURVE ( 'NONE', #61495, #60319, #101841, .T. ) ;
#48675=CARTESIAN_POINT ( 'NONE',  ( 44.46823338009918558, 5.000000000000002665, 0.000000000000000000 ) ) ;
#48676=VERTEX_POINT ( 'NONE', #101324 ) ;
#48691=VERTEX_POINT ( 'NONE', #94839 ) ;
#48728=CARTESIAN_POINT ( 'NONE',  ( 10.41054107240687188, 1.482358050883964840E-15, 0.000000000000000000 ) ) ;
#48765=EDGE_CURVE ( 'NONE', #2566, #67515, #55056, .T. ) ;
#48771=CARTESIAN_POINT ( 'NONE',  ( 20.77592568779148863, -5.000000000000000000, 6.123233995736768255E-16 ) ) ;
#48824=CARTESIAN_POINT ( 'NONE',  ( 13.37207953394533355, 1.482358050883964840E-15, 0.000000000000000000 ) ) ;
#48828=ADVANCED_FACE ( 'NONE', ( #67244 ), #56995, .T. ) ;
#48849=FACE_OUTER_BOUND ( 'NONE', #60664, .T. ) ;
#48867=CIRCLE ( 'NONE', #2385, 5.000000000000002665 ) ;
#48869=CARTESIAN_POINT ( 'NONE',  ( 35.58361799548379167, 1.482358050883964840E-15, 0.000000000000000000 ) ) ;
#48879=ORIENTED_EDGE ( 'NONE', *, *, #89799, .F. ) ;
#48891=CARTESIAN_POINT ( 'NONE',  ( 10.73176661990081371, 1.340359594676612611E-15, 0.000000000000000000 ) ) ;
#48927=DIRECTION ( 'NONE',  ( 0.000000000000000000, 0.000000000000000000, -1.000000000000000000 ) ) ;
#48959=DIRECTION ( 'NONE',  ( 1.000000000000000000, 0.000000000000000000, 0.000000000000000000 ) ) ;
#48960=CARTESIAN_POINT ( 'NONE',  ( 5.260074602449203133E-16, -0.7818963811860513147, -8.000000000000000000 ) ) ;
#48977=DIRECTION ( 'NONE',  ( -1.000000000000000000, -1.224606353822377258E-16, -0.000000000000000000 ) ) ;
#48982=EDGE_LOOP ( 'NONE', ( #16695, #18997, #89534, #4745, #64085, #77974 ) ) ;
#48992=CYLINDRICAL_SURFACE ( 'NONE', #19911, 5.000000000000002665 ) ;
#49005=CARTESIAN_POINT ( 'NONE',  ( 0.06809871960542653035, -6.146186931204441706, -5.354491962338080668 ) ) ;
#49036=DIRECTION ( 'NONE',  ( 0.000000000000000000, -1.000000000000000000, 0.000000000000000000 ) ) ;
#49072=EDGE_CURVE ( 'NONE', #16452, #103302, #77455, .T. ) ;
#49093=AXIS2_PLACEMENT_3D ( 'NONE', #62871, #69368, #4096 ) ;
#49103=EDGE_CURVE ( 'NONE', #90027, #32720, #91281, .T. ) ;
#49111=CARTESIAN_POINT ( 'NONE',  ( 37.96538461538461462, -4.171999999999999709, 5.616230220889763424E-16 ) ) ;
#49120=VERTEX_POINT ( 'NONE', #47190 ) ;
#49147=VERTEX_POINT ( 'NONE', #5680 ) ;
#49156=PLANE ( 'NONE',  #104669 ) ;
#49163=LINE ( 'NONE', #25480, #77615 ) ;
#49203=EDGE_CURVE ( 'NONE', #42513, #8439, #31580, .T. ) ;
#49249=AXIS2_PLACEMENT_3D ( 'NONE', #79308, #62612, #8998 ) ;
#49258=AXIS2_PLACEMENT_3D ( 'NONE', #68510, #51225, #92765 ) ;
#49274=CARTESIAN_POINT ( 'NONE',  ( 41.82792046605465686, -5.000000000000009770, 0.000000000000000000 ) ) ;
#49286=CIRCLE ( 'NONE', #82000, 5.000000000000004441 ) ;
#49296=ORIENTED_EDGE ( 'NONE', *, *, #39084, .T. ) ;
#49300=DIRECTION ( 'NONE',  ( 1.000000000000000000, 1.224606353822377258E-16, 0.000000000000000000 ) ) ;
#49317=LINE ( 'NONE', #90325, #91827 ) ;
#49321=CARTESIAN_POINT ( 'NONE',  ( 34.10284876471455817, 1.482358050883964840E-15, 0.000000000000000000 ) ) ;
#49329=ADVANCED_FACE ( 'NONE', ( #1275 ), #50370, .T. ) ;
#49335=VECTOR ( 'NONE', #71657, 999.9999999999998863 ) ;
#49343=CIRCLE ( 'NONE', #97607, 8.000000000000000000 ) ;
#49344=DIRECTION ( 'NONE',  ( 0.5735764363510470476, -0.8191520442889911324, 1.003171929053524007E-16 ) ) ;
#49354=DIRECTION ( 'NONE',  ( 0.000000000000000000, -1.000000000000000000, 0.000000000000000000 ) ) ;
#49370=EDGE_CURVE ( 'NONE', #29485, #5037, #10393, .T. ) ;
#49382=DIRECTION ( 'NONE',  ( 0.000000000000000000, 1.000000000000000000, 0.000000000000000000 ) ) ;
#49410=DIRECTION ( 'NONE',  ( 0.000000000000000000, -1.000000000000000000, 0.000000000000000000 ) ) ;
#49454=DIRECTION ( 'NONE',  ( 0.000000000000000000, -1.000000000000000000, 0.000000000000000000 ) ) ;
#49471=DIRECTION ( 'NONE',  ( -1.000000000000000000, -1.224606353822377258E-16, -0.000000000000000000 ) ) ;
#49472=ADVANCED_FACE ( 'NONE', ( #76251 ), #3971, .T. ) ;
#49504=DIRECTION ( 'NONE',  ( 1.000000000000000000, 1.224606353822377258E-16, 0.000000000000000000 ) ) ;
#49515=EDGE_LOOP ( 'NONE', ( #80368, #40518, #74379, #99611, #24050 ) ) ;
#49520=DIRECTION ( 'NONE',  ( 0.000000000000000000, 0.4999999999999999445, -0.8660254037844387076 ) ) ;
#49563=VECTOR ( 'NONE', #37781, 999.9999999999998863 ) ;
#49604=CARTESIAN_POINT ( 'NONE',  ( 0.000000000000000000, 0.000000000000000000, 0.000000000000000000 ) ) ;
#49621=VERTEX_POINT ( 'NONE', #4498 ) ;
#49623=DIRECTION ( 'NONE',  ( 0.5735764363510470476, -0.8191520442889911324, 1.003171929053524007E-16 ) ) ;
#49654=CONICAL_SURFACE ( 'NONE', #63474, 5.000000000000001776, 0.9599310885968803664 ) ;
#49662=AXIS2_PLACEMENT_3D ( 'NONE', #55009, #15092, #88472 ) ;
#49668=ORIENTED_EDGE ( 'NONE', *, *, #93067, .F. ) ;
#49671=DIRECTION ( 'NONE',  ( -0.5735764363510512664, 0.8191520442889881348, 1.003171929053520309E-16 ) ) ;
#49674=DIRECTION ( 'NONE',  ( -1.000000000000000000, -1.224606353822377258E-16, -0.000000000000000000 ) ) ;
#49677=FACE_OUTER_BOUND ( 'NONE', #43392, .T. ) ;
#49718=CARTESIAN_POINT ( 'NONE',  ( 7.770228158362351145, 1.340359594676612611E-15, 0.000000000000000000 ) ) ;
#49753=DIRECTION ( 'NONE',  ( 0.000000000000000000, -1.000000000000000000, 0.000000000000000000 ) ) ;
#49762=VECTOR ( 'NONE', #42728, 1000.000000000000000 ) ;
#49763=DIRECTION ( 'NONE',  ( -1.000000000000000000, -1.224606353822377258E-16, -0.000000000000000000 ) ) ;
#49823=ORIENTED_EDGE ( 'NONE', *, *, #51335, .F. ) ;
#49878=ORIENTED_EDGE ( 'NONE', *, *, #58949, .F. ) ;
#49892=CARTESIAN_POINT ( 'NONE',  ( 13.69330508143927538, 1.340359594676612611E-15, 0.000000000000000000 ) ) ;
#49924=CARTESIAN_POINT ( 'NONE',  ( 24.63846153846153797, 1.411358822780289120E-15, 0.000000000000000000 ) ) ;
#49940=ORIENTED_EDGE ( 'NONE', *, *, #78143, .T. ) ;
#49941=LINE ( 'NONE', #21869, #56728 ) ;
#49959=ORIENTED_EDGE ( 'NONE', *, *, #50775, .F. ) ;
#49978=ORIENTED_EDGE ( 'NONE', *, *, #65428, .F. ) ;
#49991=DIRECTION ( 'NONE',  ( 0.5735764363510468256, 0.8191520442889913545, 0.000000000000000000 ) ) ;
#50011=FACE_OUTER_BOUND ( 'NONE', #6992, .T. ) ;
#50014=ORIENTED_EDGE ( 'NONE', *, *, #21402, .T. ) ;
#50042=CARTESIAN_POINT ( 'NONE',  ( 29.66054107240687543, 1.482358050883964840E-15, 0.000000000000000000 ) ) ;
#50043=CARTESIAN_POINT ( 'NONE',  ( 6.249999999999998224, -6.928203230275509661, -4.000000000000000000 ) ) ;
#50045=AXIS2_PLACEMENT_3D ( 'NONE', #43383, #25642, #2373 ) ;
#50062=AXIS2_PLACEMENT_3D ( 'NONE', #8625, #15654, #96595 ) ;
#50063=DIRECTION ( 'NONE',  ( -1.000000000000000000, -0.000000000000000000, -0.000000000000000000 ) ) ;
#50083=DIRECTION ( 'NONE',  ( -1.000000000000000000, -0.000000000000000000, -0.000000000000000000 ) ) ;
#50103=DIRECTION ( 'NONE',  ( -1.000000000000000000, -0.000000000000000000, -0.000000000000000000 ) ) ;
#50136=CARTESIAN_POINT ( 'NONE',  ( 12.21253585067004543, 1.340359594676612611E-15, 0.000000000000000000 ) ) ;
#50150=ORIENTED_EDGE ( 'NONE', *, *, #92693, .T. ) ;
#50156=DIRECTION ( 'NONE',  ( -1.000000000000000000, -0.000000000000000000, -0.000000000000000000 ) ) ;
#50163=( NAMED_UNIT ( * ) SI_UNIT ( $, .STERADIAN. ) SOLID_ANGLE_UNIT ( ) );
#50173=LINE ( 'NONE', #34566, #56924 ) ;
#50176=DIRECTION ( 'NONE',  ( 0.000000000000000000, -1.000000000000000000, 0.000000000000000000 ) ) ;
#50210=LINE ( 'NONE', #24382, #90382 ) ;
#50223=ORIENTED_EDGE ( 'NONE', *, *, #71883, .T. ) ;
#50248=ORIENTED_EDGE ( 'NONE', *, *, #516, .F. ) ;
#50258=DIRECTION ( 'NONE',  ( -1.000000000000000000, -1.224606353822377258E-16, -0.000000000000000000 ) ) ;
#50268=EDGE_LOOP ( 'NONE', ( #11582, #68920, #69649, #65122, #44490 ) ) ;
#50295=VECTOR ( 'NONE', #80674, 1000.000000000000000 ) ;
#50316=DIRECTION ( 'NONE',  ( -0.5735764363510512664, 0.8191520442889881348, 1.003171929053520309E-16 ) ) ;
#50326=ADVANCED_FACE ( 'NONE', ( #47737 ), #54229, .T. ) ;
#50370=CYLINDRICAL_SURFACE ( 'NONE', #98259, 5.000000000000002665 ) ;
#50379=DIRECTION ( 'NONE',  ( 0.000000000000000000, 1.000000000000000000, 0.000000000000000000 ) ) ;
#50381=VERTEX_POINT ( 'NONE', #56351 ) ;
#50387=CIRCLE ( 'NONE', #59041, 5.000000000000002665 ) ;
#50395=CARTESIAN_POINT ( 'NONE',  ( 14.27307692307692299, 4.172000000000003261, 5.109226446042759579E-16 ) ) ;
#50397=ORIENTED_EDGE ( 'NONE', *, *, #32887, .T. ) ;
#50399=EDGE_CURVE ( 'NONE', #73528, #20871, #5182, .T. ) ;
#50415=AXIS2_PLACEMENT_3D ( 'NONE', #58184, #34492, #17221 ) ;
#50417=LINE ( 'NONE', #9419, #38405 ) ;
#50442=FACE_OUTER_BOUND ( 'NONE', #96301, .T. ) ;
#50463=DIRECTION ( 'NONE',  ( -1.000000000000000000, -0.000000000000000000, -0.000000000000000000 ) ) ;
#50489=CARTESIAN_POINT ( 'NONE',  ( 8.929771841637641927, 1.482358050883964840E-15, 0.000000000000000000 ) ) ;
#50505=AXIS2_PLACEMENT_3D ( 'NONE', #21199, #86972, #62689 ) ;
#50516=ORIENTED_EDGE ( 'NONE', *, *, #73604, .F. ) ;
#50527=CARTESIAN_POINT ( 'NONE',  ( 40.02592568779148507, 1.482358050883964840E-15, 0.000000000000000000 ) ) ;
#50528=ADVANCED_FACE ( 'NONE', ( #61172 ), #10994, .T. ) ;
#50543=ORIENTED_EDGE ( 'NONE', *, *, #103826, .F. ) ;
#50552=DIRECTION ( 'NONE',  ( 0.000000000000000000, 1.000000000000000000, 0.000000000000000000 ) ) ;
#50559=CARTESIAN_POINT ( 'NONE',  ( 26.11923076923076792, -4.171999999999999709, 5.616230220889763424E-16 ) ) ;
#50662=FACE_OUTER_BOUND ( 'NONE', #40685, .T. ) ;
#50668=SURFACE_STYLE_FILL_AREA ( #2125 ) ;
#50694=DIRECTION ( 'NONE',  ( -1.000000000000000000, -1.224606353822377258E-16, -0.000000000000000000 ) ) ;
#50695=EDGE_CURVE ( 'NONE', #70219, #85144, #97227, .T. ) ;
#50718=CARTESIAN_POINT ( 'NONE',  ( 8.929771841637641927, 5.000000000000002665, 0.000000000000000000 ) ) ;
#50720=DIRECTION ( 'NONE',  ( 0.000000000000000000, -1.000000000000000000, 0.000000000000000000 ) ) ;
#50736=EDGE_CURVE ( 'NONE', #61254, #94186, #3649, .T. ) ;
#50738=DIRECTION ( 'NONE',  ( 0.000000000000000000, -1.000000000000000000, 0.000000000000000000 ) ) ;
#50739=EDGE_LOOP ( 'NONE', ( #32329, #103790, #41214, #27508, #48637 ) ) ;
#50775=EDGE_CURVE ( 'NONE', #95821, #25469, #105261, .T. ) ;
#50785=DIRECTION ( 'NONE',  ( -1.000000000000000000, 0.000000000000000000, -0.000000000000000000 ) ) ;
#50799=FACE_OUTER_BOUND ( 'NONE', #78803, .T. ) ;
#50802=ADVANCED_FACE ( 'NONE', ( #81038 ), #7153, .F. ) ;
#50803=CARTESIAN_POINT ( 'NONE',  ( 40.92692307692308162, 4.172000000000003261, 5.109226446042759579E-16 ) ) ;
#50814=DIRECTION ( 'NONE',  ( -1.000000000000000000, -0.000000000000000000, -0.000000000000000000 ) ) ;
#50825=CARTESIAN_POINT ( 'NONE',  ( 0.000000000000000000, 0.000000000000000000, 0.000000000000000000 ) ) ;
#50847=EDGE_CURVE ( 'NONE', #104380, #74005, #55285, .T. ) ;
#50873=CARTESIAN_POINT ( 'NONE',  ( 6.249999999999998224, 4.618802153517001408, -8.000000000000000000 ) ) ;
#50922=ADVANCED_FACE ( 'NONE', ( #40592 ), #46749, .T. ) ;
#50947=FACE_OUTER_BOUND ( 'NONE', #40928, .T. ) ;
#50951=EDGE_LOOP ( 'NONE', ( #12854, #19157, #35790, #52001, #40431 ) ) ;
#50964=ADVANCED_FACE ( 'NONE', ( #15784 ), #89801, .T. ) ;
#50967=PRODUCT_DEFINITION_SHAPE ( 'NONE', 'NONE',  #54175 ) ;
#50971=ORIENTED_EDGE ( 'NONE', *, *, #96594, .T. ) ;
#50992=CARTESIAN_POINT ( 'NONE',  ( 14.85284876471456350, 1.482358050883964840E-15, 0.000000000000000000 ) ) ;
#51003=EDGE_CURVE ( 'NONE', #28378, #83974, #17932, .T. ) ;
#51019=CARTESIAN_POINT ( 'NONE',  ( 28.50099738913158376, 6.123233995736770227E-16, -5.000000000000002665 ) ) ;
#51051=DIRECTION ( 'NONE',  ( -1.000000000000000000, -1.224606353822377258E-16, -0.000000000000000000 ) ) ;
#51057=EDGE_LOOP ( 'NONE', ( #60925, #12333, #100392, #44116, #26868 ) ) ;
#51066=DIRECTION ( 'NONE',  ( -1.000000000000000000, 0.000000000000000000, -0.000000000000000000 ) ) ;
#51086=VECTOR ( 'NONE', #53658, 1000.000000000000000 ) ;
#51096=CARTESIAN_POINT ( 'NONE',  ( 40.02592568779148507, 5.000000000000003553, 0.000000000000000000 ) ) ;
#51103=ORIENTED_EDGE ( 'NONE', *, *, #102184, .T. ) ;
#51118=ORIENTED_EDGE ( 'NONE', *, *, #54093, .T. ) ;
#51141=DIRECTION ( 'NONE',  ( -1.000000000000000000, -1.224606353822377258E-16, -0.000000000000000000 ) ) ;
#51198=CARTESIAN_POINT ( 'NONE',  ( 9.830769230769229594, -4.171999999999999709, 5.616230220889763424E-16 ) ) ;
#51225=DIRECTION ( 'NONE',  ( -1.000000000000000000, -1.224606353822377258E-16, -0.000000000000000000 ) ) ;
#51229=CARTESIAN_POINT ( 'NONE',  ( 16.33361799548379523, 6.123233995736772199E-16, -5.000000000000001776 ) ) ;
#51248=ORIENTED_EDGE ( 'NONE', *, *, #28162, .T. ) ;
#51260=DIRECTION ( 'NONE',  ( 0.000000000000000000, -1.000000000000000000, 0.000000000000000000 ) ) ;
#51271=CONICAL_SURFACE ( 'NONE', #3094, 4.172000000000001485, 0.9599310885968750373 ) ;
#51299=DIRECTION ( 'NONE',  ( 0.000000000000000000, 0.000000000000000000, 1.000000000000000000 ) ) ;
#51335=EDGE_CURVE ( 'NONE', #85882, #70645, #95046, .T. ) ;
#51339=FACE_OUTER_BOUND ( 'NONE', #79663, .T. ) ;
#51363=FACE_OUTER_BOUND ( 'NONE', #7037, .T. ) ;
#51364=EDGE_LOOP ( 'NONE', ( #87117, #7000, #40842, #95028, #37791, #68518 ) ) ;
#51394=CONICAL_SURFACE ( 'NONE', #77281, 4.172000000000001485, 0.9599310885968750373 ) ;
#51452=ORIENTED_EDGE ( 'NONE', *, *, #46713, .F. ) ;
#51462=CARTESIAN_POINT ( 'NONE',  ( 18.71538461538461462, 4.172000000000003261, 5.109226446042759579E-16 ) ) ;
#51470=CARTESIAN_POINT ( 'NONE',  ( 35.00384615384614762, 1.411358822780289120E-15, 0.000000000000000000 ) ) ;
#51493=DIRECTION ( 'NONE',  ( -1.000000000000000000, -1.224606353822377258E-16, -0.000000000000000000 ) ) ;
#51501=CIRCLE ( 'NONE', #92849, 5.000000000000001776 ) ;
#51538=FACE_OUTER_BOUND ( 'NONE', #3171, .T. ) ;
#51547=EDGE_CURVE ( 'NONE', #85853, #48371, #103726, .T. ) ;
#51550=FACE_OUTER_BOUND ( 'NONE', #15927, .T. ) ;
#51590=VERTEX_POINT ( 'NONE', #635 ) ;
#51604=EDGE_CURVE ( 'NONE', #47940, #58651, #84793, .T. ) ;
#51624=DIRECTION ( 'NONE',  ( 0.000000000000000000, 0.000000000000000000, 1.000000000000000000 ) ) ;
#51634=CARTESIAN_POINT ( 'NONE',  ( 28.50099738913158376, 1.340359594676612611E-15, 0.000000000000000000 ) ) ;
#51664=EDGE_CURVE ( 'NONE', #25507, #39953, #72690, .T. ) ;
#51675=AXIS2_PLACEMENT_3D ( 'NONE', #62664, #39966, #72325 ) ;
#51700=LINE ( 'NONE', #83538, #81135 ) ;
#51711=VERTEX_POINT ( 'NONE', #91639 ) ;
#51723=ORIENTED_EDGE ( 'NONE', *, *, #30910, .F. ) ;
#51741=CARTESIAN_POINT ( 'NONE',  ( 29.66054107240687543, 1.482358050883964840E-15, 0.000000000000000000 ) ) ;
#51742=ORIENTED_EDGE ( 'NONE', *, *, #50695, .T. ) ;
#51764=VERTEX_POINT ( 'NONE', #56535 ) ;
#51775=AXIS2_PLACEMENT_3D ( 'NONE', #33622, #74966, #16747 ) ;
#51806=EDGE_CURVE ( 'NONE', #51764, #88628, #55475, .T. ) ;
#51848=CARTESIAN_POINT ( 'NONE',  ( 23.73746414932995208, 1.482358050883964840E-15, 0.000000000000000000 ) ) ;
#51872=CARTESIAN_POINT ( 'NONE',  ( 34.10284876471455817, 5.000000000000002665, 0.000000000000000000 ) ) ;
#51908=CARTESIAN_POINT ( 'NONE',  ( 6.249999999999998224, 8.000000000000000000, 0.000000000000000000 ) ) ;
#51926=CARTESIAN_POINT ( 'NONE',  ( 42.40769230769231513, -4.171999999999999709, 5.616230220889763424E-16 ) ) ;
#51942=CARTESIAN_POINT ( 'NONE',  ( 43.88846153846154152, 1.411358822780289120E-15, 0.000000000000000000 ) ) ;
#51971=ORIENTED_EDGE ( 'NONE', *, *, #44167, .F. ) ;
#52001=ORIENTED_EDGE ( 'NONE', *, *, #38678, .F. ) ;
#52003=ORIENTED_EDGE ( 'NONE', *, *, #26695, .T. ) ;
#52008=ADVANCED_FACE ( 'NONE', ( #3105 ), #84565, .T. ) ;
#52021=CARTESIAN_POINT ( 'NONE',  ( 6.249999999999998224, -4.618802153517012954, -8.000000000000001776 ) ) ;
#52023=CARTESIAN_POINT ( 'NONE',  ( 9.830769230769229594, 1.411358822780289120E-15, 0.000000000000000000 ) ) ;
#52053=EDGE_CURVE ( 'NONE', #33830, #4002, #78573, .T. ) ;
#52066=ORIENTED_EDGE ( 'NONE', *, *, #91802, .T. ) ;
#52076=EDGE_LOOP ( 'NONE', ( #94196, #60835, #87145, #56976, #89785 ) ) ;
#52094=LINE ( 'NONE', #58607, #15540 ) ;
#52099=LINE ( 'NONE', #58059, #104238 ) ;
#52120=CARTESIAN_POINT ( 'NONE',  ( 12.79230769230769305, 1.411358822780289120E-15, 0.000000000000000000 ) ) ;
#52157=ADVANCED_FACE ( 'NONE', ( #23561 ), #7862, .F. ) ;
#52182=VERTEX_POINT ( 'NONE', #57470 ) ;
#52184=ADVANCED_FACE ( 'NONE', ( #50442 ), #43585, .T. ) ;
#52185=CARTESIAN_POINT ( 'NONE',  ( 38.86638200451619696, 0.000000000000000000, 5.000000000000002665 ) ) ;
#52197=AXIS2_PLACEMENT_3D ( 'NONE', #27834, #26762, #67716 ) ;
#52244=ORIENTED_EDGE ( 'NONE', *, *, #79892, .T. ) ;
#52256=DIRECTION ( 'NONE',  ( 0.000000000000000000, -1.000000000000000000, 0.000000000000000000 ) ) ;
#52280=AXIS2_PLACEMENT_3D ( 'NONE', #50992, #99008, #90956 ) ;
#52299=ORIENTED_EDGE ( 'NONE', *, *, #89325, .F. ) ;
#52308=LINE ( 'NONE', #85217, #53168 ) ;
#52312=EDGE_CURVE ( 'NONE', #76220, #56216, #81447, .T. ) ;
#52326=EDGE_CURVE ( 'NONE', #78717, #28015, #84941, .T. ) ;
#52329=ORIENTED_EDGE ( 'NONE', *, *, #89247, .F. ) ;
#52347=CARTESIAN_POINT ( 'NONE',  ( 23.73746414932995208, -5.000000000000000888, 6.123233995736769241E-16 ) ) ;
#52355=DIRECTION ( 'NONE',  ( 0.000000000000000000, -1.000000000000000000, 0.000000000000000000 ) ) ;
#52425=VERTEX_POINT ( 'NONE', #18523 ) ;
#52464=VERTEX_POINT ( 'NONE', #96640 ) ;
#52484=EDGE_CURVE ( 'NONE', #87039, #95821, #100409, .T. ) ;
#52503=AXIS2_PLACEMENT_3D ( 'NONE', #5145, #11620, #36491 ) ;
#52506=ORIENTED_EDGE ( 'NONE', *, *, #25561, .T. ) ;
#52512=VECTOR ( 'NONE', #84377, 1000.000000000000227 ) ;
#52517=ORIENTED_EDGE ( 'NONE', *, *, #53627, .T. ) ;
#52586=FACE_OUTER_BOUND ( 'NONE', #43182, .T. ) ;
#52598=DIRECTION ( 'NONE',  ( 0.000000000000000000, 0.000000000000000000, 1.000000000000000000 ) ) ;
#52605=ORIENTED_EDGE ( 'NONE', *, *, #79709, .F. ) ;
#52629=ORIENTED_EDGE ( 'NONE', *, *, #21622, .T. ) ;
#52637=CARTESIAN_POINT ( 'NONE',  ( 34.42407431220851066, -4.999999999999990230, 0.000000000000000000 ) ) ;
#52641=VECTOR ( 'NONE', #85166, 999.9999999999998863 ) ;
#52665=DIRECTION ( 'NONE',  ( -1.000000000000000000, -0.000000000000000000, -0.000000000000000000 ) ) ;
#52672=DIRECTION ( 'NONE',  ( 0.000000000000000000, -1.000000000000000000, 0.000000000000000000 ) ) ;
#52678=CARTESIAN_POINT ( 'NONE',  ( 29.08076923076923137, 1.411358822780289120E-15, 0.000000000000000000 ) ) ;
#52688=AXIS2_PLACEMENT_3D ( 'NONE', #50042, #16620, #9575 ) ;
#52694=DIRECTION ( 'NONE',  ( -1.000000000000000000, -1.224606353822377258E-16, -0.000000000000000000 ) ) ;
#52730=ORIENTED_EDGE ( 'NONE', *, *, #41088, .T. ) ;
#52794=ORIENTED_EDGE ( 'NONE', *, *, #50695, .F. ) ;
#52796=VECTOR ( 'NONE', #67699, 1000.000000000000000 ) ;
#52810=VECTOR ( 'NONE', #78860, 1000.000000000000000 ) ;
#52815=ORIENTED_EDGE ( 'NONE', *, *, #33202, .F. ) ;
#52828=ADVANCED_FACE ( 'NONE', ( #18136 ), #31612, .T. ) ;
#52849=ORIENTED_EDGE ( 'NONE', *, *, #55747, .T. ) ;
#52887=VECTOR ( 'NONE', #91064, 1000.000000000000000 ) ;
#52900=CARTESIAN_POINT ( 'NONE',  ( 14.85284876471456350, 5.000000000000003553, 0.000000000000000000 ) ) ;
#52913=CARTESIAN_POINT ( 'NONE',  ( 0.000000000000000000, 0.000000000000000000, 0.000000000000000000 ) ) ;
#52925=CIRCLE ( 'NONE', #89113, 5.000000000000004441 ) ;
#52952=CARTESIAN_POINT ( 'NONE',  ( 37.96538461538461462, 1.411358822780289120E-15, 0.000000000000000000 ) ) ;
#52953=ADVANCED_FACE ( 'NONE', ( #4067 ), #2294, .T. ) ;
#52978=B_SPLINE_CURVE_WITH_KNOTS ( 'NONE', 3,
 ( #63640, #26396, #66810, #49005, #41461, #106720 ),
 .UNSPECIFIED., .F., .F.,
 ( 4, 2, 4 ),
 ( 2.380731631042988191E-07, 0.002336973833157630128, 0.004673709593152156581 ),
 .UNSPECIFIED. ) ;
#52983=ORIENTED_EDGE ( 'NONE', *, *, #15113, .T. ) ;
#53020=ORIENTED_EDGE ( 'NONE', *, *, #46527, .T. ) ;
#53024=CARTESIAN_POINT ( 'NONE',  ( 46.02200000000003399, 0.000000000000000000, 0.000000000000000000 ) ) ;
#53057=VERTEX_POINT ( 'NONE', #96794 ) ;
#53079=AXIS2_PLACEMENT_3D ( 'NONE', #21507, #72150, #79177 ) ;
#53132=LINE ( 'NONE', #86049, #28851 ) ;
#53168=VECTOR ( 'NONE', #77125, 999.9999999999998863 ) ;
#53211=AXIS2_PLACEMENT_3D ( 'NONE', #91176, #7557, #90626 ) ;
#53234=ORIENTED_EDGE ( 'NONE', *, *, #73121, .F. ) ;
#53258=DIRECTION ( 'NONE',  ( 0.000000000000000000, 0.000000000000000000, 1.000000000000000000 ) ) ;
#53268=CARTESIAN_POINT ( 'NONE',  ( 0.000000000000000000, 0.000000000000000000, 5.000000000000002665 ) ) ;
#53274=DIRECTION ( 'NONE',  ( -1.000000000000000000, -0.000000000000000000, -0.000000000000000000 ) ) ;
#53278=VERTEX_POINT ( 'NONE', #49274 ) ;
#53333=AXIS2_PLACEMENT_3D ( 'NONE', #87297, #54902, #13379 ) ;
#53346=AXIS2_PLACEMENT_3D ( 'NONE', #52023, #18085, #100572 ) ;
#53347=B_SPLINE_CURVE_WITH_KNOTS ( 'NONE', 3,
 ( #95404, #86277, #68487, #19971, #43661, #102970 ),
 .UNSPECIFIED., .F., .F.,
 ( 4, 2, 4 ),
 ( 2.380731629569644788E-07, 0.002336973833157563341, 0.004673709593152168724 ),
 .UNSPECIFIED. ) ;
#53348=DIRECTION ( 'NONE',  ( -1.000000000000000000, -1.224606353822377258E-16, -0.000000000000000000 ) ) ;
#53355=CARTESIAN_POINT ( 'NONE',  ( 44.78945892759311675, -5.000000000000009770, 0.000000000000000000 ) ) ;
#53359=EDGE_CURVE ( 'NONE', #30449, #26965, #7301, .T. ) ;
#53399=FACE_OUTER_BOUND ( 'NONE', #84342, .T. ) ;
#53407=ORIENTED_EDGE ( 'NONE', *, *, #59961, .F. ) ;
#53441=DIRECTION ( 'NONE',  ( -1.000000000000000000, -1.224606353822377258E-16, -0.000000000000000000 ) ) ;
#53465=ORIENTED_EDGE ( 'NONE', *, *, #39569, .T. ) ;
#53481=VECTOR ( 'NONE', #64163, 1000.000000000000227 ) ;
#53488=CARTESIAN_POINT ( 'NONE',  ( 24.05868969682389036, 1.340359594676612611E-15, 0.000000000000000000 ) ) ;
#53537=AXIS2_PLACEMENT_3D ( 'NONE', #12926, #29180, #20573 ) ;
#53590=AXIS2_PLACEMENT_3D ( 'NONE', #99729, #41487, #66299 ) ;
#53593=DIRECTION ( 'NONE',  ( -1.000000000000000000, -0.000000000000000000, -0.000000000000000000 ) ) ;
#53627=EDGE_CURVE ( 'NONE', #48268, #7084, #8570, .T. ) ;
#53633=CONICAL_SURFACE ( 'NONE', #39860, 5.000000000000001776, 0.9599310885968803664 ) ;
#53658=DIRECTION ( 'NONE',  ( -0.5735764363510510444, -0.8191520442889883569, 0.000000000000000000 ) ) ;
#53667=LINE ( 'NONE', #46636, #98078 ) ;
#53675=AXIS2_PLACEMENT_3D ( 'NONE', #5327, #14985, #104000 ) ;
#53695=AXIS2_PLACEMENT_3D ( 'NONE', #52678, #93692, #103373 ) ;
#53697=ORIENTED_EDGE ( 'NONE', *, *, #32270, .F. ) ;
#53787=ORIENTED_EDGE ( 'NONE', *, *, #55995, .T. ) ;
#53840=ORIENTED_EDGE ( 'NONE', *, *, #11140, .T. ) ;
#53842=ORIENTED_EDGE ( 'NONE', *, *, #97176, .T. ) ;
#53880=DIRECTION ( 'NONE',  ( -1.000000000000000000, -0.000000000000000000, -0.000000000000000000 ) ) ;
#53914=ORIENTED_EDGE ( 'NONE', *, *, #56125, .F. ) ;
#53965=EDGE_CURVE ( 'NONE', #25469, #8540, #43578, .T. ) ;
#53997=CIRCLE ( 'NONE', #67811, 4.172000000000001485 ) ;
#53998=DIRECTION ( 'NONE',  ( 0.000000000000000000, -1.000000000000000000, 0.000000000000000000 ) ) ;
#54000=CARTESIAN_POINT ( 'NONE',  ( 32.04230769230768772, 1.411358822780289120E-15, 0.000000000000000000 ) ) ;
#54066=EDGE_CURVE ( 'NONE', #73855, #33037, #12536, .T. ) ;
#54068=( GEOMETRIC_REPRESENTATION_CONTEXT ( 3 ) GLOBAL_UNCERTAINTY_ASSIGNED_CONTEXT ( ( #16539 ) ) GLOBAL_UNIT_ASSIGNED_CONTEXT ( ( #17816, #58807, #50163 ) ) REPRESENTATION_CONTEXT ( 'NONE', 'WORKASPACE' ) );
#54093=EDGE_CURVE ( 'NONE', #81027, #9677, #65978, .T. ) ;
#54125=DIRECTION ( 'NONE',  ( 0.000000000000000000, -1.000000000000000000, 0.000000000000000000 ) ) ;
#54152=DIRECTION ( 'NONE',  ( -0.5735764363510512664, 0.8191520442889881348, 1.003171929053520309E-16 ) ) ;
#54168=ORIENTED_EDGE ( 'NONE', *, *, #94440, .F. ) ;
#54175=PRODUCT_DEFINITION ( 'UNKNOWN', '', #2496, #31687 ) ;
#54186=ORIENTED_EDGE ( 'NONE', *, *, #9734, .T. ) ;
#54192=DIRECTION ( 'NONE',  ( -1.000000000000000000, -1.224606353822377258E-16, -0.000000000000000000 ) ) ;
#54219=EDGE_CURVE ( 'NONE', #79952, #43184, #24663, .T. ) ;
#54226=DIRECTION ( 'NONE',  ( 0.000000000000000000, -0.8660254037844382635, -0.5000000000000008882 ) ) ;
#54229=CYLINDRICAL_SURFACE ( 'NONE', #41512, 5.000000000000002665 ) ;
#54238=VERTEX_POINT ( 'NONE', #90437 ) ;
#54253=VECTOR ( 'NONE', #14178, 1000.000000000000227 ) ;
#54294=CYLINDRICAL_SURFACE ( 'NONE', #39056, 5.000000000000002665 ) ;
#54295=DIRECTION ( 'NONE',  ( 0.000000000000000000, -1.000000000000000000, 0.000000000000000000 ) ) ;
#54310=CARTESIAN_POINT ( 'NONE',  ( 17.81438722625302518, 5.000000000000003553, 0.000000000000000000 ) ) ;
#54312=DIRECTION ( 'NONE',  ( 0.5735764363510468256, 0.8191520442889913545, 0.000000000000000000 ) ) ;
#54317=CYLINDRICAL_SURFACE ( 'NONE', #91326, 5.000000000000002665 ) ;
#54320=VERTEX_POINT ( 'NONE', #51019 ) ;
#54333=AXIS2_PLACEMENT_3D ( 'NONE', #65443, #56801, #89727 ) ;
#54337=DIRECTION ( 'NONE',  ( -1.000000000000000000, -0.000000000000000000, -0.000000000000000000 ) ) ;
#54342=LINE ( 'NONE', #96441, #95540 ) ;
#54353=DIRECTION ( 'NONE',  ( -1.000000000000000000, -1.224606353822377258E-16, -0.000000000000000000 ) ) ;
#54362=ORIENTED_EDGE ( 'NONE', *, *, #58663, .F. ) ;
#54370=DIRECTION ( 'NONE',  ( 0.000000000000000000, -1.000000000000000000, 0.000000000000000000 ) ) ;
#54409=ORIENTED_EDGE ( 'NONE', *, *, #1301, .T. ) ;
#54428=ORIENTED_EDGE ( 'NONE', *, *, #13163, .F. ) ;
#54433=LINE ( 'NONE', #46893, #73643 ) ;
#54445=ORIENTED_EDGE ( 'NONE', *, *, #36894, .T. ) ;
#54478=AXIS2_PLACEMENT_3D ( 'NONE', #46686, #54226, #96322 ) ;
#54498=AXIS2_PLACEMENT_3D ( 'NONE', #43777, #76665, #65928 ) ;
#54534=CARTESIAN_POINT ( 'NONE',  ( 44.78945892759311675, 1.340359594676612611E-15, 0.000000000000000000 ) ) ;
#54606=DIRECTION ( 'NONE',  ( -1.000000000000000000, -1.224606353822377258E-16, -0.000000000000000000 ) ) ;
#54610=DIRECTION ( 'NONE',  ( -1.000000000000000000, -1.224606353822377258E-16, -0.000000000000000000 ) ) ;
#54629=CARTESIAN_POINT ( 'NONE',  ( 25.53945892759312031, 1.340359594676612611E-15, 0.000000000000000000 ) ) ;
#54659=DIRECTION ( 'NONE',  ( 0.000000000000000000, -1.000000000000000000, 0.000000000000000000 ) ) ;
#54666=EDGE_LOOP ( 'NONE', ( #83967, #68986, #14962, #89143, #29867, #60994 ) ) ;
#54669=CIRCLE ( 'NONE', #4726, 4.172000000000001485 ) ;
#54697=DIRECTION ( 'NONE',  ( -1.000000000000000000, -1.224606353822377258E-16, -0.000000000000000000 ) ) ;
#54731=EDGE_LOOP ( 'NONE', ( #37808, #70137, #103587, #32442, #41688, #55469 ) ) ;
#54751=CARTESIAN_POINT ( 'NONE',  ( 20.19615384615384457, 1.411358822780289120E-15, 0.000000000000000000 ) ) ;
#54756=ORIENTED_EDGE ( 'NONE', *, *, #18507, .T. ) ;
#54762=CARTESIAN_POINT ( 'NONE',  ( 44.46823338009918558, -5.000000000000000888, 6.123233995736769241E-16 ) ) ;
#54771=CYLINDRICAL_SURFACE ( 'NONE', #63904, 5.000000000000002665 ) ;
#54782=DIRECTION ( 'NONE',  ( 0.000000000000000000, -1.000000000000000000, 0.000000000000000000 ) ) ;
#54794=CIRCLE ( 'NONE', #78980, 5.000000000000002665 ) ;
#54826=ADVANCED_FACE ( 'NONE', ( #20806 ), #85085, .T. ) ;
#54851=ORIENTED_EDGE ( 'NONE', *, *, #13664, .T. ) ;
#54857=CARTESIAN_POINT ( 'NONE',  ( 13.69330508143927538, 1.340359594676612611E-15, 0.000000000000000000 ) ) ;
#54892=CARTESIAN_POINT ( 'NONE',  ( 14.85284876471456350, 1.482358050883964840E-15, 0.000000000000000000 ) ) ;
#54902=DIRECTION ( 'NONE',  ( -1.000000000000000000, -1.224606353822377258E-16, -0.000000000000000000 ) ) ;
#54910=VERTEX_POINT ( 'NONE', #22896 ) ;
#54943=ORIENTED_EDGE ( 'NONE', *, *, #37072, .F. ) ;
#54977=AXIS2_PLACEMENT_3D ( 'NONE', #2117, #26987, #93280 ) ;
#54985=ORIENTED_EDGE ( 'NONE', *, *, #102067, .F. ) ;
#55009=CARTESIAN_POINT ( 'NONE',  ( 15.75384615384615294, 1.411358822780289120E-15, 0.000000000000000000 ) ) ;
#55017=CARTESIAN_POINT ( 'NONE',  ( 0.000000000000000000, 6.123233995736770227E-16, -5.000000000000002665 ) ) ;
#55024=ADVANCED_FACE ( 'NONE', ( #35231 ), #67052, .T. ) ;
#55031=AXIS2_PLACEMENT_3D ( 'NONE', #42926, #50463, #83373 ) ;
#55056=CIRCLE ( 'NONE', #68884, 5.000000000000001776 ) ;
#55067=FACE_OUTER_BOUND ( 'NONE', #89886, .T. ) ;
#55080=EDGE_LOOP ( 'NONE', ( #17010, #83818, #87559, #84606, #42621, #31968 ) ) ;
#55096=EDGE_CURVE ( 'NONE', #69241, #46447, #48867, .T. ) ;
#55129=VECTOR ( 'NONE', #64464, 1000.000000000000000 ) ;
#55132=EDGE_CURVE ( 'NONE', #48079, #106696, #4967, .T. ) ;
#55144=VERTEX_POINT ( 'NONE', #21706 ) ;
#55157=CARTESIAN_POINT ( 'NONE',  ( 20.19615384615384457, -4.171999999999999709, 5.616230220889763424E-16 ) ) ;
#55161=VERTEX_POINT ( 'NONE', #46483 ) ;
#55170=DIRECTION ( 'NONE',  ( 1.000000000000000000, 0.000000000000000000, 0.000000000000000000 ) ) ;
#55176=ORIENTED_EDGE ( 'NONE', *, *, #40524, .F. ) ;
#55225=CONICAL_SURFACE ( 'NONE', #104980, 5.000000000000001776, 0.9599310885968803664 ) ;
#55245=ORIENTED_EDGE ( 'NONE', *, *, #76092, .F. ) ;
#55267=CARTESIAN_POINT ( 'NONE',  ( 0.7145311798163270778, 9.237604307034018802, 2.885982852862873934E-16 ) ) ;
#55270=MANIFOLD_SOLID_BREP ( 'ThdSchPat', #75632 ) ;
#55285=CIRCLE ( 'NONE', #57051, 5.000000000000001776 ) ;
#55310=EDGE_CURVE ( 'NONE', #3257, #54238, #95470, .T. ) ;
#55331=DIRECTION ( 'NONE',  ( -1.000000000000000000, -1.224606353822377258E-16, -0.000000000000000000 ) ) ;
#55359=AXIS2_PLACEMENT_3D ( 'NONE', #60333, #88827, #89370 ) ;
#55362=CIRCLE ( 'NONE', #22698, 5.000000000000001776 ) ;
#55395=VERTEX_POINT ( 'NONE', #26495 ) ;
#55411=ORIENTED_EDGE ( 'NONE', *, *, #90889, .F. ) ;
#55412=ORIENTED_EDGE ( 'NONE', *, *, #68196, .T. ) ;
#55418=CARTESIAN_POINT ( 'NONE',  ( 25.21823338009918203, 1.482358050883964840E-15, 0.000000000000000000 ) ) ;
#55421=CARTESIAN_POINT ( 'NONE',  ( 31.14131030317610538, 1.482358050883964840E-15, 0.000000000000000000 ) ) ;
#55423=CARTESIAN_POINT ( 'NONE',  ( 29.98176661990081371, 1.340359594676612611E-15, 0.000000000000000000 ) ) ;
#55469=ORIENTED_EDGE ( 'NONE', *, *, #17952, .F. ) ;
#55475=B_SPLINE_CURVE_WITH_KNOTS ( 'NONE', 3,
 ( #47913, #5364, #6933, #62538, #39856, #89466, #4826, #13424 ),
 .UNSPECIFIED., .F., .F.,
 ( 4, 2, 2, 4 ),
 ( 0.004673709593152168724, 0.005837709341827655544, 0.007001709090503143232, 0.009329708587854116872 ),
 .UNSPECIFIED. ) ;
#55495=ORIENTED_EDGE ( 'NONE', *, *, #1342, .T. ) ;
#55523=DIRECTION ( 'NONE',  ( -1.000000000000000000, -1.224606353822377258E-16, -0.000000000000000000 ) ) ;
#55599=CARTESIAN_POINT ( 'NONE',  ( 37.06438722625302518, 1.482358050883964840E-15, 0.000000000000000000 ) ) ;
#55607=CARTESIAN_POINT ( 'NONE',  ( 25.21823338009918203, 5.000000000000003553, 0.000000000000000000 ) ) ;
#55623=CARTESIAN_POINT ( 'NONE',  ( 44.78945892759311675, 1.340359594676612611E-15, 0.000000000000000000 ) ) ;
#55630=ORIENTED_EDGE ( 'NONE', *, *, #90793, .T. ) ;
#55644=DIRECTION ( 'NONE',  ( 0.000000000000000000, 1.000000000000000000, 0.000000000000000000 ) ) ;
#55654=CIRCLE ( 'NONE', #86737, 5.000000000000002665 ) ;
#55671=AXIS2_PLACEMENT_3D ( 'NONE', #103735, #53593, #19681 ) ;
#55689=CARTESIAN_POINT ( 'NONE',  ( 36.48461538461538822, 4.172000000000003261, 5.109226446042759579E-16 ) ) ;
#55692=ORIENTED_EDGE ( 'NONE', *, *, #64545, .T. ) ;
#55746=DIRECTION ( 'NONE',  ( -1.000000000000000000, -1.224606353822377258E-16, -0.000000000000000000 ) ) ;
#55747=EDGE_CURVE ( 'NONE', #39953, #14796, #58014, .T. ) ;
#55792=DIRECTION ( 'NONE',  ( 0.000000000000000000, -1.000000000000000000, 0.000000000000000000 ) ) ;
#55822=EDGE_LOOP ( 'NONE', ( #50397, #42644, #53465, #56053, #2909, #47643 ) ) ;
#55856=CIRCLE ( 'NONE', #47595, 5.000000000000002665 ) ;
#55868=EDGE_CURVE ( 'NONE', #98655, #65067, #35297, .T. ) ;
#55878=DIRECTION ( 'NONE',  ( -1.000000000000000000, -1.224606353822377258E-16, -0.000000000000000000 ) ) ;
#55881=CARTESIAN_POINT ( 'NONE',  ( 0.000000000000000000, 0.000000000000000000, 5.000000000000002665 ) ) ;
#55918=DIRECTION ( 'NONE',  ( 0.000000000000000000, -1.000000000000000000, 0.000000000000000000 ) ) ;
#55925=CIRCLE ( 'NONE', #97288, 5.000000000000002665 ) ;
#55944=LINE ( 'NONE', #98027, #103950 ) ;
#55948=CIRCLE ( 'NONE', #64614, 5.000000000000001776 ) ;
#55966=EDGE_CURVE ( 'NONE', #86773, #48676, #26683, .T. ) ;
#55973=ORIENTED_EDGE ( 'NONE', *, *, #22873, .F. ) ;
#55980=DIRECTION ( 'NONE',  ( 0.000000000000000000, -1.000000000000000000, 0.000000000000000000 ) ) ;
#55995=EDGE_CURVE ( 'NONE', #83974, #57077, #67982, .T. ) ;
#56015=VERTEX_POINT ( 'NONE', #69199 ) ;
#56019=ORIENTED_EDGE ( 'NONE', *, *, #95544, .T. ) ;
#56045=LINE ( 'NONE', #79289, #59462 ) ;
#56053=ORIENTED_EDGE ( 'NONE', *, *, #14830, .F. ) ;
#56082=DIRECTION ( 'NONE',  ( 0.000000000000000000, -1.000000000000000000, 0.000000000000000000 ) ) ;
#56104=DIRECTION ( 'NONE',  ( -1.000000000000000000, -1.224606353822377258E-16, -0.000000000000000000 ) ) ;
#56121=ORIENTED_EDGE ( 'NONE', *, *, #33718, .T. ) ;
#56124=ORIENTED_EDGE ( 'NONE', *, *, #102924, .T. ) ;
#56125=EDGE_CURVE ( 'NONE', #7878, #19325, #33516, .T. ) ;
#56151=AXIS2_PLACEMENT_3D ( 'NONE', #52120, #105971, #7277 ) ;
#56172=AXIS2_PLACEMENT_3D ( 'NONE', #60951, #94383, #29154 ) ;
#56207=ORIENTED_EDGE ( 'NONE', *, *, #45008, .F. ) ;
#56214=CARTESIAN_POINT ( 'NONE',  ( 0.000000000000000000, 0.000000000000000000, 5.000000000000002665 ) ) ;
#56216=VERTEX_POINT ( 'NONE', #8153 ) ;
#56231=AXIS2_PLACEMENT_3D ( 'NONE', #1873, #76303, #33752 ) ;
#56246=AXIS2_PLACEMENT_3D ( 'NONE', #74480, #555, #66396 ) ;
#56262=CARTESIAN_POINT ( 'NONE',  ( 21.09715123528542691, 1.340359594676612611E-15, 0.000000000000000000 ) ) ;
#56318=ORIENTED_EDGE ( 'NONE', *, *, #65516, .T. ) ;
#56351=CARTESIAN_POINT ( 'NONE',  ( 12.21253585067004543, 0.000000000000000000, 5.000000000000002665 ) ) ;
#56363=CARTESIAN_POINT ( 'NONE',  ( 23.73746414932995208, -5.000000000000000000, 6.123233995736768255E-16 ) ) ;
#56368=EDGE_CURVE ( 'NONE', #85320, #41603, #104239, .T. ) ;
#56408=CIRCLE ( 'NONE', #23746, 5.000000000000001776 ) ;
#56410=EDGE_CURVE ( 'NONE', #55161, #58381, #43712, .T. ) ;
#56414=VECTOR ( 'NONE', #45947, 1000.000000000000114 ) ;
#56431=VECTOR ( 'NONE', #2999, 1000.000000000000227 ) ;
#56459=LINE ( 'NONE', #44825, #48211 ) ;
#56523=PLANE ( 'NONE',  #43146 ) ;
#56535=CARTESIAN_POINT ( 'NONE',  ( 0.000000000000000000, 6.928203230275505220, -4.000000000000007994 ) ) ;
#56539=ADVANCED_FACE ( 'NONE', ( #59790 ), #11196, .T. ) ;
#56546=CIRCLE ( 'NONE', #104771, 5.000000000000001776 ) ;
#56554=AXIS2_PLACEMENT_3D ( 'NONE', #87578, #72440, #37997 ) ;
#56615=DIRECTION ( 'NONE',  ( -1.000000000000000000, -0.000000000000000000, -0.000000000000000000 ) ) ;
#56640=VERTEX_POINT ( 'NONE', #59254 ) ;
#56663=DIRECTION ( 'NONE',  ( 0.000000000000000000, -1.000000000000000000, 0.000000000000000000 ) ) ;
#56676=FILL_AREA_STYLE_COLOUR ( '', #97146 ) ;
#56714=ORIENTED_EDGE ( 'NONE', *, *, #55868, .T. ) ;
#56724=CARTESIAN_POINT ( 'NONE',  ( 26.69900261086841198, -5.000000000000000888, 6.123233995736769241E-16 ) ) ;
#56728=VECTOR ( 'NONE', #78473, 999.9999999999998863 ) ;
#56797=DIRECTION ( 'NONE',  ( -1.000000000000000000, -1.224606353822377258E-16, -0.000000000000000000 ) ) ;
#56801=DIRECTION ( 'NONE',  ( -1.000000000000000000, -1.224606353822377258E-16, -0.000000000000000000 ) ) ;
#56805=ORIENTED_EDGE ( 'NONE', *, *, #69466, .F. ) ;
#56807=DIRECTION ( 'NONE',  ( -1.000000000000000000, -1.224606353822377258E-16, -0.000000000000000000 ) ) ;
#56829=DIRECTION ( 'NONE',  ( -1.000000000000000000, -1.224606353822377258E-16, -0.000000000000000000 ) ) ;
#56830=ORIENTED_EDGE ( 'NONE', *, *, #31632, .T. ) ;
#56867=LINE ( 'NONE', #48771, #56949 ) ;
#56875=CARTESIAN_POINT ( 'NONE',  ( 18.71538461538461462, -4.171999999999999709, 5.616230220889763424E-16 ) ) ;
#56907=CARTESIAN_POINT ( 'NONE',  ( 37.38561277374697056, 1.340359594676612611E-15, 0.000000000000000000 ) ) ;
#56909=AXIS2_PLACEMENT_3D ( 'NONE', #46545, #54606, #30385 ) ;
#56924=VECTOR ( 'NONE', #9167, 999.9999999999998863 ) ;
#56932=CARTESIAN_POINT ( 'NONE',  ( 26.69900261086841198, 3.851859888774471706E-31, 5.000000000000001776 ) ) ;
#56947=CONICAL_SURFACE ( 'NONE', #53590, 4.172000000000001485, 0.9599310885968750373 ) ;
#56949=VECTOR ( 'NONE', #7786, 999.9999999999998863 ) ;
#56976=ORIENTED_EDGE ( 'NONE', *, *, #97659, .F. ) ;
#56979=CIRCLE ( 'NONE', #29484, 5.000000000000001776 ) ;
#56990=EDGE_CURVE ( 'NONE', #94292, #41603, #89369, .T. ) ;
#56995=CYLINDRICAL_SURFACE ( 'NONE', #82639, 5.000000000000002665 ) ;
#57013=LINE ( 'NONE', #23627, #26666 ) ;
#57015=DIRECTION ( 'NONE',  ( 0.000000000000000000, 0.000000000000000000, 1.000000000000000000 ) ) ;
#57019=CARTESIAN_POINT ( 'NONE',  ( 0.000000000000000000, 0.000000000000000000, 0.000000000000000000 ) ) ;
#57033=DIRECTION ( 'NONE',  ( 0.000000000000000000, 0.000000000000000000, 1.000000000000000000 ) ) ;
#57051=AXIS2_PLACEMENT_3D ( 'NONE', #25515, #24454, #8221 ) ;
#57054=CIRCLE ( 'NONE', #74230, 5.000000000000002665 ) ;
#57077=VERTEX_POINT ( 'NONE', #59535 ) ;
#57082=CARTESIAN_POINT ( 'NONE',  ( 13.37207953394533355, 1.482358050883964840E-15, 0.000000000000000000 ) ) ;
#57087=CARTESIAN_POINT ( 'NONE',  ( 11.31153846153846132, 4.172000000000003261, 0.000000000000000000 ) ) ;
#57168=EDGE_CURVE ( 'NONE', #7878, #37991, #11376, .T. ) ;
#57214=VERTEX_POINT ( 'NONE', #69223 ) ;
#57218=ADVANCED_FACE ( 'NONE', ( #102091 ), #59606, .T. ) ;
#57373=CIRCLE ( 'NONE', #19571, 5.000000000000002665 ) ;
#57394=VERTEX_POINT ( 'NONE', #98247 ) ;
#57397=CARTESIAN_POINT ( 'NONE',  ( 36.48461538461538822, 4.172000000000003261, 0.000000000000000000 ) ) ;
#57455=FACE_OUTER_BOUND ( 'NONE', #59640, .T. ) ;
#57458=LINE ( 'NONE', #18105, #80977 ) ;
#57470=CARTESIAN_POINT ( 'NONE',  ( 28.50099738913158376, 0.000000000000000000, 5.000000000000002665 ) ) ;
#57516=CARTESIAN_POINT ( 'NONE',  ( 0.000000000000000000, 6.123233995736770227E-16, -5.000000000000002665 ) ) ;
#57532=DIRECTION ( 'NONE',  ( 0.000000000000000000, -1.000000000000000000, 0.000000000000000000 ) ) ;
#57537=CARTESIAN_POINT ( 'NONE',  ( 0.08285530294364991388, 1.570896314703519092, -8.000000000000000000 ) ) ;
#57539=DIRECTION ( 'NONE',  ( -1.000000000000000000, -0.000000000000000000, -0.000000000000000000 ) ) ;
#57569=EDGE_CURVE ( 'NONE', #12793, #8878, #40724, .T. ) ;
#57617=AXIS2_PLACEMENT_3D ( 'NONE', #65636, #8978, #24669 ) ;
#57631=ADVANCED_FACE ( 'NONE', ( #1476 ), #63142, .T. ) ;
#57638=ORIENTED_EDGE ( 'NONE', *, *, #77238, .T. ) ;
#57651=AXIS2_PLACEMENT_3D ( 'NONE', #37070, #12745, #93148 ) ;
#57677=DIRECTION ( 'NONE',  ( -1.000000000000000000, -0.000000000000000000, -0.000000000000000000 ) ) ;
#57697=FACE_OUTER_BOUND ( 'NONE', #83391, .T. ) ;
#57713=CONICAL_SURFACE ( 'NONE', #12910, 4.172000000000001485, 0.9599310885968750373 ) ;
#57744=ORIENTED_EDGE ( 'NONE', *, *, #98771, .F. ) ;
#57758=ADVANCED_FACE ( 'NONE', ( #12890 ), #82045, .T. ) ;
#57781=DIRECTION ( 'NONE',  ( -1.000000000000000000, -0.000000000000000000, -0.000000000000000000 ) ) ;
#57801=CARTESIAN_POINT ( 'NONE',  ( 0.7145311798163198613, -4.618802153516998743, 7.999999999999998224 ) ) ;
#57811=AXIS2_PLACEMENT_3D ( 'NONE', #98831, #33087, #40610 ) ;
#57830=CARTESIAN_POINT ( 'NONE',  ( 11.89131030317610183, 1.482358050883964840E-15, 0.000000000000000000 ) ) ;
#57851=VECTOR ( 'NONE', #69977, 1000.000000000000000 ) ;
#57854=EDGE_LOOP ( 'NONE', ( #104770, #98884, #6133, #62361, #65938, #35529 ) ) ;
#57878=ORIENTED_EDGE ( 'NONE', *, *, #51003, .T. ) ;
#57882=CARTESIAN_POINT ( 'NONE',  ( 40.34715123528543046, 5.000000000000015099, 6.123233995736782060E-16 ) ) ;
#57883=EDGE_CURVE ( 'NONE', #93742, #17674, #29147, .T. ) ;
#57889=FACE_OUTER_BOUND ( 'NONE', #49515, .T. ) ;
#57892=ADVANCED_FACE ( 'NONE', ( #87342 ), #87236, .T. ) ;
#57925=ADVANCED_FACE ( 'NONE', ( #77651 ), #68299, .T. ) ;
#57931=CARTESIAN_POINT ( 'NONE',  ( 45.94900261086841198, 1.482358050883964840E-15, 0.000000000000000000 ) ) ;
#57933=DIRECTION ( 'NONE',  ( -1.000000000000000000, -1.224606353822377258E-16, -0.000000000000000000 ) ) ;
#57941=ORIENTED_EDGE ( 'NONE', *, *, #17952, .T. ) ;
#57967=AXIS2_PLACEMENT_3D ( 'NONE', #4722, #31149, #64036 ) ;
#57976=EDGE_CURVE ( 'NONE', #68447, #56015, #6285, .T. ) ;
#57978=DIRECTION ( 'NONE',  ( -1.000000000000000000, -1.224606353822377258E-16, -0.000000000000000000 ) ) ;
#57986=FACE_OUTER_BOUND ( 'NONE', #40505, .T. ) ;
#58014=LINE ( 'NONE', #91989, #78295 ) ;
#58041=EDGE_CURVE ( 'NONE', #79135, #83753, #58138, .T. ) ;
#58059=CARTESIAN_POINT ( 'NONE',  ( 17.81438722625302518, -5.000000000000000000, 6.123233995736768255E-16 ) ) ;
#58062=ADVANCED_FACE ( 'NONE', ( #80278 ), #45964, .T. ) ;
#58064=DIRECTION ( 'NONE',  ( 0.000000000000000000, -1.000000000000000000, 0.000000000000000000 ) ) ;
#58072=DIRECTION ( 'NONE',  ( 0.000000000000000000, -1.000000000000000000, 0.000000000000000000 ) ) ;
#58090=CARTESIAN_POINT ( 'NONE',  ( 0.000000000000000000, 6.123233995736770227E-16, -5.000000000000002665 ) ) ;
#58099=DIRECTION ( 'NONE',  ( -1.000000000000000000, -0.000000000000000000, -0.000000000000000000 ) ) ;
#58112=EDGE_CURVE ( 'NONE', #21850, #97131, #34445, .T. ) ;
#58131=CARTESIAN_POINT ( 'NONE',  ( 6.249999999999998224, 8.000000000000000000, 0.000000000000000000 ) ) ;
#58138=LINE ( 'NONE', #39851, #52887 ) ;
#58180=DIRECTION ( 'NONE',  ( 0.000000000000000000, -1.000000000000000000, 0.000000000000000000 ) ) ;
#58184=CARTESIAN_POINT ( 'NONE',  ( 25.53945892759312031, 1.340359594676612611E-15, 0.000000000000000000 ) ) ;
#58193=VERTEX_POINT ( 'NONE', #50043 ) ;
#58196=CARTESIAN_POINT ( 'NONE',  ( 35.58361799548379167, -5.000000000000000000, 6.123233995736768255E-16 ) ) ;
#58201=ADVANCED_FACE ( 'NONE', ( #82953 ), #25357, .T. ) ;
#58204=FACE_OUTER_BOUND ( 'NONE', #99480, .T. ) ;
#58211=VERTEX_POINT ( 'NONE', #50559 ) ;
#58243=CIRCLE ( 'NONE', #85850, 5.000000000000001776 ) ;
#58255=SURFACE_SIDE_STYLE ('',( #50668 ) ) ;
#58260=DIRECTION ( 'NONE',  ( -1.000000000000000000, -1.224606353822377258E-16, -0.000000000000000000 ) ) ;
#58275=CIRCLE ( 'NONE', #11693, 5.000000000000001776 ) ;
#58308=CARTESIAN_POINT ( 'NONE',  ( 0.000000000000000000, -6.928203230275503444, 4.000000000000010658 ) ) ;
#58344=CONICAL_SURFACE ( 'NONE', #75587, 4.172000000000001485, 0.9599310885968750373 ) ;
#58381=VERTEX_POINT ( 'NONE', #37099 ) ;
#58403=AXIS2_PLACEMENT_3D ( 'NONE', #13630, #69247, #5551 ) ;
#58423=CARTESIAN_POINT ( 'NONE',  ( 26.69900261086841198, 5.000000000000003553, 0.000000000000000000 ) ) ;
#58471=CIRCLE ( 'NONE', #36110, 5.000000000000001776 ) ;
#58481=AXIS2_PLACEMENT_3D ( 'NONE', #88579, #78884, #30905 ) ;
#58498=VERTEX_POINT ( 'NONE', #56932 ) ;
#58504=DIRECTION ( 'NONE',  ( -1.000000000000000000, -1.224606353822377258E-16, -0.000000000000000000 ) ) ;
#58509=CIRCLE ( 'NONE', #8513, 5.000000000000001776 ) ;
#58549=AXIS2_PLACEMENT_3D ( 'NONE', #12699, #21371, #47718 ) ;
#58563=DIRECTION ( 'NONE',  ( -0.5735764363510510444, -0.8191520442889883569, 0.000000000000000000 ) ) ;
#58575=EDGE_LOOP ( 'NONE', ( #97152, #49296, #97285, #26510, #18565, #66592 ) ) ;
#58607=CARTESIAN_POINT ( 'NONE',  ( 6.249999999999998224, 4.618802153517004960, 7.999999999999998224 ) ) ;
#58619=ORIENTED_EDGE ( 'NONE', *, *, #59961, .T. ) ;
#58651=VERTEX_POINT ( 'NONE', #60697 ) ;
#58659=FACE_OUTER_BOUND ( 'NONE', #79319, .T. ) ;
#58663=EDGE_CURVE ( 'NONE', #13600, #47858, #44503, .T. ) ;
#58666=VECTOR ( 'NONE', #45760, 999.9999999999998863 ) ;
#58701=ORIENTED_EDGE ( 'NONE', *, *, #27110, .T. ) ;
#58716=ORIENTED_EDGE ( 'NONE', *, *, #26863, .F. ) ;
#58781=CARTESIAN_POINT ( 'NONE',  ( 31.14131030317610538, 1.482358050883964840E-15, 0.000000000000000000 ) ) ;
#58787=DIRECTION ( 'NONE',  ( 1.000000000000000000, 1.224606353822377258E-16, 0.000000000000000000 ) ) ;
#58791=EDGE_CURVE ( 'NONE', #94292, #36949, #83991, .T. ) ;
#58807=( NAMED_UNIT ( * ) PLANE_ANGLE_UNIT ( ) SI_UNIT ( $, .RADIAN. ) );
#58823=CARTESIAN_POINT ( 'NONE',  ( 0.06730325657896424341, -1.557442666625489025, 7.999999999999996447 ) ) ;
#58838=CARTESIAN_POINT ( 'NONE',  ( 28.17977184163764193, 1.482358050883964840E-15, 0.000000000000000000 ) ) ;
#58842=DIRECTION ( 'NONE',  ( -1.000000000000000000, -1.224606353822377258E-16, -0.000000000000000000 ) ) ;
#58852=B_SPLINE_CURVE_WITH_KNOTS ( 'NONE', 3,
 ( #40157, #98391, #104356, #30504, #96298, #31570, #105943, #55267 ),
 .UNSPECIFIED., .F., .F.,
 ( 4, 2, 2, 4 ),
 ( 0.004673709593152147908, 0.005837709341827639065, 0.007001709090503129354, 0.009329708587854111668 ),
 .UNSPECIFIED. ) ;
#58873=ORIENTED_EDGE ( 'NONE', *, *, #74065, .F. ) ;
#58886=LINE ( 'NONE', #91777, #9945 ) ;
#58895=VECTOR ( 'NONE', #58563, 1000.000000000000000 ) ;
#58898=LINE ( 'NONE', #99317, #88289 ) ;
#58915=CYLINDRICAL_SURFACE ( 'NONE', #95431, 5.000000000000002665 ) ;
#58921=ORIENTED_EDGE ( 'NONE', *, *, #86469, .T. ) ;
#58934=EDGE_CURVE ( 'NONE', #106160, #23116, #75127, .T. ) ;
#58949=EDGE_CURVE ( 'NONE', #7253, #8789, #26625, .T. ) ;
#58952=VECTOR ( 'NONE', #23598, 1000.000000000000000 ) ;
#58994=VERTEX_POINT ( 'NONE', #84290 ) ;
#59004=EDGE_CURVE ( 'NONE', #48048, #52425, #20304, .T. ) ;
#59017=DIRECTION ( 'NONE',  ( -1.000000000000000000, -1.224606353822377258E-16, -0.000000000000000000 ) ) ;
#59038=CARTESIAN_POINT ( 'NONE',  ( 38.54515645702225868, 1.482358050883964840E-15, 0.000000000000000000 ) ) ;
#59041=AXIS2_PLACEMENT_3D ( 'NONE', #50136, #83045, #15643 ) ;
#59045=ORIENTED_EDGE ( 'NONE', *, *, #64195, .F. ) ;
#59098=CARTESIAN_POINT ( 'NONE',  ( 22.57792046605466041, 1.340359594676612611E-15, 0.000000000000000000 ) ) ;
#59111=AXIS2_PLACEMENT_3D ( 'NONE', #35591, #96463, #105079 ) ;
#59187=AXIS2_PLACEMENT_3D ( 'NONE', #21266, #103212, #11518 ) ;
#59191=CIRCLE ( 'NONE', #67805, 5.000000000000002665 ) ;
#59205=ORIENTED_EDGE ( 'NONE', *, *, #88501, .F. ) ;
#59224=AXIS2_PLACEMENT_3D ( 'NONE', #51908, #2281, #84821 ) ;
#59226=AXIS2_PLACEMENT_3D ( 'NONE', #73263, #24238, #90001 ) ;
#59242=ORIENTED_EDGE ( 'NONE', *, *, #103147, .F. ) ;
#59254=CARTESIAN_POINT ( 'NONE',  ( 35.58361799548379167, 6.123233995736772199E-16, -5.000000000000001776 ) ) ;
#59274=CARTESIAN_POINT ( 'NONE',  ( 15.17407431220850533, 1.340359594676612611E-15, 0.000000000000000000 ) ) ;
#59294=ORIENTED_EDGE ( 'NONE', *, *, #11970, .T. ) ;
#59307=LINE ( 'NONE', #84102, #52641 ) ;
#59311=CARTESIAN_POINT ( 'NONE',  ( 40.92692307692308162, 1.411358822780289120E-15, 0.000000000000000000 ) ) ;
#59313=LINE ( 'NONE', #34000, #66527 ) ;
#59316=CARTESIAN_POINT ( 'NONE',  ( 17.81438722625302518, 1.482358050883964840E-15, 0.000000000000000000 ) ) ;
#59348=EDGE_CURVE ( 'NONE', #35464, #67362, #35673, .T. ) ;
#59354=CARTESIAN_POINT ( 'NONE',  ( 31.14131030317610538, 1.482358050883964840E-15, 0.000000000000000000 ) ) ;
#59359=DIRECTION ( 'NONE',  ( -0.5735764363510510444, -0.8191520442889883569, 0.000000000000000000 ) ) ;
#59380=AXIS2_PLACEMENT_3D ( 'NONE', #104764, #22820, #89121 ) ;
#59382=ORIENTED_EDGE ( 'NONE', *, *, #91938, .T. ) ;
#59386=DIRECTION ( 'NONE',  ( -1.000000000000000000, -1.224606353822377258E-16, -0.000000000000000000 ) ) ;
#59390=DIRECTION ( 'NONE',  ( -1.000000000000000000, -1.224606353822377258E-16, -0.000000000000000000 ) ) ;
#59402=ORIENTED_EDGE ( 'NONE', *, *, #49103, .T. ) ;
#59439=EDGE_CURVE ( 'NONE', #52182, #30449, #8938, .T. ) ;
#59447=ORIENTED_EDGE ( 'NONE', *, *, #1576, .T. ) ;
#59449=CARTESIAN_POINT ( 'NONE',  ( 0.000000000000000000, 0.000000000000000000, 5.000000000000002665 ) ) ;
#59454=EDGE_CURVE ( 'NONE', #29601, #49147, #23570, .T. ) ;
#59458=CIRCLE ( 'NONE', #12914, 5.000000000000002665 ) ;
#59462=VECTOR ( 'NONE', #31819, 999.9999999999998863 ) ;
#59466=CARTESIAN_POINT ( 'NONE',  ( 40.34715123528543046, -5.000000000000009770, 0.000000000000000000 ) ) ;
#59478=EDGE_CURVE ( 'NONE', #58193, #27470, #92444, .T. ) ;
#59497=CARTESIAN_POINT ( 'NONE',  ( 24.63846153846153797, 4.172000000000003261, 5.109226446042759579E-16 ) ) ;
#59504=ORIENTED_EDGE ( 'NONE', *, *, #20829, .F. ) ;
#59505=LINE ( 'NONE', #92379, #66445 ) ;
#59535=CARTESIAN_POINT ( 'NONE',  ( 16.65484354297773351, 0.000000000000000000, 5.000000000000002665 ) ) ;
#59541=DIRECTION ( 'NONE',  ( 0.000000000000000000, 1.000000000000000000, 0.000000000000000000 ) ) ;
#59568=EDGE_CURVE ( 'NONE', #51711, #98765, #70908, .T. ) ;
#59587=EDGE_LOOP ( 'NONE', ( #17228, #28246, #18951, #6320, #77010 ) ) ;
#59604=AXIS2_PLACEMENT_3D ( 'NONE', #63680, #5430, #71214 ) ;
#59606=CONICAL_SURFACE ( 'NONE', #32045, 5.000000000000001776, 0.9599310885968803664 ) ;
#59621=EDGE_CURVE ( 'NONE', #67362, #77056, #79522, .T. ) ;
#59627=DIRECTION ( 'NONE',  ( -1.000000000000000000, -1.224606353822377258E-16, -0.000000000000000000 ) ) ;
#59640=EDGE_LOOP ( 'NONE', ( #71493, #8014, #3426, #1665, #3493 ) ) ;
#59654=FACE_OUTER_BOUND ( 'NONE', #100157, .T. ) ;
#59662=DIRECTION ( 'NONE',  ( 0.000000000000000000, -1.000000000000000000, 0.000000000000000000 ) ) ;
#59715=CARTESIAN_POINT ( 'NONE',  ( 16.65484354297773351, 5.000000000000004441, 6.123233995736770227E-16 ) ) ;
#59725=DIRECTION ( 'NONE',  ( 1.000000000000000000, 1.224606353822377258E-16, 0.000000000000000000 ) ) ;
#59750=EDGE_CURVE ( 'NONE', #47858, #105570, #85699, .T. ) ;
#59752=DIRECTION ( 'NONE',  ( 0.000000000000000000, 0.000000000000000000, 1.000000000000000000 ) ) ;
#59775=CARTESIAN_POINT ( 'NONE',  ( 31.46253585067004721, 0.000000000000000000, 5.000000000000002665 ) ) ;
#59790=FACE_OUTER_BOUND ( 'NONE', #55080, .T. ) ;
#59823=ORIENTED_EDGE ( 'NONE', *, *, #54093, .F. ) ;
#59847=AXIS2_PLACEMENT_3D ( 'NONE', #79781, #103534, #5882 ) ;
#59934=DIRECTION ( 'NONE',  ( 0.000000000000000000, 1.000000000000000000, 0.000000000000000000 ) ) ;
#59955=DIRECTION ( 'NONE',  ( 1.000000000000000000, 1.224606353822377258E-16, 0.000000000000000000 ) ) ;
#59961=EDGE_CURVE ( 'NONE', #20128, #67515, #44928, .T. ) ;
#59968=DIRECTION ( 'NONE',  ( 0.000000000000000000, -1.000000000000000000, 0.000000000000000000 ) ) ;
#60013=LINE ( 'NONE', #100431, #95123 ) ;
#60037=AXIS2_PLACEMENT_3D ( 'NONE', #97401, #89342, #81742 ) ;
#60061=CARTESIAN_POINT ( 'NONE',  ( 27.59999999999999787, -4.171999999999999709, 5.616230220889763424E-16 ) ) ;
#60092=ORIENTED_EDGE ( 'NONE', *, *, #50399, .T. ) ;
#60140=CIRCLE ( 'NONE', #89443, 5.000000000000002665 ) ;
#60193=VECTOR ( 'NONE', #4800, 1000.000000000000114 ) ;
#60233=AXIS2_PLACEMENT_3D ( 'NONE', #54751, #13763, #105445 ) ;
#60257=VECTOR ( 'NONE', #43108, 1000.000000000000000 ) ;
#60319=VERTEX_POINT ( 'NONE', #50718 ) ;
#60329=ORIENTED_EDGE ( 'NONE', *, *, #105426, .T. ) ;
#60333=CARTESIAN_POINT ( 'NONE',  ( 31.46253585067004721, 1.340359594676612611E-15, 0.000000000000000000 ) ) ;
#60339=DIRECTION ( 'NONE',  ( 0.000000000000000000, -1.000000000000000000, 0.000000000000000000 ) ) ;
#60377=CARTESIAN_POINT ( 'NONE',  ( 0.000000000000000000, 0.000000000000000000, 5.000000000000002665 ) ) ;
#60397=ADVANCED_FACE ( 'NONE', ( #73944 ), #32996, .T. ) ;
#60398=VECTOR ( 'NONE', #37772, 1000.000000000000000 ) ;
#60444=CARTESIAN_POINT ( 'NONE',  ( 12.79230769230769305, -4.171999999999999709, 5.616230220889763424E-16 ) ) ;
#60446=LINE ( 'NONE', #69583, #82120 ) ;
#60454=ORIENTED_EDGE ( 'NONE', *, *, #12855, .F. ) ;
#60467=AXIS2_PLACEMENT_3D ( 'NONE', #96826, #22956, #55792 ) ;
#60509=CARTESIAN_POINT ( 'NONE',  ( 0.000000000000000000, 6.123233995736770227E-16, -5.000000000000002665 ) ) ;
#60536=CARTESIAN_POINT ( 'NONE',  ( 40.02592568779148507, 1.482358050883964840E-15, 0.000000000000000000 ) ) ;
#60541=CIRCLE ( 'NONE', #32968, 4.172000000000001485 ) ;
#60555=AXIS2_PLACEMENT_3D ( 'NONE', #98813, #26062, #81552 ) ;
#60574=LINE ( 'NONE', #67059, #87020 ) ;
#60585=AXIS2_PLACEMENT_3D ( 'NONE', #35145, #99844, #85264 ) ;
#60594=ORIENTED_EDGE ( 'NONE', *, *, #47383, .T. ) ;
#60610=CARTESIAN_POINT ( 'NONE',  ( 13.37207953394533355, 6.123233995736772199E-16, -5.000000000000001776 ) ) ;
#60644=EDGE_CURVE ( 'NONE', #46447, #85900, #54433, .T. ) ;
#60654=VERTEX_POINT ( 'NONE', #40399 ) ;
#60664=EDGE_LOOP ( 'NONE', ( #61247, #85562, #54445, #60329, #15036 ) ) ;
#60668=ORIENTED_EDGE ( 'NONE', *, *, #1301, .F. ) ;
#60694=EDGE_CURVE ( 'NONE', #99927, #95837, #52978, .T. ) ;
#60697=CARTESIAN_POINT ( 'NONE',  ( 18.71538461538461462, 4.172000000000003261, 0.000000000000000000 ) ) ;
#60700=EDGE_CURVE ( 'NONE', #19012, #90464, #16121, .T. ) ;
#60733=EDGE_LOOP ( 'NONE', ( #29887, #80926, #1088, #58921, #67335 ) ) ;
#60735=AXIS2_PLACEMENT_3D ( 'NONE', #100044, #75773, #102173 ) ;
#60755=CIRCLE ( 'NONE', #14206, 4.172000000000001485 ) ;
#60779=EDGE_LOOP ( 'NONE', ( #105538, #76751, #98623 ) ) ;
#60787=AXIS2_PLACEMENT_3D ( 'NONE', #18089, #91960, #67165 ) ;
#60790=DIRECTION ( 'NONE',  ( 0.000000000000000000, -1.000000000000000000, 0.000000000000000000 ) ) ;
#60803=VERTEX_POINT ( 'NONE', #67350 ) ;
#60808=DIRECTION ( 'NONE',  ( 0.000000000000000000, -1.000000000000000000, 0.000000000000000000 ) ) ;
#60835=ORIENTED_EDGE ( 'NONE', *, *, #21865, .T. ) ;
#60839=VERTEX_POINT ( 'NONE', #100229 ) ;
#60877=LINE ( 'NONE', #93767, #81255 ) ;
#60924=DIRECTION ( 'NONE',  ( 0.000000000000000000, -1.000000000000000000, 0.000000000000000000 ) ) ;
#60925=ORIENTED_EDGE ( 'NONE', *, *, #47647, .T. ) ;
#60943=ORIENTED_EDGE ( 'NONE', *, *, #21486, .F. ) ;
#60951=CARTESIAN_POINT ( 'NONE',  ( 0.000000000000000000, 0.000000000000000000, 0.000000000000000000 ) ) ;
#60994=ORIENTED_EDGE ( 'NONE', *, *, #63933, .F. ) ;
#61001=EDGE_CURVE ( 'NONE', #6808, #96464, #42719, .T. ) ;
#61039=COLOUR_RGB ( '', 0.31764706, 0.68627451, 0.89019608) ;
#61055=CYLINDRICAL_SURFACE ( 'NONE', #104779, 5.000000000000002665 ) ;
#61062=ORIENTED_EDGE ( 'NONE', *, *, #62847, .F. ) ;
#61071=CARTESIAN_POINT ( 'NONE',  ( 33.52307692307692122, 1.411358822780289120E-15, 0.000000000000000000 ) ) ;
#61073=STYLED_ITEM ( 'NONE', ( #8130 ), #55270 ) ;
#61082=EDGE_CURVE ( 'NONE', #25507, #19124, #104896, .T. ) ;
#61141=ORIENTED_EDGE ( 'NONE', *, *, #93974, .F. ) ;
#61150=CARTESIAN_POINT ( 'NONE',  ( 16.65484354297773351, 1.340359594676612611E-15, 0.000000000000000000 ) ) ;
#61168=LINE ( 'NONE', #46561, #83261 ) ;
#61172=FACE_OUTER_BOUND ( 'NONE', #31276, .T. ) ;
#61199=CARTESIAN_POINT ( 'NONE',  ( 19.29515645702225868, -5.000000000000000888, 6.123233995736769241E-16 ) ) ;
#61236=DIRECTION ( 'NONE',  ( 1.000000000000000000, 1.224606353822377258E-16, 0.000000000000000000 ) ) ;
#61247=ORIENTED_EDGE ( 'NONE', *, *, #77286, .F. ) ;
#61254=VERTEX_POINT ( 'NONE', #27735 ) ;
#61283=CARTESIAN_POINT ( 'NONE',  ( 21.09715123528542691, 6.123233995736770227E-16, -5.000000000000002665 ) ) ;
#61332=CARTESIAN_POINT ( 'NONE',  ( 44.46823338009918558, 1.482358050883964840E-15, 0.000000000000000000 ) ) ;
#61341=CIRCLE ( 'NONE', #52688, 5.000000000000001776 ) ;
#61387=ORIENTED_EDGE ( 'NONE', *, *, #76092, .T. ) ;
#61388=FACE_OUTER_BOUND ( 'NONE', #62265, .T. ) ;
#61422=ORIENTED_EDGE ( 'NONE', *, *, #69143, .F. ) ;
#61443=CIRCLE ( 'NONE', #75185, 5.000000000000001776 ) ;
#61458=CIRCLE ( 'NONE', #56246, 4.172000000000001485 ) ;
#61480=DIRECTION ( 'NONE',  ( 1.000000000000000000, 1.224606353822377258E-16, 0.000000000000000000 ) ) ;
#61486=DIRECTION ( 'NONE',  ( -1.000000000000000000, -1.224606353822377258E-16, -0.000000000000000000 ) ) ;
#61495=VERTEX_POINT ( 'NONE', #24404 ) ;
#61503=LINE ( 'NONE', #86840, #74675 ) ;
#61504=DIRECTION ( 'NONE',  ( 1.000000000000000000, 1.224606353822377258E-16, 0.000000000000000000 ) ) ;
#61512=ORIENTED_EDGE ( 'NONE', *, *, #35352, .T. ) ;
#61518=FACE_OUTER_BOUND ( 'NONE', #80764, .T. ) ;
#61605=AXIS2_PLACEMENT_3D ( 'NONE', #83367, #93606, #11596 ) ;
#61621=ORIENTED_EDGE ( 'NONE', *, *, #53627, .F. ) ;
#61628=AXIS2_PLACEMENT_3D ( 'NONE', #63736, #96618, #22755 ) ;
#61655=DIRECTION ( 'NONE',  ( 0.000000000000000000, -1.000000000000000000, 0.000000000000000000 ) ) ;
#61658=CIRCLE ( 'NONE', #9964, 5.000000000000002665 ) ;
#61684=FACE_OUTER_BOUND ( 'NONE', #92920, .T. ) ;
#61770=DIRECTION ( 'NONE',  ( 0.000000000000000000, 0.000000000000000000, -1.000000000000000000 ) ) ;
#61779=EDGE_CURVE ( 'NONE', #68633, #13798, #9358, .T. ) ;
#61867=VECTOR ( 'NONE', #24208, 1000.000000000000000 ) ;
#61895=AXIS2_PLACEMENT_3D ( 'NONE', #100458, #18506, #85345 ) ;
#61898=ORIENTED_EDGE ( 'NONE', *, *, #83668, .F. ) ;
#61919=CIRCLE ( 'NONE', #99764, 5.000000000000002665 ) ;
#61957=VERTEX_POINT ( 'NONE', #2875 ) ;
#61961=ORIENTED_EDGE ( 'NONE', *, *, #95841, .T. ) ;
#61991=CARTESIAN_POINT ( 'NONE',  ( 42.40769230769231513, 1.411358822780289120E-15, 0.000000000000000000 ) ) ;
#61997=ORIENTED_EDGE ( 'NONE', *, *, #41133, .F. ) ;
#62017=CARTESIAN_POINT ( 'NONE',  ( 31.14131030317610538, -5.000000000000000000, 6.123233995736768255E-16 ) ) ;
#62019=AXIS2_PLACEMENT_3D ( 'NONE', #61150, #332, #58072 ) ;
#62030=VERTEX_POINT ( 'NONE', #81522 ) ;
#62085=DIRECTION ( 'NONE',  ( -1.000000000000000000, -0.000000000000000000, -0.000000000000000000 ) ) ;
#62094=AXIS2_PLACEMENT_3D ( 'NONE', #98975, #8917, #65037 ) ;
#62097=EDGE_LOOP ( 'NONE', ( #44163, #40470, #96459, #23171, #22855 ) ) ;
#62127=ORIENTED_EDGE ( 'NONE', *, *, #9543, .F. ) ;
#62129=EDGE_CURVE ( 'NONE', #45319, #68633, #55925, .T. ) ;
#62142=CIRCLE ( 'NONE', #8661, 5.000000000000001776 ) ;
#62144=FACE_OUTER_BOUND ( 'NONE', #70157, .T. ) ;
#62175=VECTOR ( 'NONE', #77211, 1000.000000000000000 ) ;
#62195=EDGE_LOOP ( 'NONE', ( #30286, #86656, #69790, #92998, #37663, #24095 ) ) ;
#62201=EDGE_CURVE ( 'NONE', #9931, #42028, #76114, .T. ) ;
#62204=ORIENTED_EDGE ( 'NONE', *, *, #23416, .F. ) ;
#62206=EDGE_LOOP ( 'NONE', ( #47792, #91756, #72106, #46435, #59045, #13440 ) ) ;
#62228=CIRCLE ( 'NONE', #98368, 5.000000000000002665 ) ;
#62247=CARTESIAN_POINT ( 'NONE',  ( 26.11923076923076792, 1.411358822780289120E-15, 0.000000000000000000 ) ) ;
#62265=EDGE_LOOP ( 'NONE', ( #74092, #80987, #69133, #28082, #35016 ) ) ;
#62294=CARTESIAN_POINT ( 'NONE',  ( 0.000000000000000000, 0.000000000000000000, 0.000000000000000000 ) ) ;
#62304=DIRECTION ( 'NONE',  ( 0.000000000000000000, 1.000000000000000000, 0.000000000000000000 ) ) ;
#62346=CYLINDRICAL_SURFACE ( 'NONE', #75910, 5.000000000000002665 ) ;
#62361=ORIENTED_EDGE ( 'NONE', *, *, #66599, .F. ) ;
#62378=DIRECTION ( 'NONE',  ( 0.000000000000000000, 0.000000000000000000, 1.000000000000000000 ) ) ;
#62454=CARTESIAN_POINT ( 'NONE',  ( 0.000000000000000000, 0.000000000000000000, 0.000000000000000000 ) ) ;
#62462=ORIENTED_EDGE ( 'NONE', *, *, #54066, .F. ) ;
#62538=CARTESIAN_POINT ( 'NONE',  ( 0.08224679563971193375, 6.145890662064649845, -5.355005115540897975 ) ) ;
#62549=CARTESIAN_POINT ( 'NONE',  ( 0.000000000000000000, 6.123233995736770227E-16, -5.000000000000002665 ) ) ;
#62553=DIRECTION ( 'NONE',  ( 0.000000000000000000, -1.000000000000000000, 0.000000000000000000 ) ) ;
#62607=EDGE_CURVE ( 'NONE', #7097, #15625, #54342, .T. ) ;
#62612=DIRECTION ( 'NONE',  ( -1.000000000000000000, -1.224606353822377258E-16, -0.000000000000000000 ) ) ;
#62664=CARTESIAN_POINT ( 'NONE',  ( 35.00384615384614762, 1.411358822780289120E-15, 0.000000000000000000 ) ) ;
#62670=LINE ( 'NONE', #71789, #46141 ) ;
#62675=ORIENTED_EDGE ( 'NONE', *, *, #11209, .T. ) ;
#62679=DIRECTION ( 'NONE',  ( -0.5735764363510510444, -0.8191520442889883569, 0.000000000000000000 ) ) ;
#62684=VECTOR ( 'NONE', #62679, 1000.000000000000000 ) ;
#62689=DIRECTION ( 'NONE',  ( 0.000000000000000000, -1.000000000000000000, 0.000000000000000000 ) ) ;
#62711=EDGE_CURVE ( 'NONE', #51711, #14152, #57013, .T. ) ;
#62737=ORIENTED_EDGE ( 'NONE', *, *, #44810, .T. ) ;
#62740=CARTESIAN_POINT ( 'NONE',  ( 11.89131030317610183, 1.482358050883964840E-15, 0.000000000000000000 ) ) ;
#62770=( GEOMETRIC_REPRESENTATION_CONTEXT ( 3 ) GLOBAL_UNCERTAINTY_ASSIGNED_CONTEXT ( ( #94528 ) ) GLOBAL_UNIT_ASSIGNED_CONTEXT ( ( #73383, #32444, #65319 ) ) REPRESENTATION_CONTEXT ( 'NONE', 'WORKASPACE' ) );
#62847=EDGE_CURVE ( 'NONE', #28015, #41783, #93841, .T. ) ;
#62871=CARTESIAN_POINT ( 'NONE',  ( 0.000000000000000000, 0.000000000000000000, 0.000000000000000000 ) ) ;
#62882=AXIS2_PLACEMENT_3D ( 'NONE', #82801, #74166, #87325 ) ;
#62884=ORIENTED_EDGE ( 'NONE', *, *, #5855, .F. ) ;
#62933=CARTESIAN_POINT ( 'NONE',  ( 10.41054107240687188, 1.482358050883964840E-15, 0.000000000000000000 ) ) ;
#62945=CIRCLE ( 'NONE', #99102, 5.000000000000002665 ) ;
#62977=CARTESIAN_POINT ( 'NONE',  ( 37.06438722625302518, 5.000000000000003553, 0.000000000000000000 ) ) ;
#63004=VERTEX_POINT ( 'NONE', #9793 ) ;
#63024=VERTEX_POINT ( 'NONE', #67529 ) ;
#63040=CIRCLE ( 'NONE', #13040, 5.000000000000002665 ) ;
#63042=ORIENTED_EDGE ( 'NONE', *, *, #55310, .F. ) ;
#63060=AXIS2_PLACEMENT_3D ( 'NONE', #70699, #95498, #21641 ) ;
#63081=FACE_OUTER_BOUND ( 'NONE', #55822, .T. ) ;
#63086=ORIENTED_EDGE ( 'NONE', *, *, #72149, .F. ) ;
#63117=EDGE_CURVE ( 'NONE', #2494, #98655, #105987, .T. ) ;
#63129=ORIENTED_EDGE ( 'NONE', *, *, #32887, .F. ) ;
#63142=CONICAL_SURFACE ( 'NONE', #26982, 5.000000000000001776, 0.9599310885968803664 ) ;
#63214=VECTOR ( 'NONE', #85304, 1000.000000000000000 ) ;
#63269=CIRCLE ( 'NONE', #82421, 4.172000000000001485 ) ;
#63270=ORIENTED_EDGE ( 'NONE', *, *, #14425, .T. ) ;
#63315=ADVANCED_FACE ( 'NONE', ( #75471 ), #16457, .T. ) ;
#63333=SHAPE_DEFINITION_REPRESENTATION ( #50967, #44072 ) ;
#63350=CARTESIAN_POINT ( 'NONE',  ( -5.749871404199004277E-15, -6.732211846623389562, 4.339467034331195627 ) ) ;
#63362=ADVANCED_FACE ( 'NONE', ( #23773 ), #32389, .T. ) ;
#63394=EDGE_CURVE ( 'NONE', #8257, #75630, #59307, .T. ) ;
#63396=CARTESIAN_POINT ( 'NONE',  ( 45.94900261086841198, 1.482358050883964840E-15, 0.000000000000000000 ) ) ;
#63418=ORIENTED_EDGE ( 'NONE', *, *, #54219, .F. ) ;
#63474=AXIS2_PLACEMENT_3D ( 'NONE', #87931, #80340, #105167 ) ;
#63489=CIRCLE ( 'NONE', #47974, 5.000000000000001776 ) ;
#63548=CIRCLE ( 'NONE', #17034, 5.000000000000001776 ) ;
#63554=CARTESIAN_POINT ( 'NONE',  ( 41.82792046605465686, 5.000000000000015099, 6.123233995736782060E-16 ) ) ;
#63565=VERTEX_POINT ( 'NONE', #2638 ) ;
#63593=CARTESIAN_POINT ( 'NONE',  ( 0.000000000000000000, 0.000000000000000000, 0.000000000000000000 ) ) ;
#63595=CARTESIAN_POINT ( 'NONE',  ( 35.00384615384614762, 4.172000000000003261, 5.109226446042759579E-16 ) ) ;
#63629=DIRECTION ( 'NONE',  ( 0.000000000000000000, -1.000000000000000000, 0.000000000000000000 ) ) ;
#63632=ORIENTED_EDGE ( 'NONE', *, *, #46527, .F. ) ;
#63640=CARTESIAN_POINT ( 'NONE',  ( 0.7145311798161616545, -4.618802153517262532, -8.000000000000001776 ) ) ;
#63642=DIRECTION ( 'NONE',  ( 0.000000000000000000, -1.000000000000000000, 0.000000000000000000 ) ) ;
#63680=CARTESIAN_POINT ( 'NONE',  ( 42.98746414932995208, 1.482358050883964840E-15, 0.000000000000000000 ) ) ;
#63684=VECTOR ( 'NONE', #72291, 1000.000000000000000 ) ;
#63736=CARTESIAN_POINT ( 'NONE',  ( 46.85000000000000142, 0.000000000000000000, 0.000000000000000000 ) ) ;
#63742=ORIENTED_EDGE ( 'NONE', *, *, #95544, .F. ) ;
#63765=CIRCLE ( 'NONE', #62094, 5.000000000000002665 ) ;
#63792=ADVANCED_FACE ( 'NONE', ( #11130 ), #37288, .T. ) ;
#63795=ORIENTED_EDGE ( 'NONE', *, *, #74446, .T. ) ;
#63828=CARTESIAN_POINT ( 'NONE',  ( 6.249999999999998224, 8.000000000000000000, 0.000000000000000000 ) ) ;
#63895=EDGE_LOOP ( 'NONE', ( #33706, #104582, #35071, #2685, #48548 ) ) ;
#63904=AXIS2_PLACEMENT_3D ( 'NONE', #30541, #24051, #80116 ) ;
#63933=EDGE_CURVE ( 'NONE', #56640, #85522, #25186, .T. ) ;
#63951=VECTOR ( 'NONE', #49520, 999.9999999999998863 ) ;
#63998=EDGE_LOOP ( 'NONE', ( #72850, #48248, #24284, #12944, #48879, #4230 ) ) ;
#64027=DIRECTION ( 'NONE',  ( 0.000000000000000000, -1.000000000000000000, 0.000000000000000000 ) ) ;
#64036=DIRECTION ( 'NONE',  ( 0.000000000000000000, -1.000000000000000000, 0.000000000000000000 ) ) ;
#64085=ORIENTED_EDGE ( 'NONE', *, *, #20283, .F. ) ;
#64090=CYLINDRICAL_SURFACE ( 'NONE', #93945, 5.000000000000002665 ) ;
#64097=CIRCLE ( 'NONE', #38237, 5.000000000000001776 ) ;
#64109=FACE_OUTER_BOUND ( 'NONE', #67648, .T. ) ;
#64117=ORIENTED_EDGE ( 'NONE', *, *, #97959, .F. ) ;
#64163=DIRECTION ( 'NONE',  ( -0.5735764363510512664, 0.8191520442889881348, 1.003171929053520309E-16 ) ) ;
#64182=VERTEX_POINT ( 'NONE', #75907 ) ;
#64195=EDGE_CURVE ( 'NONE', #8878, #96901, #47388, .T. ) ;
#64226=ORIENTED_EDGE ( 'NONE', *, *, #42472, .T. ) ;
#64231=FACE_OUTER_BOUND ( 'NONE', #42088, .T. ) ;
#64272=EDGE_CURVE ( 'NONE', #28378, #86142, #14656, .T. ) ;
#64309=AXIS2_PLACEMENT_3D ( 'NONE', #58838, #98728, #42100 ) ;
#64318=EDGE_CURVE ( 'NONE', #95821, #13709, #102312, .T. ) ;
#64339=CARTESIAN_POINT ( 'NONE',  ( 20.77592568779148863, 1.482358050883964840E-15, 0.000000000000000000 ) ) ;
#64360=DIRECTION ( 'NONE',  ( -1.000000000000000000, -1.224606353822377258E-16, -0.000000000000000000 ) ) ;
#64362=ORIENTED_EDGE ( 'NONE', *, *, #17834, .T. ) ;
#64363=CARTESIAN_POINT ( 'NONE',  ( 23.73746414932995208, 1.482358050883964840E-15, 0.000000000000000000 ) ) ;
#64428=DIRECTION ( 'NONE',  ( 0.000000000000000000, -1.000000000000000000, 0.000000000000000000 ) ) ;
#64431=ORIENTED_EDGE ( 'NONE', *, *, #59478, .T. ) ;
#64464=DIRECTION ( 'NONE',  ( -0.000000000000000000, 1.000000000000000000, 1.877893248421449036E-16 ) ) ;
#64484=CARTESIAN_POINT ( 'NONE',  ( 0.000000000000000000, 0.000000000000000000, 0.000000000000000000 ) ) ;
#64485=ORIENTED_EDGE ( 'NONE', *, *, #51806, .F. ) ;
#64497=CONICAL_SURFACE ( 'NONE', #17984, 5.000000000000001776, 0.9599310885968803664 ) ;
#64504=EDGE_CURVE ( 'NONE', #85144, #73958, #61443, .T. ) ;
#64545=EDGE_CURVE ( 'NONE', #73958, #71240, #99046, .T. ) ;
#64549=ORIENTED_EDGE ( 'NONE', *, *, #82143, .T. ) ;
#64599=CYLINDRICAL_SURFACE ( 'NONE', #42240, 5.000000000000002665 ) ;
#64614=AXIS2_PLACEMENT_3D ( 'NONE', #71074, #80749, #55918 ) ;
#64618=EDGE_CURVE ( 'NONE', #87871, #56640, #75232, .T. ) ;
#64669=DIRECTION ( 'NONE',  ( 0.000000000000000000, -1.000000000000000000, 0.000000000000000000 ) ) ;
#64681=EDGE_LOOP ( 'NONE', ( #12712, #74126, #96859, #103835, #37442 ) ) ;
#64699=EDGE_LOOP ( 'NONE', ( #14221, #2106, #87369, #60092, #59242, #86750 ) ) ;
#64725=DIRECTION ( 'NONE',  ( -1.000000000000000000, -0.000000000000000000, -0.000000000000000000 ) ) ;
#64762=AXIS2_PLACEMENT_3D ( 'NONE', #104036, #45298, #30176 ) ;
#64765=AXIS2_PLACEMENT_3D ( 'NONE', #43401, #42861, #18615 ) ;
#64787=CARTESIAN_POINT ( 'NONE',  ( 25.53945892759312031, -5.000000000000000000, 0.000000000000000000 ) ) ;
#64858=DIRECTION ( 'NONE',  ( 0.000000000000000000, -1.000000000000000000, 0.000000000000000000 ) ) ;
#64882=CARTESIAN_POINT ( 'NONE',  ( 20.77592568779148863, 3.851859888774471706E-31, 5.000000000000001776 ) ) ;
#64887=ORIENTED_EDGE ( 'NONE', *, *, #32270, .T. ) ;
#64889=VECTOR ( 'NONE', #3524, 1000.000000000000000 ) ;
#64909=AXIS2_PLACEMENT_3D ( 'NONE', #83377, #9472, #76342 ) ;
#64953=DIRECTION ( 'NONE',  ( 0.5735764363510470476, -0.8191520442889911324, 1.003171929053524007E-16 ) ) ;
#64978=DIRECTION ( 'NONE',  ( -1.000000000000000000, -0.000000000000000000, -0.000000000000000000 ) ) ;
#65037=DIRECTION ( 'NONE',  ( 0.000000000000000000, -1.000000000000000000, 0.000000000000000000 ) ) ;
#65044=CONICAL_SURFACE ( 'NONE', #2993, 5.000000000000001776, 0.9599310885968803664 ) ;
#65067=VERTEX_POINT ( 'NONE', #24489 ) ;
#65087=CARTESIAN_POINT ( 'NONE',  ( 8.349999999999999645, -4.171999999999999709, 0.000000000000000000 ) ) ;
#65117=CARTESIAN_POINT ( 'NONE',  ( 22.25669491856071858, 1.482358050883964840E-15, 0.000000000000000000 ) ) ;
#65122=ORIENTED_EDGE ( 'NONE', *, *, #63117, .F. ) ;
#65133=PLANE ( 'NONE',  #4521 ) ;
#65161=DIRECTION ( 'NONE',  ( -0.5735764363510512664, 0.8191520442889881348, 1.003171929053520309E-16 ) ) ;
#65221=AXIS2_PLACEMENT_3D ( 'NONE', #98452, #106006, #32697 ) ;
#65241=ORIENTED_EDGE ( 'NONE', *, *, #42760, .T. ) ;
#65242=EDGE_LOOP ( 'NONE', ( #47603, #95175, #24872, #82440, #22015, #95862 ) ) ;
#65258=EDGE_CURVE ( 'NONE', #77934, #8789, #104370, .T. ) ;
#65266=DIRECTION ( 'NONE',  ( 0.000000000000000000, -1.000000000000000000, 0.000000000000000000 ) ) ;
#65294=EDGE_CURVE ( 'NONE', #84725, #69241, #87475, .T. ) ;
#65302=AXIS2_PLACEMENT_3D ( 'NONE', #3548, #10032, #59662 ) ;
#65308=EDGE_CURVE ( 'NONE', #19124, #29545, #106045, .T. ) ;
#65319=( NAMED_UNIT ( * ) SI_UNIT ( $, .STERADIAN. ) SOLID_ANGLE_UNIT ( ) );
#65404=CARTESIAN_POINT ( 'NONE',  ( 17.23461538461538467, -4.171999999999999709, 0.000000000000000000 ) ) ;
#65407=AXIS2_PLACEMENT_3D ( 'NONE', #87527, #88056, #15743 ) ;
#65412=AXIS2_PLACEMENT_3D ( 'NONE', #80238, #38751, #78644 ) ;
#65425=CARTESIAN_POINT ( 'NONE',  ( 39.44615384615384812, 1.411358822780289120E-15, 0.000000000000000000 ) ) ;
#65428=EDGE_CURVE ( 'NONE', #17674, #98844, #25179, .T. ) ;
#65443=CARTESIAN_POINT ( 'NONE',  ( 43.30868969682389036, 1.340359594676612611E-15, 0.000000000000000000 ) ) ;
#65453=CARTESIAN_POINT ( 'NONE',  ( 17.23461538461538467, 1.411358822780289120E-15, 0.000000000000000000 ) ) ;
#65508=DIRECTION ( 'NONE',  ( 0.000000000000000000, -1.000000000000000000, 0.000000000000000000 ) ) ;
#65516=EDGE_CURVE ( 'NONE', #31421, #74005, #4181, .T. ) ;
#65523=VERTEX_POINT ( 'NONE', #2574 ) ;
#65543=EDGE_CURVE ( 'NONE', #76065, #106696, #21716, .T. ) ;
#65590=VECTOR ( 'NONE', #105051, 1000.000000000000000 ) ;
#65591=DIRECTION ( 'NONE',  ( 0.5735764363510468256, 0.8191520442889913545, 0.000000000000000000 ) ) ;
#65624=CARTESIAN_POINT ( 'NONE',  ( 11.31153846153846132, 4.172000000000003261, 5.109226446042759579E-16 ) ) ;
#65636=CARTESIAN_POINT ( 'NONE',  ( 22.25669491856071858, 1.482358050883964840E-15, 0.000000000000000000 ) ) ;
#65654=ORIENTED_EDGE ( 'NONE', *, *, #7127, .T. ) ;
#65665=CARTESIAN_POINT ( 'NONE',  ( 0.000000000000000000, 0.000000000000000000, 0.000000000000000000 ) ) ;
#65703=EDGE_CURVE ( 'NONE', #88469, #4042, #63040, .T. ) ;
#65707=CARTESIAN_POINT ( 'NONE',  ( 10.41054107240687188, 1.482358050883964840E-15, 0.000000000000000000 ) ) ;
#65711=CARTESIAN_POINT ( 'NONE',  ( 46.85000000000000142, 0.000000000000000000, 0.000000000000000000 ) ) ;
#65723=ORIENTED_EDGE ( 'NONE', *, *, #21486, .T. ) ;
#65737=ORIENTED_EDGE ( 'NONE', *, *, #47383, .F. ) ;
#65801=CARTESIAN_POINT ( 'NONE',  ( 15.75384615384615294, 1.411358822780289120E-15, 0.000000000000000000 ) ) ;
#65803=CARTESIAN_POINT ( 'NONE',  ( 0.000000000000000000, 0.000000000000000000, 0.000000000000000000 ) ) ;
#65804=CARTESIAN_POINT ( 'NONE',  ( 8.929771841637641927, 3.851859888774471706E-31, 5.000000000000001776 ) ) ;
#65813=DIRECTION ( 'NONE',  ( 0.000000000000000000, -1.000000000000000000, 0.000000000000000000 ) ) ;
#65861=ORIENTED_EDGE ( 'NONE', *, *, #910, .F. ) ;
#65863=CARTESIAN_POINT ( 'NONE',  ( 0.000000000000000000, 0.000000000000000000, 0.000000000000000000 ) ) ;
#65884=ORIENTED_EDGE ( 'NONE', *, *, #28162, .F. ) ;
#65890=DIRECTION ( 'NONE',  ( -1.000000000000000000, -0.000000000000000000, -0.000000000000000000 ) ) ;
#65914=DIRECTION ( 'NONE',  ( -1.000000000000000000, -1.224606353822377258E-16, -0.000000000000000000 ) ) ;
#65927=ORIENTED_EDGE ( 'NONE', *, *, #68911, .T. ) ;
#65928=DIRECTION ( 'NONE',  ( 0.000000000000000000, 0.000000000000000000, 1.000000000000000000 ) ) ;
#65938=ORIENTED_EDGE ( 'NONE', *, *, #95898, .F. ) ;
#65978=CIRCLE ( 'NONE', #19541, 5.000000000000002665 ) ;
#65982=EDGE_CURVE ( 'NONE', #45532, #90027, #75180, .T. ) ;
#65989=ORIENTED_EDGE ( 'NONE', *, *, #80825, .T. ) ;
#66010=ORIENTED_EDGE ( 'NONE', *, *, #62607, .T. ) ;
#66031=ADVANCED_FACE ( 'NONE', ( #32251 ), #65133, .T. ) ;
#66032=ORIENTED_EDGE ( 'NONE', *, *, #94959, .F. ) ;
#66033=DIRECTION ( 'NONE',  ( 0.000000000000000000, -1.000000000000000000, 0.000000000000000000 ) ) ;
#66048=CARTESIAN_POINT ( 'NONE',  ( 14.85284876471456350, 1.482358050883964840E-15, 0.000000000000000000 ) ) ;
#66089=DIRECTION ( 'NONE',  ( -1.000000000000000000, -1.224606353822377258E-16, -0.000000000000000000 ) ) ;
#66159=DIRECTION ( 'NONE',  ( 0.000000000000000000, 0.000000000000000000, 1.000000000000000000 ) ) ;
#66167=DIRECTION ( 'NONE',  ( -1.000000000000000000, -1.224606353822377258E-16, -0.000000000000000000 ) ) ;
#66179=LINE ( 'NONE', #17115, #71508 ) ;
#66192=CARTESIAN_POINT ( 'NONE',  ( 6.249999999999998224, 8.000000000000000000, 0.000000000000000000 ) ) ;
#66196=CYLINDRICAL_SURFACE ( 'NONE', #94547, 5.000000000000002665 ) ;
#66223=LINE ( 'NONE', #91058, #79225 ) ;
#66240=CARTESIAN_POINT ( 'NONE',  ( 37.06438722625302518, 6.123233995736772199E-16, -5.000000000000001776 ) ) ;
#66252=ORIENTED_EDGE ( 'NONE', *, *, #44810, .F. ) ;
#66253=ADVANCED_FACE ( 'NONE', ( #21927 ), #45134, .T. ) ;
#66299=DIRECTION ( 'NONE',  ( 0.000000000000000000, -1.000000000000000000, 0.000000000000000000 ) ) ;
#66319=DIRECTION ( 'NONE',  ( 0.000000000000000000, 0.000000000000000000, 1.000000000000000000 ) ) ;
#66356=AXIS2_PLACEMENT_3D ( 'NONE', #66938, #59386, #99819 ) ;
#66396=DIRECTION ( 'NONE',  ( 0.000000000000000000, -1.000000000000000000, 0.000000000000000000 ) ) ;
#66420=CARTESIAN_POINT ( 'NONE',  ( 21.09715123528542691, 1.340359594676612611E-15, 0.000000000000000000 ) ) ;
#66443=DIRECTION ( 'NONE',  ( 0.000000000000000000, -1.000000000000000000, 0.000000000000000000 ) ) ;
#66445=VECTOR ( 'NONE', #31407, 1000.000000000000000 ) ;
#66468=DIRECTION ( 'NONE',  ( -1.000000000000000000, -1.224606353822377258E-16, -0.000000000000000000 ) ) ;
#66513=DIRECTION ( 'NONE',  ( 0.000000000000000000, 0.000000000000000000, -1.000000000000000000 ) ) ;
#66521=CONICAL_SURFACE ( 'NONE', #97526, 4.172000000000001485, 0.9599310885968750373 ) ;
#66527=VECTOR ( 'NONE', #18335, 999.9999999999998863 ) ;
#66544=CIRCLE ( 'NONE', #28710, 5.000000000000002665 ) ;
#66577=ADVANCED_FACE ( 'NONE', ( #77888 ), #102689, .T. ) ;
#66579=CARTESIAN_POINT ( 'NONE',  ( 24.63846153846153797, -4.171999999999999709, 5.616230220889763424E-16 ) ) ;
#66592=ORIENTED_EDGE ( 'NONE', *, *, #15113, .F. ) ;
#66597=CONICAL_SURFACE ( 'NONE', #80359, 4.172000000000001485, 0.9599310885968750373 ) ;
#66599=EDGE_CURVE ( 'NONE', #91139, #93494, #35656, .T. ) ;
#66643=AXIS2_PLACEMENT_3D ( 'NONE', #102154, #13659, #45531 ) ;
#66656=DIRECTION ( 'NONE',  ( -1.000000000000000000, -0.000000000000000000, -0.000000000000000000 ) ) ;
#66669=VECTOR ( 'NONE', #54312, 999.9999999999998863 ) ;
#66712=FACE_OUTER_BOUND ( 'NONE', #45909, .T. ) ;
#66727=ORIENTED_EDGE ( 'NONE', *, *, #37586, .F. ) ;
#66743=DIRECTION ( 'NONE',  ( -0.5735764363510512664, 0.8191520442889881348, 1.003171929053520309E-16 ) ) ;
#66747=DIRECTION ( 'NONE',  ( 0.000000000000000000, -1.000000000000000000, 0.000000000000000000 ) ) ;
#66800=DIRECTION ( 'NONE',  ( -1.000000000000000000, -1.224606353822377258E-16, -0.000000000000000000 ) ) ;
#66810=CARTESIAN_POINT ( 'NONE',  ( 0.3167204509598209872, -5.377136764700215288, -6.686525924292707757 ) ) ;
#66824=DIRECTION ( 'NONE',  ( -1.000000000000000000, -0.000000000000000000, -0.000000000000000000 ) ) ;
#66846=EDGE_LOOP ( 'NONE', ( #45326, #44858, #46870, #77664, #15095 ) ) ;
#66855=LINE ( 'NONE', #60377, #60257 ) ;
#66858=AXIS2_PLACEMENT_3D ( 'NONE', #106092, #57539, #57015 ) ;
#66867=DIRECTION ( 'NONE',  ( 0.000000000000000000, -1.000000000000000000, 0.000000000000000000 ) ) ;
#66909=DIRECTION ( 'NONE',  ( -0.5735764363510510444, -0.8191520442889883569, 0.000000000000000000 ) ) ;
#66911=DIRECTION ( 'NONE',  ( -1.000000000000000000, -1.224606353822377258E-16, -0.000000000000000000 ) ) ;
#66918=EDGE_LOOP ( 'NONE', ( #92192, #49940, #74537, #45343, #45790, #91363 ) ) ;
#66919=ADVANCED_FACE ( 'NONE', ( #105336 ), #32252, .T. ) ;
#66923=CIRCLE ( 'NONE', #103039, 5.000000000000002665 ) ;
#66938=CARTESIAN_POINT ( 'NONE',  ( 41.50669491856072568, 1.482358050883964840E-15, 0.000000000000000000 ) ) ;
#66981=VECTOR ( 'NONE', #17135, 1000.000000000000000 ) ;
#66992=LINE ( 'NONE', #60509, #18914 ) ;
#67002=ORIENTED_EDGE ( 'NONE', *, *, #91993, .T. ) ;
#67025=ORIENTED_EDGE ( 'NONE', *, *, #27425, .F. ) ;
#67052=PLANE ( 'NONE',  #59224 ) ;
#67059=CARTESIAN_POINT ( 'NONE',  ( 37.96538461538461462, -4.171999999999999709, 0.000000000000000000 ) ) ;
#67072=DIRECTION ( 'NONE',  ( 0.000000000000000000, -1.000000000000000000, 0.000000000000000000 ) ) ;
#67136=CARTESIAN_POINT ( 'NONE',  ( 11.31153846153846132, 1.411358822780289120E-15, 0.000000000000000000 ) ) ;
#67141=ORIENTED_EDGE ( 'NONE', *, *, #58663, .T. ) ;
#67150=AXIS2_PLACEMENT_3D ( 'NONE', #82804, #8905, #776 ) ;
#67152=CONICAL_SURFACE ( 'NONE', #87863, 5.000000000000001776, 0.9599310885968803664 ) ;
#67165=DIRECTION ( 'NONE',  ( 0.000000000000000000, -1.000000000000000000, 0.000000000000000000 ) ) ;
#67179=DIRECTION ( 'NONE',  ( 0.5735764363510468256, 0.8191520442889913545, 0.000000000000000000 ) ) ;
#67187=LINE ( 'NONE', #11578, #58895 ) ;
#67195=DIRECTION ( 'NONE',  ( -1.000000000000000000, -1.224606353822377258E-16, -0.000000000000000000 ) ) ;
#67202=CARTESIAN_POINT ( 'NONE',  ( 40.34715123528543046, 1.340359594676612611E-15, 0.000000000000000000 ) ) ;
#67240=EDGE_LOOP ( 'NONE', ( #90640, #71686, #61141, #80745, #8456 ) ) ;
#67244=FACE_OUTER_BOUND ( 'NONE', #62206, .T. ) ;
#67257=B_SPLINE_CURVE_WITH_KNOTS ( 'NONE', 3,
 ( #19135, #22836, #105835, #40050, #71878, #96699 ),
 .UNSPECIFIED., .F., .F.,
 ( 4, 2, 4 ),
 ( 2.380731629580637688E-07, 0.002336973833157565076, 0.004673709593152172194 ),
 .UNSPECIFIED. ) ;
#67335=ORIENTED_EDGE ( 'NONE', *, *, #56410, .F. ) ;
#67350=CARTESIAN_POINT ( 'NONE',  ( 12.21253585067004543, -5.000000000000000000, 0.000000000000000000 ) ) ;
#67351=CONICAL_SURFACE ( 'NONE', #34660, 8.000000000000000000, 1.047197551196600296 ) ;
#67358=ADVANCED_FACE ( 'NONE', ( #45665 ), #87452, .T. ) ;
#67362=VERTEX_POINT ( 'NONE', #47233 ) ;
#67366=ORIENTED_EDGE ( 'NONE', *, *, #76842, .T. ) ;
#67378=ORIENTED_EDGE ( 'NONE', *, *, #53965, .T. ) ;
#67405=LINE ( 'NONE', #92723, #2259 ) ;
#67406=AXIS2_PLACEMENT_3D ( 'NONE', #1064, #66911, #7580 ) ;
#67428=( NAMED_UNIT ( * ) PLANE_ANGLE_UNIT ( ) SI_UNIT ( $, .RADIAN. ) );
#67442=CARTESIAN_POINT ( 'NONE',  ( 23.15769230769230802, 4.172000000000003261, 5.109226446042759579E-16 ) ) ;
#67452=CARTESIAN_POINT ( 'NONE',  ( 42.98746414932995208, 1.482358050883964840E-15, 0.000000000000000000 ) ) ;
#67459=FACE_OUTER_BOUND ( 'NONE', #79692, .T. ) ;
#67470=FACE_OUTER_BOUND ( 'NONE', #77470, .T. ) ;
#67515=VERTEX_POINT ( 'NONE', #13270 ) ;
#67521=FACE_OUTER_BOUND ( 'NONE', #98355, .T. ) ;
#67529=CARTESIAN_POINT ( 'NONE',  ( 13.69330508143927538, 6.123233995736770227E-16, -5.000000000000002665 ) ) ;
#67558=EDGE_LOOP ( 'NONE', ( #51248, #65241, #5502, #42848, #104944, #4029 ) ) ;
#67579=ORIENTED_EDGE ( 'NONE', *, *, #43802, .T. ) ;
#67593=ORIENTED_EDGE ( 'NONE', *, *, #103917, .F. ) ;
#67615=ORIENTED_EDGE ( 'NONE', *, *, #82333, .T. ) ;
#67632=DIRECTION ( 'NONE',  ( -1.000000000000000000, -1.224606353822377258E-16, -0.000000000000000000 ) ) ;
#67648=EDGE_LOOP ( 'NONE', ( #39793, #28102, #102763, #42113, #44621, #22052 ) ) ;
#67674=ORIENTED_EDGE ( 'NONE', *, *, #17342, .T. ) ;
#67699=DIRECTION ( 'NONE',  ( -1.000000000000000000, -0.000000000000000000, -0.000000000000000000 ) ) ;
#67716=DIRECTION ( 'NONE',  ( 0.000000000000000000, -1.000000000000000000, 0.000000000000000000 ) ) ;
#67751=ORIENTED_EDGE ( 'NONE', *, *, #64272, .F. ) ;
#67799=DIRECTION ( 'NONE',  ( 0.000000000000000000, -1.000000000000000000, 0.000000000000000000 ) ) ;
#67805=AXIS2_PLACEMENT_3D ( 'NONE', #39055, #56797, #14745 ) ;
#67811=AXIS2_PLACEMENT_3D ( 'NONE', #4270, #10222, #60924 ) ;
#67870=CONICAL_SURFACE ( 'NONE', #43773, 4.172000000000001485, 0.9599310885968750373 ) ;
#67898=ORIENTED_EDGE ( 'NONE', *, *, #79650, .T. ) ;
#67899=EDGE_LOOP ( 'NONE', ( #17204, #84753, #79052, #23694, #6002, #24480 ) ) ;
#67906=EDGE_LOOP ( 'NONE', ( #29909, #96204, #89776, #65989, #32003 ) ) ;
#67943=DIRECTION ( 'NONE',  ( -1.000000000000000000, -1.224606353822377258E-16, -0.000000000000000000 ) ) ;
#67964=CARTESIAN_POINT ( 'NONE',  ( 0.000000000000000000, 0.000000000000000000, 8.000000000000000000 ) ) ;
#67977=CONICAL_SURFACE ( 'NONE', #81657, 8.000000000000000000, 1.047197551196600296 ) ;
#67982=CIRCLE ( 'NONE', #11146, 5.000000000000002665 ) ;
#67995=VERTEX_POINT ( 'NONE', #30839 ) ;
#68043=CARTESIAN_POINT ( 'NONE',  ( 34.42407431220851066, 1.340359594676612611E-15, 0.000000000000000000 ) ) ;
#68087=CARTESIAN_POINT ( 'NONE',  ( 18.71538461538461462, 1.411358822780289120E-15, 0.000000000000000000 ) ) ;
#68109=EDGE_LOOP ( 'NONE', ( #4760, #3319, #68343, #49823, #103478 ) ) ;
#68112=DIRECTION ( 'NONE',  ( -1.000000000000000000, -1.224606353822377258E-16, -0.000000000000000000 ) ) ;
#68134=ORIENTED_EDGE ( 'NONE', *, *, #9145, .F. ) ;
#68147=CONICAL_SURFACE ( 'NONE', #85400, 4.172000000000001485, 0.9599310885968750373 ) ;
#68161=VERTEX_POINT ( 'NONE', #42603 ) ;
#68181=CARTESIAN_POINT ( 'NONE',  ( 38.86638200451619696, 5.000000000000004441, 6.123233995736770227E-16 ) ) ;
#68196=EDGE_CURVE ( 'NONE', #33037, #27928, #58243, .T. ) ;
#68233=CARTESIAN_POINT ( 'NONE',  ( 15.17407431220850533, 1.340359594676612611E-15, 0.000000000000000000 ) ) ;
#68254=EDGE_CURVE ( 'NONE', #71639, #43184, #82350, .T. ) ;
#68299=CONICAL_SURFACE ( 'NONE', #99286, 5.000000000000001776, 0.9599310885968803664 ) ;
#68300=FACE_OUTER_BOUND ( 'NONE', #5699, .T. ) ;
#68343=ORIENTED_EDGE ( 'NONE', *, *, #42361, .T. ) ;
#68354=AXIS2_PLACEMENT_3D ( 'NONE', #78423, #70875, #46592 ) ;
#68398=CYLINDRICAL_SURFACE ( 'NONE', #89405, 5.000000000000002665 ) ;
#68423=ORIENTED_EDGE ( 'NONE', *, *, #69598, .T. ) ;
#68430=ORIENTED_EDGE ( 'NONE', *, *, #58041, .F. ) ;
#68447=VERTEX_POINT ( 'NONE', #18783 ) ;
#68472=DIRECTION ( 'NONE',  ( 0.000000000000000000, -1.000000000000000000, 0.000000000000000000 ) ) ;
#68487=CARTESIAN_POINT ( 'NONE',  ( 0.3167204509598380846, 8.479269695850865318, -1.313474075707212974 ) ) ;
#68508=CARTESIAN_POINT ( 'NONE',  ( 17.81438722625302518, 1.482358050883964840E-15, 0.000000000000000000 ) ) ;
#68510=CARTESIAN_POINT ( 'NONE',  ( 40.02592568779148507, 1.482358050883964840E-15, 0.000000000000000000 ) ) ;
#68512=ADVANCED_FACE ( 'NONE', ( #39062 ), #94534, .T. ) ;
#68518=ORIENTED_EDGE ( 'NONE', *, *, #11330, .F. ) ;
#68533=DIRECTION ( 'NONE',  ( 0.000000000000000000, -1.000000000000000000, 0.000000000000000000 ) ) ;
#68612=EDGE_CURVE ( 'NONE', #95088, #45889, #89362, .T. ) ;
#68624=ORIENTED_EDGE ( 'NONE', *, *, #23335, .T. ) ;
#68633=VERTEX_POINT ( 'NONE', #82142 ) ;
#68654=ORIENTED_EDGE ( 'NONE', *, *, #58934, .T. ) ;
#68724=ORIENTED_EDGE ( 'NONE', *, *, #4236, .T. ) ;
#68735=DIRECTION ( 'NONE',  ( 0.5735764363510468256, 0.8191520442889913545, 0.000000000000000000 ) ) ;
#68769=CIRCLE ( 'NONE', #22265, 8.000000000000000000 ) ;
#68790=CIRCLE ( 'NONE', #65302, 5.000000000000001776 ) ;
#68803=CARTESIAN_POINT ( 'NONE',  ( 20.77592568779148863, 1.482358050883964840E-15, 0.000000000000000000 ) ) ;
#68836=AXIS2_PLACEMENT_3D ( 'NONE', #36024, #68898, #27937 ) ;
#68840=ORIENTED_EDGE ( 'NONE', *, *, #12344, .F. ) ;
#68854=ADVANCED_FACE ( 'NONE', ( #75100 ), #10895, .T. ) ;
#68855=CARTESIAN_POINT ( 'NONE',  ( 35.58361799548379167, 3.851859888774471706E-31, 5.000000000000001776 ) ) ;
#68859=AXIS2_PLACEMENT_3D ( 'NONE', #27855, #29441, #69864 ) ;
#68884=AXIS2_PLACEMENT_3D ( 'NONE', #88854, #40295, #46274 ) ;
#68898=DIRECTION ( 'NONE',  ( -1.000000000000000000, -1.224606353822377258E-16, -0.000000000000000000 ) ) ;
#68903=LINE ( 'NONE', #11153, #45293 ) ;
#68904=CARTESIAN_POINT ( 'NONE',  ( 29.08076923076923137, 4.172000000000003261, 0.000000000000000000 ) ) ;
#68911=EDGE_CURVE ( 'NONE', #68447, #81401, #34702, .T. ) ;
#68918=ADVANCED_FACE ( 'NONE', ( #83730 ), #27148, .T. ) ;
#68920=ORIENTED_EDGE ( 'NONE', *, *, #5855, .T. ) ;
#68946=AXIS2_PLACEMENT_3D ( 'NONE', #99453, #57933, #75175 ) ;
#68956=CARTESIAN_POINT ( 'NONE',  ( 29.98176661990081371, 1.340359594676612611E-15, 0.000000000000000000 ) ) ;
#68963=AXIS2_PLACEMENT_3D ( 'NONE', #47589, #71872, #104778 ) ;
#68986=ORIENTED_EDGE ( 'NONE', *, *, #18862, .T. ) ;
#68995=DIRECTION ( 'NONE',  ( 0.000000000000000000, -1.000000000000000000, 0.000000000000000000 ) ) ;
#69007=DIRECTION ( 'NONE',  ( 0.000000000000000000, -1.000000000000000000, 0.000000000000000000 ) ) ;
#69059=CARTESIAN_POINT ( 'NONE',  ( 27.02022815836235026, 1.340359594676612611E-15, 0.000000000000000000 ) ) ;
#69071=EDGE_CURVE ( 'NONE', #46447, #98765, #60140, .T. ) ;
#69133=ORIENTED_EDGE ( 'NONE', *, *, #105991, .F. ) ;
#69140=CIRCLE ( 'NONE', #60585, 5.000000000000001776 ) ;
#69143=EDGE_CURVE ( 'NONE', #45319, #43284, #97135, .T. ) ;
#69154=DIRECTION ( 'NONE',  ( -0.5735764363510510444, -0.8191520442889883569, 0.000000000000000000 ) ) ;
#69199=CARTESIAN_POINT ( 'NONE',  ( 46.85000000000000142, 0.000000000000000000, 4.171999999999999709 ) ) ;
#69223=CARTESIAN_POINT ( 'NONE',  ( 45.94900261086841198, 5.000000000000002665, 0.000000000000000000 ) ) ;
#69241=VERTEX_POINT ( 'NONE', #73376 ) ;
#69247=DIRECTION ( 'NONE',  ( 1.000000000000000000, 1.224606353822377258E-16, 0.000000000000000000 ) ) ;
#69260=CARTESIAN_POINT ( 'NONE',  ( 29.08076923076923137, -4.171999999999999709, 5.616230220889763424E-16 ) ) ;
#69293=CARTESIAN_POINT ( 'NONE',  ( 8.929771841637641927, -5.000000000000000888, 6.123233995736769241E-16 ) ) ;
#69330=DIRECTION ( 'NONE',  ( -1.000000000000000000, -1.224606353822377258E-16, -0.000000000000000000 ) ) ;
#69333=ORIENTED_EDGE ( 'NONE', *, *, #28208, .T. ) ;
#69368=DIRECTION ( 'NONE',  ( -1.000000000000000000, -0.000000000000000000, -0.000000000000000000 ) ) ;
#69399=CARTESIAN_POINT ( 'NONE',  ( 21.09715123528542691, 0.000000000000000000, 5.000000000000002665 ) ) ;
#69410=EDGE_CURVE ( 'NONE', #65523, #29468, #32710, .T. ) ;
#69415=DIRECTION ( 'NONE',  ( 0.000000000000000000, -1.000000000000000000, 0.000000000000000000 ) ) ;
#69420=DIRECTION ( 'NONE',  ( 0.000000000000000000, -1.000000000000000000, 0.000000000000000000 ) ) ;
#69466=EDGE_CURVE ( 'NONE', #83030, #85853, #106735, .T. ) ;
#69503=CIRCLE ( 'NONE', #40226, 5.000000000000002665 ) ;
#69509=CARTESIAN_POINT ( 'NONE',  ( 21.67692307692307452, 1.411358822780289120E-15, 0.000000000000000000 ) ) ;
#69518=CARTESIAN_POINT ( 'NONE',  ( 0.000000000000000000, 0.000000000000000000, 5.000000000000002665 ) ) ;
#69542=DIRECTION ( 'NONE',  ( -1.000000000000000000, -1.224606353822377258E-16, -0.000000000000000000 ) ) ;
#69575=ORIENTED_EDGE ( 'NONE', *, *, #94959, .T. ) ;
#69579=VECTOR ( 'NONE', #74947, 999.9999999999998863 ) ;
#69582=LINE ( 'NONE', #86313, #46587 ) ;
#69583=CARTESIAN_POINT ( 'NONE',  ( 28.17977184163764193, -5.000000000000000000, 6.123233995736768255E-16 ) ) ;
#69598=EDGE_CURVE ( 'NONE', #9392, #5037, #77538, .T. ) ;
#69623=CARTESIAN_POINT ( 'NONE',  ( 28.50099738913158376, 1.340359594676612611E-15, 0.000000000000000000 ) ) ;
#69638=EDGE_CURVE ( 'NONE', #56216, #34834, #10268, .T. ) ;
#69649=ORIENTED_EDGE ( 'NONE', *, *, #55868, .F. ) ;
#69653=AXIS2_PLACEMENT_3D ( 'NONE', #61991, #78655, #12337 ) ;
#69689=CONICAL_SURFACE ( 'NONE', #26682, 5.000000000000001776, 0.9599310885968803664 ) ;
#69692=CARTESIAN_POINT ( 'NONE',  ( 12.79230769230769305, -4.171999999999999709, 0.000000000000000000 ) ) ;
#69696=EDGE_CURVE ( 'NONE', #19990, #43284, #80866, .T. ) ;
#69701=ORIENTED_EDGE ( 'NONE', *, *, #65703, .F. ) ;
#69742=ORIENTED_EDGE ( 'NONE', *, *, #25025, .F. ) ;
#69757=CARTESIAN_POINT ( 'NONE',  ( 19.29515645702225868, 1.482358050883964840E-15, 0.000000000000000000 ) ) ;
#69769=VECTOR ( 'NONE', #49671, 1000.000000000000227 ) ;
#69790=ORIENTED_EDGE ( 'NONE', *, *, #33519, .T. ) ;
#69817=ORIENTED_EDGE ( 'NONE', *, *, #41743, .T. ) ;
#69840=CIRCLE ( 'NONE', #19921, 8.000000000000000000 ) ;
#69842=ORIENTED_EDGE ( 'NONE', *, *, #87171, .F. ) ;
#69864=DIRECTION ( 'NONE',  ( 0.000000000000000000, -1.000000000000000000, 0.000000000000000000 ) ) ;
#69869=DIRECTION ( 'NONE',  ( -1.000000000000000000, -0.000000000000000000, -0.000000000000000000 ) ) ;
#69942=CARTESIAN_POINT ( 'NONE',  ( 28.17977184163764193, -5.000000000000000888, 6.123233995736769241E-16 ) ) ;
#69964=AXIS2_PLACEMENT_3D ( 'NONE', #105238, #72334, #56663 ) ;
#69977=DIRECTION ( 'NONE',  ( -1.000000000000000000, -0.000000000000000000, -0.000000000000000000 ) ) ;
#69979=CARTESIAN_POINT ( 'NONE',  ( 43.30868969682389036, 6.123233995736770227E-16, -5.000000000000002665 ) ) ;
#69983=CONICAL_SURFACE ( 'NONE', #76830, 5.000000000000001776, 0.9599310885968803664 ) ;
#69984=CYLINDRICAL_SURFACE ( 'NONE', #90529, 5.000000000000002665 ) ;
#69990=ORIENTED_EDGE ( 'NONE', *, *, #77286, .T. ) ;
#70013=EDGE_CURVE ( 'NONE', #76623, #9931, #93048, .T. ) ;
#70059=AXIS2_PLACEMENT_3D ( 'NONE', #92814, #18971, #50738 ) ;
#70085=ORIENTED_EDGE ( 'NONE', *, *, #70232, .F. ) ;
#70088=ORIENTED_EDGE ( 'NONE', *, *, #79577, .T. ) ;
#70105=DIRECTION ( 'NONE',  ( 0.000000000000000000, -1.000000000000000000, 0.000000000000000000 ) ) ;
#70137=ORIENTED_EDGE ( 'NONE', *, *, #3776, .T. ) ;
#70147=DIRECTION ( 'NONE',  ( 0.5735764363510470476, -0.8191520442889911324, 1.003171929053524007E-16 ) ) ;
#70157=EDGE_LOOP ( 'NONE', ( #29091, #50014, #72233, #87917, #1107 ) ) ;
#70216=AXIS2_PLACEMENT_3D ( 'NONE', #92953, #42806, #84335 ) ;
#70219=VERTEX_POINT ( 'NONE', #104324 ) ;
#70232=EDGE_CURVE ( 'NONE', #13600, #47740, #12130, .T. ) ;
#70278=DIRECTION ( 'NONE',  ( 0.000000000000000000, -1.000000000000000000, 0.000000000000000000 ) ) ;
#70282=EDGE_CURVE ( 'NONE', #68161, #29601, #103800, .T. ) ;
#70289=AXIS2_PLACEMENT_3D ( 'NONE', #85116, #20442, #94278 ) ;
#70301=FACE_OUTER_BOUND ( 'NONE', #64681, .T. ) ;
#70326=DIRECTION ( 'NONE',  ( 0.000000000000000000, 0.000000000000000000, 1.000000000000000000 ) ) ;
#70355=CARTESIAN_POINT ( 'NONE',  ( 31.46253585067004721, 6.123233995736770227E-16, -5.000000000000002665 ) ) ;
#70395=ORIENTED_EDGE ( 'NONE', *, *, #100852, .T. ) ;
#70410=CARTESIAN_POINT ( 'NONE',  ( 46.85000000000000142, 0.000000000000000000, 0.000000000000000000 ) ) ;
#70429=DIRECTION ( 'NONE',  ( 0.000000000000000000, -1.000000000000000000, 0.000000000000000000 ) ) ;
#70442=ORIENTED_EDGE ( 'NONE', *, *, #104047, .T. ) ;
#70443=ORIENTED_EDGE ( 'NONE', *, *, #100761, .T. ) ;
#70457=CARTESIAN_POINT ( 'NONE',  ( 0.000000000000000000, 0.000000000000000000, 5.000000000000002665 ) ) ;
#70477=DIRECTION ( 'NONE',  ( -0.5735764363510512664, 0.8191520442889881348, 1.003171929053520309E-16 ) ) ;
#70499=ADVANCED_FACE ( 'NONE', ( #27040 ), #48220, .T. ) ;
#70501=VECTOR ( 'NONE', #97655, 1000.000000000000000 ) ;
#70520=CONICAL_SURFACE ( 'NONE', #60233, 4.172000000000001485, 0.9599310885968750373 ) ;
#70545=EDGE_CURVE ( 'NONE', #68161, #45532, #88429, .T. ) ;
#70556=EDGE_LOOP ( 'NONE', ( #7426, #20419, #80826 ) ) ;
#70566=VECTOR ( 'NONE', #43801, 999.9999999999998863 ) ;
#70576=CARTESIAN_POINT ( 'NONE',  ( 22.25669491856071858, 5.000000000000003553, 0.000000000000000000 ) ) ;
#70582=DIRECTION ( 'NONE',  ( 0.000000000000000000, -1.000000000000000000, 0.000000000000000000 ) ) ;
#70586=DIRECTION ( 'NONE',  ( -0.5735764363510510444, -0.8191520442889883569, 0.000000000000000000 ) ) ;
#70614=CIRCLE ( 'NONE', #75765, 5.000000000000002665 ) ;
#70634=AXIS2_PLACEMENT_3D ( 'NONE', #578, #82606, #41086 ) ;
#70640=CYLINDRICAL_SURFACE ( 'NONE', #59847, 5.000000000000002665 ) ;
#70645=VERTEX_POINT ( 'NONE', #22655 ) ;
#70683=FACE_OUTER_BOUND ( 'NONE', #79410, .T. ) ;
#70699=CARTESIAN_POINT ( 'NONE',  ( 18.13561277374696701, 1.340359594676612611E-15, 0.000000000000000000 ) ) ;
#70708=ORIENTED_EDGE ( 'NONE', *, *, #26695, .F. ) ;
#70739=VECTOR ( 'NONE', #98022, 999.9999999999998863 ) ;
#70756=DIRECTION ( 'NONE',  ( -1.000000000000000000, -1.224606353822377258E-16, -0.000000000000000000 ) ) ;
#70758=CARTESIAN_POINT ( 'NONE',  ( 24.63846153846153797, -4.171999999999999709, 0.000000000000000000 ) ) ;
#70773=EDGE_LOOP ( 'NONE', ( #10607, #77468, #79007, #71439, #37194, #10166 ) ) ;
#70805=DIRECTION ( 'NONE',  ( 0.000000000000000000, -1.000000000000000000, 0.000000000000000000 ) ) ;
#70843=FACE_OUTER_BOUND ( 'NONE', #27428, .T. ) ;
#70875=DIRECTION ( 'NONE',  ( -1.000000000000000000, -1.224606353822377258E-16, -0.000000000000000000 ) ) ;
#70882=EDGE_CURVE ( 'NONE', #86664, #97763, #27729, .T. ) ;
#70908=LINE ( 'NONE', #36984, #51086 ) ;
#70928=ORIENTED_EDGE ( 'NONE', *, *, #34496, .T. ) ;
#70934=CARTESIAN_POINT ( 'NONE',  ( 0.1306530452038122403, -7.903938623646872941, -2.309976723937608778 ) ) ;
#70945=VECTOR ( 'NONE', #70477, 1000.000000000000227 ) ;
#70964=DIRECTION ( 'NONE',  ( -0.5735764363510512664, 0.8191520442889881348, 1.003171929053520309E-16 ) ) ;
#70974=VERTEX_POINT ( 'NONE', #101175 ) ;
#71010=DIRECTION ( 'NONE',  ( 1.000000000000000000, 1.224606353822377258E-16, 0.000000000000000000 ) ) ;
#71011=EDGE_CURVE ( 'NONE', #2234, #57214, #96372, .T. ) ;
#71012=CIRCLE ( 'NONE', #5572, 5.000000000000002665 ) ;
#71074=CARTESIAN_POINT ( 'NONE',  ( 32.62207953394533178, 1.482358050883964840E-15, 0.000000000000000000 ) ) ;
#71117=CARTESIAN_POINT ( 'NONE',  ( 15.17407431220850533, 0.000000000000000000, 5.000000000000002665 ) ) ;
#71147=CYLINDRICAL_SURFACE ( 'NONE', #56172, 5.000000000000002665 ) ;
#71171=VERTEX_POINT ( 'NONE', #105933 ) ;
#71214=DIRECTION ( 'NONE',  ( 0.000000000000000000, -1.000000000000000000, 0.000000000000000000 ) ) ;
#71240=VERTEX_POINT ( 'NONE', #60610 ) ;
#71273=FACE_OUTER_BOUND ( 'NONE', #67240, .T. ) ;
#71325=DIRECTION ( 'NONE',  ( -1.000000000000000000, -1.224606353822377258E-16, -0.000000000000000000 ) ) ;
#71344=ADVANCED_FACE ( 'NONE', ( #13609 ), #55225, .T. ) ;
#71346=EDGE_CURVE ( 'NONE', #106160, #95837, #101518, .T. ) ;
#71372=CARTESIAN_POINT ( 'NONE',  ( 6.849999999999999645, 9.237604307034018802, 0.000000000000000000 ) ) ;
#71377=ORIENTED_EDGE ( 'NONE', *, *, #42472, .F. ) ;
#71387=CARTESIAN_POINT ( 'NONE',  ( 23.73746414932995208, 3.851859888774471706E-31, 5.000000000000001776 ) ) ;
#71421=VERTEX_POINT ( 'NONE', #71848 ) ;
#71429=CIRCLE ( 'NONE', #80053, 5.000000000000001776 ) ;
#71434=CIRCLE ( 'NONE', #726, 4.172000000000001485 ) ;
#71439=ORIENTED_EDGE ( 'NONE', *, *, #25794, .T. ) ;
#71481=ORIENTED_EDGE ( 'NONE', *, *, #19505, .F. ) ;
#71493=ORIENTED_EDGE ( 'NONE', *, *, #45758, .F. ) ;
#71508=VECTOR ( 'NONE', #49991, 999.9999999999998863 ) ;
#71518=AXIS2_PLACEMENT_3D ( 'NONE', #25892, #74895, #75977 ) ;
#71520=ORIENTED_EDGE ( 'NONE', *, *, #94575, .F. ) ;
#71528=EDGE_CURVE ( 'NONE', #24694, #29313, #48143, .T. ) ;
#71539=DIRECTION ( 'NONE',  ( -0.5735764363510510444, -0.8191520442889883569, 0.000000000000000000 ) ) ;
#71568=ADVANCED_FACE ( 'NONE', ( #47040 ), #77503, .T. ) ;
#71608=ADVANCED_FACE ( 'NONE', ( #91252 ), #6881, .T. ) ;
#71612=DIRECTION ( 'NONE',  ( 0.000000000000000000, -1.000000000000000000, 0.000000000000000000 ) ) ;
#71639=VERTEX_POINT ( 'NONE', #72385 ) ;
#71654=VECTOR ( 'NONE', #39151, 1000.000000000000000 ) ;
#71657=DIRECTION ( 'NONE',  ( 0.5735764363510470476, -0.8191520442889911324, 1.003171929053524007E-16 ) ) ;
#71665=DIRECTION ( 'NONE',  ( -1.000000000000000000, -0.000000000000000000, -0.000000000000000000 ) ) ;
#71686=ORIENTED_EDGE ( 'NONE', *, *, #10161, .T. ) ;
#71693=DIRECTION ( 'NONE',  ( -1.000000000000000000, -1.224606353822377258E-16, -0.000000000000000000 ) ) ;
#71713=DIRECTION ( 'NONE',  ( -1.000000000000000000, -1.224606353822377258E-16, -0.000000000000000000 ) ) ;
#71733=AXIS2_PLACEMENT_3D ( 'NONE', #46169, #79583, #5178 ) ;
#71770=VECTOR ( 'NONE', #8706, 999.9999999999998863 ) ;
#71789=CARTESIAN_POINT ( 'NONE',  ( 10.41054107240687188, -5.000000000000000000, 6.123233995736768255E-16 ) ) ;
#71821=ORIENTED_EDGE ( 'NONE', *, *, #65543, .F. ) ;
#71838=CARTESIAN_POINT ( 'NONE',  ( 40.34715123528543046, 0.000000000000000000, 5.000000000000002665 ) ) ;
#71848=CARTESIAN_POINT ( 'NONE',  ( 0.7145311798163216377, 4.618802153517004960, 7.999999999999998224 ) ) ;
#71872=DIRECTION ( 'NONE',  ( -1.000000000000000000, -1.224606353822377258E-16, -0.000000000000000000 ) ) ;
#71873=CARTESIAN_POINT ( 'NONE',  ( 15.75384615384615294, -4.171999999999999709, 5.616230220889763424E-16 ) ) ;
#71878=CARTESIAN_POINT ( 'NONE',  ( -5.559924265777227426E-15, -7.321656987762867885, 3.318518101603013193 ) ) ;
#71883=EDGE_CURVE ( 'NONE', #58211, #27928, #56459, .T. ) ;
#71911=DIRECTION ( 'NONE',  ( 1.000000000000000000, 0.000000000000000000, -0.000000000000000000 ) ) ;
#72047=ORIENTED_EDGE ( 'NONE', *, *, #40524, .T. ) ;
#72063=DIRECTION ( 'NONE',  ( 0.000000000000000000, -1.000000000000000000, 0.000000000000000000 ) ) ;
#72100=DIRECTION ( 'NONE',  ( -1.000000000000000000, -0.000000000000000000, -0.000000000000000000 ) ) ;
#72106=ORIENTED_EDGE ( 'NONE', *, *, #80421, .T. ) ;
#72149=EDGE_CURVE ( 'NONE', #14152, #2234, #32704, .T. ) ;
#72150=DIRECTION ( 'NONE',  ( -1.000000000000000000, -1.224606353822377258E-16, -0.000000000000000000 ) ) ;
#72152=EDGE_LOOP ( 'NONE', ( #88571, #15804, #12455 ) ) ;
#72169=DIRECTION ( 'NONE',  ( 0.000000000000000000, -1.000000000000000000, 0.000000000000000000 ) ) ;
#72219=ORIENTED_EDGE ( 'NONE', *, *, #42361, .F. ) ;
#72220=ADVANCED_FACE ( 'NONE', ( #15892 ), #93041, .T. ) ;
#72233=ORIENTED_EDGE ( 'NONE', *, *, #58041, .T. ) ;
#72256=VERTEX_POINT ( 'NONE', #57397 ) ;
#72264=DIRECTION ( 'NONE',  ( -1.000000000000000000, -0.000000000000000000, -0.000000000000000000 ) ) ;
#72265=FACE_OUTER_BOUND ( 'NONE', #43713, .T. ) ;
#72287=VERTEX_POINT ( 'NONE', #85418 ) ;
#72291=DIRECTION ( 'NONE',  ( -0.5735764363510510444, -0.8191520442889883569, 0.000000000000000000 ) ) ;
#72324=DIRECTION ( 'NONE',  ( 0.000000000000000000, 0.000000000000000000, -1.000000000000000000 ) ) ;
#72325=DIRECTION ( 'NONE',  ( 0.000000000000000000, -1.000000000000000000, 0.000000000000000000 ) ) ;
#72330=DIRECTION ( 'NONE',  ( 0.000000000000000000, -1.000000000000000000, 0.000000000000000000 ) ) ;
#72334=DIRECTION ( 'NONE',  ( -1.000000000000000000, -1.224606353822377258E-16, -0.000000000000000000 ) ) ;
#72341=DIRECTION ( 'NONE',  ( -1.000000000000000000, -1.224606353822377258E-16, -0.000000000000000000 ) ) ;
#72366=CONICAL_SURFACE ( 'NONE', #6922, 4.172000000000001485, 0.9599310885968750373 ) ;
#72369=EDGE_LOOP ( 'NONE', ( #56714, #86886, #99567, #94314, #35514, #30106 ) ) ;
#72385=CARTESIAN_POINT ( 'NONE',  ( 6.849999999999999645, 0.000000000000000000, 5.000000000000002665 ) ) ;
#72401=EDGE_CURVE ( 'NONE', #13600, #73449, #3505, .T. ) ;
#72403=AXIS2_PLACEMENT_3D ( 'NONE', #32639, #49300, #74114 ) ;
#72420=EDGE_CURVE ( 'NONE', #58381, #83030, #36274, .T. ) ;
#72433=CONICAL_SURFACE ( 'NONE', #24343, 5.000000000000001776, 0.9599310885968803664 ) ;
#72440=DIRECTION ( 'NONE',  ( -1.000000000000000000, -1.224606353822377258E-16, -0.000000000000000000 ) ) ;
#72452=ORIENTED_EDGE ( 'NONE', *, *, #102568, .F. ) ;
#72477=CARTESIAN_POINT ( 'NONE',  ( 0.4969600502617456672, -4.995646404165269061, 7.347286611336970807 ) ) ;
#72490=DIRECTION ( 'NONE',  ( 0.000000000000000000, -1.000000000000000000, 0.000000000000000000 ) ) ;
#72505=CARTESIAN_POINT ( 'NONE',  ( 0.000000000000000000, 0.000000000000000000, 0.000000000000000000 ) ) ;
#72535=ORIENTED_EDGE ( 'NONE', *, *, #45008, .T. ) ;
#72557=DIRECTION ( 'NONE',  ( 0.000000000000000000, 0.000000000000000000, 1.000000000000000000 ) ) ;
#72558=AXIS2_PLACEMENT_3D ( 'NONE', #28048, #53348, #54370 ) ;
#72566=ORIENTED_EDGE ( 'NONE', *, *, #16088, .T. ) ;
#72627=DIRECTION ( 'NONE',  ( -1.000000000000000000, -0.000000000000000000, -0.000000000000000000 ) ) ;
#72654=ORIENTED_EDGE ( 'NONE', *, *, #98771, .T. ) ;
#72690=CIRCLE ( 'NONE', #48572, 4.172000000000001485 ) ;
#72716=DIRECTION ( 'NONE',  ( -1.000000000000000000, -1.224606353822377258E-16, -0.000000000000000000 ) ) ;
#72770=EDGE_LOOP ( 'NONE', ( #82979, #105531, #12146, #51742, #32505, #26339 ) ) ;
#72786=AXIS2_PLACEMENT_3D ( 'NONE', #32669, #31088, #24578 ) ;
#72789=ORIENTED_EDGE ( 'NONE', *, *, #103652, .T. ) ;
#72795=FACE_OUTER_BOUND ( 'NONE', #80581, .T. ) ;
#72807=DIRECTION ( 'NONE',  ( -1.000000000000000000, -0.000000000000000000, -0.000000000000000000 ) ) ;
#72848=EDGE_CURVE ( 'NONE', #14796, #90464, #75874, .T. ) ;
#72850=ORIENTED_EDGE ( 'NONE', *, *, #86111, .F. ) ;
#72873=DIRECTION ( 'NONE',  ( 0.000000000000000000, -1.000000000000000000, 0.000000000000000000 ) ) ;
#72904=CARTESIAN_POINT ( 'NONE',  ( 0.000000000000000000, 6.123233995736770227E-16, -5.000000000000002665 ) ) ;
#72906=EDGE_CURVE ( 'NONE', #60839, #51590, #101665, .T. ) ;
#73010=DIRECTION ( 'NONE',  ( -1.000000000000000000, -1.224606353822377258E-16, -0.000000000000000000 ) ) ;
#73109=AXIS2_PLACEMENT_3D ( 'NONE', #89215, #82707, #98358 ) ;
#73121=EDGE_CURVE ( 'NONE', #51590, #71639, #3867, .T. ) ;
#73163=DIRECTION ( 'NONE',  ( -1.000000000000000000, -1.224606353822377258E-16, -0.000000000000000000 ) ) ;
#73189=ORIENTED_EDGE ( 'NONE', *, *, #46713, .T. ) ;
#73193=CYLINDRICAL_SURFACE ( 'NONE', #75898, 5.000000000000002665 ) ;
#73201=CARTESIAN_POINT ( 'NONE',  ( 12.21253585067004543, 1.340359594676612611E-15, 0.000000000000000000 ) ) ;
#73204=EDGE_CURVE ( 'NONE', #94186, #12693, #27717, .T. ) ;
#73223=DIRECTION ( 'NONE',  ( -1.000000000000000000, -1.224606353822377258E-16, -0.000000000000000000 ) ) ;
#73229=AXIS2_PLACEMENT_3D ( 'NONE', #61071, #86424, #11963 ) ;
#73252=EDGE_LOOP ( 'NONE', ( #86989, #84925, #23659, #71377, #8419, #98432 ) ) ;
#73262=AXIS2_PLACEMENT_3D ( 'NONE', #78904, #11501, #76778 ) ;
#73263=CARTESIAN_POINT ( 'NONE',  ( 32.62207953394533178, 1.482358050883964840E-15, 0.000000000000000000 ) ) ;
#73273=CIRCLE ( 'NONE', #47501, 5.000000000000001776 ) ;
#73292=ORIENTED_EDGE ( 'NONE', *, *, #47294, .T. ) ;
#73309=EDGE_LOOP ( 'NONE', ( #90217, #2351, #54851, #97265, #19568, #11727 ) ) ;
#73321=FACE_OUTER_BOUND ( 'NONE', #28433, .T. ) ;
#73331=ORIENTED_EDGE ( 'NONE', *, *, #36551, .T. ) ;
#73335=CYLINDRICAL_SURFACE ( 'NONE', #1430, 5.000000000000002665 ) ;
#73350=CARTESIAN_POINT ( 'NONE',  ( 19.29515645702225868, 5.000000000000002665, 0.000000000000000000 ) ) ;
#73351=CARTESIAN_POINT ( 'NONE',  ( 25.53945892759312031, 6.123233995736770227E-16, -5.000000000000002665 ) ) ;
#73359=DIRECTION ( 'NONE',  ( 0.000000000000000000, -1.000000000000000000, 0.000000000000000000 ) ) ;
#73375=EDGE_CURVE ( 'NONE', #65067, #55144, #39776, .T. ) ;
#73376=CARTESIAN_POINT ( 'NONE',  ( 44.78945892759311675, 5.000000000000015099, 6.123233995736782060E-16 ) ) ;
#73383=( LENGTH_UNIT ( ) NAMED_UNIT ( * ) SI_UNIT ( .MILLI., .METRE. ) );
#73437=DIRECTION ( 'NONE',  ( 0.000000000000000000, -1.000000000000000000, 0.000000000000000000 ) ) ;
#73449=VERTEX_POINT ( 'NONE', #51198 ) ;
#73501=VECTOR ( 'NONE', #101790, 999.9999999999998863 ) ;
#73508=ORIENTED_EDGE ( 'NONE', *, *, #49072, .T. ) ;
#73512=DIRECTION ( 'NONE',  ( 0.000000000000000000, -1.000000000000000000, 0.000000000000000000 ) ) ;
#73528=VERTEX_POINT ( 'NONE', #71117 ) ;
#73589=CIRCLE ( 'NONE', #46059, 5.000000000000001776 ) ;
#73594=ORIENTED_EDGE ( 'NONE', *, *, #102333, .F. ) ;
#73604=EDGE_CURVE ( 'NONE', #53057, #72256, #89817, .T. ) ;
#73643=VECTOR ( 'NONE', #30754, 1000.000000000000000 ) ;
#73652=CIRCLE ( 'NONE', #6438, 4.172000000000001485 ) ;
#73682=CARTESIAN_POINT ( 'NONE',  ( 13.37207953394533355, 3.851859888774471706E-31, 5.000000000000001776 ) ) ;
#73683=FACE_OUTER_BOUND ( 'NONE', #16031, .T. ) ;
#73708=ORIENTED_EDGE ( 'NONE', *, *, #99432, .F. ) ;
#73729=CARTESIAN_POINT ( 'NONE',  ( 0.7145311798163210826, 4.618802153517001408, -8.000000000000000000 ) ) ;
#73741=DIRECTION ( 'NONE',  ( 0.000000000000000000, 0.000000000000000000, -1.000000000000000000 ) ) ;
#73756=DIRECTION ( 'NONE',  ( -1.000000000000000000, -1.224606353822377258E-16, -0.000000000000000000 ) ) ;
#73757=CYLINDRICAL_SURFACE ( 'NONE', #19725, 5.000000000000002665 ) ;
#73787=AXIS2_PLACEMENT_3D ( 'NONE', #29917, #97797, #7192 ) ;
#73830=AXIS2_PLACEMENT_3D ( 'NONE', #39842, #30709, #55980 ) ;
#73838=ORIENTED_EDGE ( 'NONE', *, *, #78132, .F. ) ;
#73844=CARTESIAN_POINT ( 'NONE',  ( 0.000000000000000000, 0.000000000000000000, 5.000000000000002665 ) ) ;
#73853=FACE_OUTER_BOUND ( 'NONE', #14564, .T. ) ;
#73855=VERTEX_POINT ( 'NONE', #10622 ) ;
#73864=CARTESIAN_POINT ( 'NONE',  ( 35.90484354297773706, 1.340359594676612611E-15, 0.000000000000000000 ) ) ;
#73878=LINE ( 'NONE', #7018, #63684 ) ;
#73890=ORIENTED_EDGE ( 'NONE', *, *, #55096, .T. ) ;
#73934=VECTOR ( 'NONE', #92651, 1000.000000000000227 ) ;
#73944=FACE_OUTER_BOUND ( 'NONE', #54731, .T. ) ;
#73958=VERTEX_POINT ( 'NONE', #82927 ) ;
#73966=LINE ( 'NONE', #48620, #71770 ) ;
#73997=DIRECTION ( 'NONE',  ( -1.000000000000000000, -1.224606353822377258E-16, -0.000000000000000000 ) ) ;
#74005=VERTEX_POINT ( 'NONE', #91568 ) ;
#74019=ORIENTED_EDGE ( 'NONE', *, *, #30380, .F. ) ;
#74027=CARTESIAN_POINT ( 'NONE',  ( 12.79230769230769305, 4.172000000000003261, 0.000000000000000000 ) ) ;
#74062=ORIENTED_EDGE ( 'NONE', *, *, #68911, .F. ) ;
#74065=EDGE_CURVE ( 'NONE', #31075, #24250, #55362, .T. ) ;
#74069=ADVANCED_FACE ( 'NONE', ( #19841 ), #41600, .T. ) ;
#74084=VERTEX_POINT ( 'NONE', #94767 ) ;
#74092=ORIENTED_EDGE ( 'NONE', *, *, #43450, .T. ) ;
#74099=CARTESIAN_POINT ( 'NONE',  ( 14.85284876471456350, 1.482358050883964840E-15, 0.000000000000000000 ) ) ;
#74113=CARTESIAN_POINT ( 'NONE',  ( 0.000000000000000000, 0.000000000000000000, 0.000000000000000000 ) ) ;
#74114=DIRECTION ( 'NONE',  ( 0.000000000000000000, 1.000000000000000000, 0.000000000000000000 ) ) ;
#74126=ORIENTED_EDGE ( 'NONE', *, *, #62711, .T. ) ;
#74131=ORIENTED_EDGE ( 'NONE', *, *, #38130, .F. ) ;
#74149=EDGE_CURVE ( 'NONE', #84262, #87039, #20386, .T. ) ;
#74152=DIRECTION ( 'NONE',  ( -1.000000000000000000, -1.224606353822377258E-16, -0.000000000000000000 ) ) ;
#74166=DIRECTION ( 'NONE',  ( -1.000000000000000000, -1.224606353822377258E-16, -0.000000000000000000 ) ) ;
#74195=EDGE_CURVE ( 'NONE', #42925, #31421, #7175, .T. ) ;
#74196=EDGE_LOOP ( 'NONE', ( #52605, #32844, #31017, #4705, #24744, #68840 ) ) ;
#74220=CARTESIAN_POINT ( 'NONE',  ( 32.04230769230768772, 1.411358822780289120E-15, 0.000000000000000000 ) ) ;
#74226=EDGE_CURVE ( 'NONE', #104720, #70219, #21028, .T. ) ;
#74230=AXIS2_PLACEMENT_3D ( 'NONE', #16096, #48977, #24750 ) ;
#74260=ORIENTED_EDGE ( 'NONE', *, *, #78370, .F. ) ;
#74276=DIRECTION ( 'NONE',  ( 0.000000000000000000, 0.000000000000000000, 1.000000000000000000 ) ) ;
#74284=ORIENTED_EDGE ( 'NONE', *, *, #92312, .T. ) ;
#74293=EDGE_CURVE ( 'NONE', #4337, #2494, #9968, .T. ) ;
#74329=CIRCLE ( 'NONE', #41627, 5.000000000000001776 ) ;
#74371=CIRCLE ( 'NONE', #19327, 5.000000000000001776 ) ;
#74379=ORIENTED_EDGE ( 'NONE', *, *, #103147, .T. ) ;
#74446=EDGE_CURVE ( 'NONE', #18270, #48268, #91584, .T. ) ;
#74468=LINE ( 'NONE', #25988, #33744 ) ;
#74480=CARTESIAN_POINT ( 'NONE',  ( 37.96538461538461462, 1.411358822780289120E-15, 0.000000000000000000 ) ) ;
#74497=ORIENTED_EDGE ( 'NONE', *, *, #1070, .F. ) ;
#74518=ORIENTED_EDGE ( 'NONE', *, *, #49103, .F. ) ;
#74537=ORIENTED_EDGE ( 'NONE', *, *, #8335, .T. ) ;
#74547=ADVANCED_FACE ( 'NONE', ( #22076 ), #87859, .T. ) ;
#74627=AXIS2_PLACEMENT_3D ( 'NONE', #59038, #58504, #42842 ) ;
#74666=EDGE_CURVE ( 'NONE', #11758, #33126, #26188, .T. ) ;
#74675=VECTOR ( 'NONE', #46363, 999.9999999999998863 ) ;
#74701=VECTOR ( 'NONE', #49344, 999.9999999999998863 ) ;
#74729=CARTESIAN_POINT ( 'NONE',  ( 0.000000000000000000, 0.000000000000000000, 5.000000000000002665 ) ) ;
#74748=DIRECTION ( 'NONE',  ( 0.000000000000000000, -1.000000000000000000, 0.000000000000000000 ) ) ;
#74786=ORIENTED_EDGE ( 'NONE', *, *, #48465, .F. ) ;
#74840=DIRECTION ( 'NONE',  ( 0.000000000000000000, 1.000000000000000000, 0.000000000000000000 ) ) ;
#74895=DIRECTION ( 'NONE',  ( -1.000000000000000000, -1.224606353822377258E-16, -0.000000000000000000 ) ) ;
#74925=DIRECTION ( 'NONE',  ( 1.000000000000000000, 1.224606353822377258E-16, 0.000000000000000000 ) ) ;
#74943=ORIENTED_EDGE ( 'NONE', *, *, #87460, .T. ) ;
#74947=DIRECTION ( 'NONE',  ( 0.5735764363510468256, 0.8191520442889913545, 0.000000000000000000 ) ) ;
#74966=DIRECTION ( 'NONE',  ( -1.000000000000000000, -1.224606353822377258E-16, -0.000000000000000000 ) ) ;
#74997=ORIENTED_EDGE ( 'NONE', *, *, #57883, .F. ) ;
#75007=EDGE_CURVE ( 'NONE', #48472, #95649, #31635, .T. ) ;
#75051=DIRECTION ( 'NONE',  ( 0.000000000000000000, -1.000000000000000000, 0.000000000000000000 ) ) ;
#75066=CIRCLE ( 'NONE', #64765, 5.000000000000001776 ) ;
#75070=ADVANCED_FACE ( 'NONE', ( #57455 ), #91658, .T. ) ;
#75082=DIRECTION ( 'NONE',  ( -1.000000000000000000, -1.224606353822377258E-16, -0.000000000000000000 ) ) ;
#75100=FACE_OUTER_BOUND ( 'NONE', #83121, .T. ) ;
#75127=B_SPLINE_CURVE_WITH_KNOTS ( 'NONE', 3,
 ( #106422, #63350, #88669, #96250, #39070, #30998, #72477, #22898 ),
 .UNSPECIFIED., .F., .F.,
 ( 4, 2, 2, 4 ),
 ( 0.004673709593152172194, 0.005837709341827658147, 0.007001709090503144967, 0.009329708587854115137 ),
 .UNSPECIFIED. ) ;
#75155=EDGE_CURVE ( 'NONE', #4042, #22420, #71012, .T. ) ;
#75175=DIRECTION ( 'NONE',  ( 0.000000000000000000, -1.000000000000000000, 0.000000000000000000 ) ) ;
#75180=CIRCLE ( 'NONE', #14888, 5.000000000000002665 ) ;
#75185=AXIS2_PLACEMENT_3D ( 'NONE', #48824, #55331, #72063 ) ;
#75186=CARTESIAN_POINT ( 'NONE',  ( 17.81438722625302518, 5.000000000000002665, 0.000000000000000000 ) ) ;
#75194=VECTOR ( 'NONE', #66656, 1000.000000000000000 ) ;
#75200=EDGE_CURVE ( 'NONE', #8257, #24684, #37579, .T. ) ;
#75203=DIRECTION ( 'NONE',  ( -0.5735764363510512664, 0.8191520442889881348, 1.003171929053520309E-16 ) ) ;
#75232=LINE ( 'NONE', #100581, #52796 ) ;
#75282=VERTEX_POINT ( 'NONE', #26746 ) ;
#75287=CARTESIAN_POINT ( 'NONE',  ( 21.09715123528542691, 1.340359594676612611E-15, 0.000000000000000000 ) ) ;
#75289=CARTESIAN_POINT ( 'NONE',  ( 6.249999999999998224, 8.000000000000000000, 0.000000000000000000 ) ) ;
#75309=CARTESIAN_POINT ( 'NONE',  ( 0.000000000000000000, 0.000000000000000000, 0.000000000000000000 ) ) ;
#75326=DIRECTION ( 'NONE',  ( -1.000000000000000000, -0.000000000000000000, -0.000000000000000000 ) ) ;
#75343=CARTESIAN_POINT ( 'NONE',  ( 6.849999999999999645, 4.618802153517001408, -8.000000000000000000 ) ) ;
#75348=DIRECTION ( 'NONE',  ( 0.000000000000000000, 0.000000000000000000, -1.000000000000000000 ) ) ;
#75350=CARTESIAN_POINT ( 'NONE',  ( 29.66054107240687543, 5.000000000000003553, 0.000000000000000000 ) ) ;
#75352=AXIS2_PLACEMENT_3D ( 'NONE', #42244, #34200, #67072 ) ;
#75355=VECTOR ( 'NONE', #69154, 1000.000000000000000 ) ;
#75375=DIRECTION ( 'NONE',  ( -1.000000000000000000, -0.000000000000000000, -0.000000000000000000 ) ) ;
#75401=AXIS2_PLACEMENT_3D ( 'NONE', #86877, #12950, #38334 ) ;
#75422=DIRECTION ( 'NONE',  ( -0.5735764363510510444, -0.8191520442889883569, 0.000000000000000000 ) ) ;
#75471=FACE_OUTER_BOUND ( 'NONE', #50739, .T. ) ;
#75486=ORIENTED_EDGE ( 'NONE', *, *, #23428, .T. ) ;
#75496=EDGE_CURVE ( 'NONE', #86992, #15625, #30707, .T. ) ;
#75525=DIRECTION ( 'NONE',  ( 0.000000000000000000, -1.000000000000000000, 0.000000000000000000 ) ) ;
#75532=DIRECTION ( 'NONE',  ( -1.000000000000000000, -0.000000000000000000, -0.000000000000000000 ) ) ;
#75539=ORIENTED_EDGE ( 'NONE', *, *, #50775, .T. ) ;
#75560=VERTEX_POINT ( 'NONE', #6134 ) ;
#75587=AXIS2_PLACEMENT_3D ( 'NONE', #105077, #39290, #72169 ) ;
#75604=ORIENTED_EDGE ( 'NONE', *, *, #71528, .T. ) ;
#75612=DIRECTION ( 'NONE',  ( 0.000000000000000000, 0.000000000000000000, 1.000000000000000000 ) ) ;
#75621=AXIS2_PLACEMENT_3D ( 'NONE', #23899, #6605, #40047 ) ;
#75623=CARTESIAN_POINT ( 'NONE',  ( 0.000000000000000000, 0.000000000000000000, 0.000000000000000000 ) ) ;
#75630=VERTEX_POINT ( 'NONE', #46607 ) ;
#75632=CLOSED_SHELL ( 'NONE', ( #5091, #31767, #27022, #12503, #16205, #41211, #4876, #80292, #16821, #57892, #12028, #32848, #52953, #74547, #90627, #12710, #56539, #37929, #72220, #6479, #96165, #42601, #88517, #87249, #57925, #4820, #99404, #54826, #88060, #45592, #105434, #96244, #34934, #71344, #28569, #91073, #1849, #16977, #23422, #42993, #66577, #16380, #52184, #28036, #3480, #76354, #30988, #98886, #71568, #83210, #19078, #68512, #103207, #102434, #8609, #103665, #28789, #58062, #48828, #89777, #16608, #15865, #11105, #71608, #4482, #50922, #36635, #68918, #88926, #50964, #68854, #98044, #32016, #97296, #47044, #57631, #86743, #79316, #98357, #10878, #66253, #11352, #63362, #66031, #5702, #78755, #55024, #31639, #21795, #45482, #1523, #44613, #33371, #89833, #104966, #22519, #87320, #7318, #106424, #52157, #82219, #23676, #89802, #48420, #22206, #9795, #38103, #14496, #30316, #105473, #6794, #39584, #6127, #63792, #33949, #52828, #32923, #93920, #27649, #88071, #39289, #1714, #7726, #49472, #8537, #7017, #60397, #58201, #98602, #50326, #57758, #42278, #77105, #66919, #25860, #34222, #75070, #81952, #25982, #18573, #44126, #50528, #63315, #86260, #45204, #101291, #74069, #14771, #103304, #303, #46208, #84721, #5574, #89272, #31408, #70499, #22342, #34293, #12783, #89969, #96885, #47041, #52008, #57218, #5903, #49329, #89784, #14132, #81575, #67358, #3082, #102190, #22813, #103668, #4611, #95034, #36155, #88270, #78495, #76764, #50802, #13972, #84219 ) ) ;
#75671=ORIENTED_EDGE ( 'NONE', *, *, #4016, .T. ) ;
#75717=CARTESIAN_POINT ( 'NONE',  ( 41.82792046605465686, 1.340359594676612611E-15, 0.000000000000000000 ) ) ;
#75719=FACE_OUTER_BOUND ( 'NONE', #20237, .T. ) ;
#75731=ORIENTED_EDGE ( 'NONE', *, *, #69696, .F. ) ;
#75734=ORIENTED_EDGE ( 'NONE', *, *, #90948, .F. ) ;
#75765=AXIS2_PLACEMENT_3D ( 'NONE', #51634, #52694, #85621 ) ;
#75771=CIRCLE ( 'NONE', #62019, 5.000000000000002665 ) ;
#75773=DIRECTION ( 'NONE',  ( -1.000000000000000000, -0.000000000000000000, -0.000000000000000000 ) ) ;
#75788=CARTESIAN_POINT ( 'NONE',  ( 7.770228158362351145, 1.340359594676612611E-15, 0.000000000000000000 ) ) ;
#75821=CARTESIAN_POINT ( 'NONE',  ( 0.000000000000000000, 0.000000000000000000, 0.000000000000000000 ) ) ;
#75840=DIRECTION ( 'NONE',  ( -1.000000000000000000, -1.224606353822377258E-16, -0.000000000000000000 ) ) ;
#75874=CIRCLE ( 'NONE', #84425, 5.000000000000001776 ) ;
#75895=EDGE_CURVE ( 'NONE', #4337, #20128, #104729, .T. ) ;
#75898=AXIS2_PLACEMENT_3D ( 'NONE', #57019, #89933, #15509 ) ;
#75907=CARTESIAN_POINT ( 'NONE',  ( 6.249999999999998224, 6.928203230275504332, -4.000000000000007994 ) ) ;
#75909=AXIS2_PLACEMENT_3D ( 'NONE', #76510, #3708, #92697 ) ;
#75910=AXIS2_PLACEMENT_3D ( 'NONE', #5679, #86100, #102793 ) ;
#75927=DIRECTION ( 'NONE',  ( -1.000000000000000000, -0.000000000000000000, -0.000000000000000000 ) ) ;
#75968=PRODUCT ( 'hex screw gradec_din_DIN EN 24018 - M10 x 40-WS', 'hex screw gradec_din_DIN EN 24018 - M10 x 40-WS', '', ( #38527 ) ) ;
#75977=DIRECTION ( 'NONE',  ( 0.000000000000000000, -1.000000000000000000, 0.000000000000000000 ) ) ;
#75984=ORIENTED_EDGE ( 'NONE', *, *, #40339, .T. ) ;
#76015=DIRECTION ( 'NONE',  ( 0.000000000000000000, -1.000000000000000000, 0.000000000000000000 ) ) ;
#76053=EDGE_CURVE ( 'NONE', #64182, #42513, #23850, .T. ) ;
#76065=VERTEX_POINT ( 'NONE', #42623 ) ;
#76068=DIRECTION ( 'NONE',  ( 0.000000000000000000, -1.000000000000000000, 0.000000000000000000 ) ) ;
#76087=DIRECTION ( 'NONE',  ( 0.000000000000000000, -1.000000000000000000, 0.000000000000000000 ) ) ;
#76092=EDGE_CURVE ( 'NONE', #49621, #19990, #63489, .T. ) ;
#76114=LINE ( 'NONE', #2211, #81721 ) ;
#76115=EDGE_CURVE ( 'NONE', #86142, #86773, #41566, .T. ) ;
#76129=CARTESIAN_POINT ( 'NONE',  ( 11.89131030317610183, -5.000000000000000888, 6.123233995736769241E-16 ) ) ;
#76135=LINE ( 'NONE', #92315, #21836 ) ;
#76147=ORIENTED_EDGE ( 'NONE', *, *, #15996, .T. ) ;
#76164=LINE ( 'NONE', #28200, #70566 ) ;
#76220=VERTEX_POINT ( 'NONE', #2694 ) ;
#76251=FACE_OUTER_BOUND ( 'NONE', #35689, .T. ) ;
#76256=EDGE_CURVE ( 'NONE', #12690, #35868, #52308, .T. ) ;
#76258=AXIS2_PLACEMENT_3D ( 'NONE', #17154, #73223, #25816 ) ;
#76276=FACE_OUTER_BOUND ( 'NONE', #50268, .T. ) ;
#76303=DIRECTION ( 'NONE',  ( -1.000000000000000000, -1.224606353822377258E-16, -0.000000000000000000 ) ) ;
#76320=DIRECTION ( 'NONE',  ( -1.000000000000000000, -1.224606353822377258E-16, -0.000000000000000000 ) ) ;
#76339=DIRECTION ( 'NONE',  ( 0.000000000000000000, -1.000000000000000000, 0.000000000000000000 ) ) ;
#76342=DIRECTION ( 'NONE',  ( 0.000000000000000000, 1.000000000000000000, 0.000000000000000000 ) ) ;
#76344=FACE_OUTER_BOUND ( 'NONE', #57854, .T. ) ;
#76345=ORIENTED_EDGE ( 'NONE', *, *, #11209, .F. ) ;
#76354=ADVANCED_FACE ( 'NONE', ( #48849 ), #106498, .T. ) ;
#76365=ORIENTED_EDGE ( 'NONE', *, *, #87637, .T. ) ;
#76470=ORIENTED_EDGE ( 'NONE', *, *, #47201, .T. ) ;
#76510=CARTESIAN_POINT ( 'NONE',  ( 30.56153846153846132, 1.411358822780289120E-15, 0.000000000000000000 ) ) ;
#76512=EDGE_LOOP ( 'NONE', ( #18687, #74260, #58619, #68724, #96864 ) ) ;
#76565=CARTESIAN_POINT ( 'NONE',  ( 44.78945892759311675, 0.000000000000000000, 5.000000000000002665 ) ) ;
#76600=ORIENTED_EDGE ( 'NONE', *, *, #2307, .T. ) ;
#76603=DIRECTION ( 'NONE',  ( -1.000000000000000000, -1.224606353822377258E-16, -0.000000000000000000 ) ) ;
#76621=CARTESIAN_POINT ( 'NONE',  ( 19.61638200451619696, 0.000000000000000000, 5.000000000000002665 ) ) ;
#76623=VERTEX_POINT ( 'NONE', #625 ) ;
#76653=DIRECTION ( 'NONE',  ( -1.000000000000000000, -0.000000000000000000, -0.000000000000000000 ) ) ;
#76665=DIRECTION ( 'NONE',  ( -1.000000000000000000, -0.000000000000000000, -0.000000000000000000 ) ) ;
#76681=CIRCLE ( 'NONE', #47350, 5.000000000000001776 ) ;
#76751=ORIENTED_EDGE ( 'NONE', *, *, #86111, .T. ) ;
#76752=DIRECTION ( 'NONE',  ( -1.000000000000000000, -1.224606353822377258E-16, -0.000000000000000000 ) ) ;
#76761=FACE_OUTER_BOUND ( 'NONE', #24174, .T. ) ;
#76764=ADVANCED_FACE ( 'NONE', ( #51339 ), #13562, .T. ) ;
#76770=CARTESIAN_POINT ( 'NONE',  ( 25.21823338009918203, 5.000000000000002665, 0.000000000000000000 ) ) ;
#76773=EDGE_CURVE ( 'NONE', #2627, #97763, #100957, .T. ) ;
#76778=DIRECTION ( 'NONE',  ( 0.000000000000000000, 1.000000000000000000, 0.000000000000000000 ) ) ;
#76789=ORIENTED_EDGE ( 'NONE', *, *, #73121, .T. ) ;
#76830=AXIS2_PLACEMENT_3D ( 'NONE', #106444, #25034, #90814 ) ;
#76842=EDGE_CURVE ( 'NONE', #37991, #68633, #102563, .T. ) ;
#76865=FACE_OUTER_BOUND ( 'NONE', #10133, .T. ) ;
#76879=FACE_OUTER_BOUND ( 'NONE', #72369, .T. ) ;
#76883=CARTESIAN_POINT ( 'NONE',  ( 39.44615384615384812, 4.172000000000003261, 5.109226446042759579E-16 ) ) ;
#76893=CARTESIAN_POINT ( 'NONE',  ( 22.57792046605466041, 6.123233995736770227E-16, -5.000000000000002665 ) ) ;
#76928=ORIENTED_EDGE ( 'NONE', *, *, #102337, .T. ) ;
#76932=CARTESIAN_POINT ( 'NONE',  ( 0.000000000000000000, 6.123233995736770227E-16, -5.000000000000002665 ) ) ;
#76936=ORIENTED_EDGE ( 'NONE', *, *, #93217, .T. ) ;
#76950=CARTESIAN_POINT ( 'NONE',  ( 37.06438722625302518, 5.000000000000002665, 0.000000000000000000 ) ) ;
#76976=CARTESIAN_POINT ( 'NONE',  ( 35.58361799548379167, 1.482358050883964840E-15, 0.000000000000000000 ) ) ;
#76997=VERTEX_POINT ( 'NONE', #73350 ) ;
#77010=ORIENTED_EDGE ( 'NONE', *, *, #42092, .T. ) ;
#77014=CARTESIAN_POINT ( 'NONE',  ( 0.000000000000000000, 0.000000000000000000, 0.000000000000000000 ) ) ;
#77056=VERTEX_POINT ( 'NONE', #15130 ) ;
#77064=CIRCLE ( 'NONE', #30515, 5.000000000000002665 ) ;
#77066=CARTESIAN_POINT ( 'NONE',  ( 27.02022815836235026, 1.340359594676612611E-15, 0.000000000000000000 ) ) ;
#77105=ADVANCED_FACE ( 'NONE', ( #11809 ), #42589, .T. ) ;
#77106=AXIS2_PLACEMENT_3D ( 'NONE', #34629, #1123, #91253 ) ;
#77125=DIRECTION ( 'NONE',  ( 0.5735764363510470476, -0.8191520442889911324, 1.003171929053524007E-16 ) ) ;
#77142=EDGE_LOOP ( 'NONE', ( #29368, #18545, #65654, #95651, #62127 ) ) ;
#77150=CONICAL_SURFACE ( 'NONE', #44443, 4.172000000000001485, 0.9599310885968750373 ) ;
#77205=ORIENTED_EDGE ( 'NONE', *, *, #32278, .F. ) ;
#77211=DIRECTION ( 'NONE',  ( -1.000000000000000000, -0.000000000000000000, -0.000000000000000000 ) ) ;
#77216=AXIS2_PLACEMENT_3D ( 'NONE', #24310, #81425, #23237 ) ;
#77218=VECTOR ( 'NONE', #50156, 1000.000000000000000 ) ;
#77221=ORIENTED_EDGE ( 'NONE', *, *, #51547, .F. ) ;
#77223=CARTESIAN_POINT ( 'NONE',  ( 21.67692307692307452, -4.171999999999999709, 0.000000000000000000 ) ) ;
#77235=CARTESIAN_POINT ( 'NONE',  ( 31.14131030317610538, 1.482358050883964840E-15, 0.000000000000000000 ) ) ;
#77238=EDGE_CURVE ( 'NONE', #8439, #64182, #96474, .T. ) ;
#77254=ORIENTED_EDGE ( 'NONE', *, *, #26377, .T. ) ;
#77269=AXIS2_PLACEMENT_3D ( 'NONE', #11738, #101827, #60339 ) ;
#77281=AXIS2_PLACEMENT_3D ( 'NONE', #38566, #40133, #64428 ) ;
#77286=EDGE_CURVE ( 'NONE', #48079, #7253, #92877, .T. ) ;
#77339=ORIENTED_EDGE ( 'NONE', *, *, #52484, .T. ) ;
#77386=VECTOR ( 'NONE', #82942, 1000.000000000000000 ) ;
#77439=LINE ( 'NONE', #20324, #92585 ) ;
#77455=LINE ( 'NONE', #28953, #31008 ) ;
#77466=EDGE_CURVE ( 'NONE', #97131, #77056, #58471, .T. ) ;
#77468=ORIENTED_EDGE ( 'NONE', *, *, #70882, .T. ) ;
#77470=EDGE_LOOP ( 'NONE', ( #53914, #27280, #67366, #82234, #101589 ) ) ;
#77503=CONICAL_SURFACE ( 'NONE', #65407, 5.000000000000001776, 0.9599310885968803664 ) ;
#77525=CARTESIAN_POINT ( 'NONE',  ( 6.849999999999999645, 4.618802153517001408, -8.000000000000000000 ) ) ;
#77537=ORIENTED_EDGE ( 'NONE', *, *, #62129, .T. ) ;
#77538=LINE ( 'NONE', #94260, #73934 ) ;
#77574=CARTESIAN_POINT ( 'NONE',  ( 26.69900261086841198, 1.482358050883964840E-15, 0.000000000000000000 ) ) ;
#77577=DIRECTION ( 'NONE',  ( 0.000000000000000000, -1.000000000000000000, 0.000000000000000000 ) ) ;
#77580=ORIENTED_EDGE ( 'NONE', *, *, #74149, .F. ) ;
#77615=VECTOR ( 'NONE', #8188, 1000.000000000000227 ) ;
#77625=ORIENTED_EDGE ( 'NONE', *, *, #47201, .F. ) ;
#77640=DIRECTION ( 'NONE',  ( -1.000000000000000000, -0.000000000000000000, -0.000000000000000000 ) ) ;
#77651=FACE_OUTER_BOUND ( 'NONE', #1824, .T. ) ;
#77664=ORIENTED_EDGE ( 'NONE', *, *, #20965, .T. ) ;
#77688=VERTEX_POINT ( 'NONE', #69293 ) ;
#77693=LINE ( 'NONE', #3802, #16914 ) ;
#77700=ORIENTED_EDGE ( 'NONE', *, *, #51806, .T. ) ;
#77722=EDGE_CURVE ( 'NONE', #7253, #48079, #96437, .T. ) ;
#77783=CIRCLE ( 'NONE', #31302, 5.000000000000001776 ) ;
#77784=AXIS2_PLACEMENT_3D ( 'NONE', #91561, #73756, #17668 ) ;
#77844=EDGE_LOOP ( 'NONE', ( #45184, #58701, #75604, #64887, #89346, #79560 ) ) ;
#77848=ORIENTED_EDGE ( 'NONE', *, *, #34229, .T. ) ;
#77888=FACE_OUTER_BOUND ( 'NONE', #44393, .T. ) ;
#77895=ORIENTED_EDGE ( 'NONE', *, *, #102948, .F. ) ;
#77934=VERTEX_POINT ( 'NONE', #99360 ) ;
#77963=FACE_OUTER_BOUND ( 'NONE', #106213, .T. ) ;
#77974=ORIENTED_EDGE ( 'NONE', *, *, #49203, .F. ) ;
#77979=FACE_OUTER_BOUND ( 'NONE', #65242, .T. ) ;
#78013=CARTESIAN_POINT ( 'NONE',  ( 0.000000000000000000, 0.000000000000000000, 0.000000000000000000 ) ) ;
#78028=EDGE_CURVE ( 'NONE', #3051, #71421, #17421, .T. ) ;
#78030=CARTESIAN_POINT ( 'NONE',  ( 26.11923076923076792, 4.172000000000003261, 5.109226446042759579E-16 ) ) ;
#78046=DIRECTION ( 'NONE',  ( -1.000000000000000000, -0.000000000000000000, -0.000000000000000000 ) ) ;
#78071=FACE_OUTER_BOUND ( 'NONE', #28539, .T. ) ;
#78132=EDGE_CURVE ( 'NONE', #5164, #56216, #76164, .T. ) ;
#78143=EDGE_CURVE ( 'NONE', #8789, #76065, #32699, .T. ) ;
#78145=AXIS2_PLACEMENT_3D ( 'NONE', #78442, #14225, #102732 ) ;
#78168=DIRECTION ( 'NONE',  ( 1.000000000000000000, 1.224606353822377258E-16, 0.000000000000000000 ) ) ;
#78238=EDGE_CURVE ( 'NONE', #51764, #42859, #34556, .T. ) ;
#78284=CARTESIAN_POINT ( 'NONE',  ( 9.830769230769229594, 4.172000000000003261, 0.000000000000000000 ) ) ;
#78295=VECTOR ( 'NONE', #65591, 999.9999999999998863 ) ;
#78301=CARTESIAN_POINT ( 'NONE',  ( 6.249999999999998224, 4.618802153517001408, -8.000000000000000000 ) ) ;
#78315=CARTESIAN_POINT ( 'NONE',  ( 0.000000000000000000, 0.000000000000000000, 0.000000000000000000 ) ) ;
#78337=ORIENTED_EDGE ( 'NONE', *, *, #20768, .T. ) ;
#78353=DIRECTION ( 'NONE',  ( -1.000000000000000000, -1.224606353822377258E-16, -0.000000000000000000 ) ) ;
#78360=CARTESIAN_POINT ( 'NONE',  ( 44.78945892759311675, 6.123233995736770227E-16, -5.000000000000002665 ) ) ;
#78370=EDGE_CURVE ( 'NONE', #20128, #4337, #87880, .T. ) ;
#78423=CARTESIAN_POINT ( 'NONE',  ( 11.31153846153846132, 1.411358822780289120E-15, 0.000000000000000000 ) ) ;
#78442=CARTESIAN_POINT ( 'NONE',  ( 34.10284876471455817, 1.482358050883964840E-15, 0.000000000000000000 ) ) ;
#78473=DIRECTION ( 'NONE',  ( 0.5735764363510470476, -0.8191520442889911324, 1.003171929053524007E-16 ) ) ;
#78480=FACE_OUTER_BOUND ( 'NONE', #29046, .T. ) ;
#78488=DIRECTION ( 'NONE',  ( -0.000000000000000000, 0.000000000000000000, -1.000000000000000000 ) ) ;
#78495=ADVANCED_FACE ( 'NONE', ( #3761 ), #79242, .T. ) ;
#78504=CARTESIAN_POINT ( 'NONE',  ( 0.000000000000000000, 6.928203230275506108, 4.000000000000007105 ) ) ;
#78513=EDGE_LOOP ( 'NONE', ( #37909, #79250, #67898, #26798, #87243 ) ) ;
#78531=AXIS2_PLACEMENT_3D ( 'NONE', #51942, #76752, #84856 ) ;
#78573=LINE ( 'NONE', #96896, #17727 ) ;
#78575=EDGE_CURVE ( 'NONE', #106154, #6487, #29142, .T. ) ;
#78583=CARTESIAN_POINT ( 'NONE',  ( 34.10284876471455817, 1.482358050883964840E-15, 0.000000000000000000 ) ) ;
#78589=AXIS2_PLACEMENT_3D ( 'NONE', #36697, #78168, #5358 ) ;
#78606=LINE ( 'NONE', #62977, #66669 ) ;
#78626=CARTESIAN_POINT ( 'NONE',  ( 0.08285530295198710593, 1.570896314769988811, 7.999999999999996447 ) ) ;
#78644=DIRECTION ( 'NONE',  ( 0.000000000000000000, -1.000000000000000000, 0.000000000000000000 ) ) ;
#78655=DIRECTION ( 'NONE',  ( -1.000000000000000000, -1.224606353822377258E-16, -0.000000000000000000 ) ) ;
#78690=ORIENTED_EDGE ( 'NONE', *, *, #95754, .T. ) ;
#78717=VERTEX_POINT ( 'NONE', #98059 ) ;
#78742=EDGE_CURVE ( 'NONE', #43261, #83753, #103426, .T. ) ;
#78753=VECTOR ( 'NONE', #66824, 1000.000000000000000 ) ;
#78755=ADVANCED_FACE ( 'NONE', ( #16079 ), #56523, .T. ) ;
#78776=CIRCLE ( 'NONE', #40902, 4.172000000000001485 ) ;
#78803=EDGE_LOOP ( 'NONE', ( #38721, #88732, #53787, #105569, #9546, #17968 ) ) ;
#78839=DIRECTION ( 'NONE',  ( 0.000000000000000000, -1.000000000000000000, 0.000000000000000000 ) ) ;
#78860=DIRECTION ( 'NONE',  ( -1.000000000000000000, -0.000000000000000000, -0.000000000000000000 ) ) ;
#78875=ORIENTED_EDGE ( 'NONE', *, *, #14425, .F. ) ;
#78884=DIRECTION ( 'NONE',  ( 1.000000000000000000, 0.000000000000000000, -0.000000000000000000 ) ) ;
#78900=ORIENTED_EDGE ( 'NONE', *, *, #26967, .F. ) ;
#78902=FACE_OUTER_BOUND ( 'NONE', #64699, .T. ) ;
#78904=CARTESIAN_POINT ( 'NONE',  ( 42.98746414932995208, 1.482358050883964840E-15, 0.000000000000000000 ) ) ;
#78940=EDGE_CURVE ( 'NONE', #105570, #104380, #56979, .T. ) ;
#78955=CIRCLE ( 'NONE', #92735, 4.172000000000001485 ) ;
#78980=AXIS2_PLACEMENT_3D ( 'NONE', #37336, #45926, #37868 ) ;
#79007=ORIENTED_EDGE ( 'NONE', *, *, #27984, .T. ) ;
#79052=ORIENTED_EDGE ( 'NONE', *, *, #98566, .T. ) ;
#79055=ORIENTED_EDGE ( 'NONE', *, *, #50847, .T. ) ;
#79058=FACE_OUTER_BOUND ( 'NONE', #58575, .T. ) ;
#79135=VERTEX_POINT ( 'NONE', #84949 ) ;
#79161=ORIENTED_EDGE ( 'NONE', *, *, #29791, .F. ) ;
#79168=CARTESIAN_POINT ( 'NONE',  ( 0.3194001229790396357, 3.115132258388582098, 7.999999999999998224 ) ) ;
#79177=DIRECTION ( 'NONE',  ( 0.000000000000000000, -1.000000000000000000, 0.000000000000000000 ) ) ;
#79202=DIRECTION ( 'NONE',  ( -0.000000000000000000, 0.000000000000000000, -1.000000000000000000 ) ) ;
#79204=FACE_OUTER_BOUND ( 'NONE', #106750, .T. ) ;
#79225=VECTOR ( 'NONE', #75375, 1000.000000000000000 ) ;
#79242=CONICAL_SURFACE ( 'NONE', #22474, 5.000000000000001776, 0.9599310885968803664 ) ;
#79250=ORIENTED_EDGE ( 'NONE', *, *, #95841, .F. ) ;
#79262=ORIENTED_EDGE ( 'NONE', *, *, #70545, .T. ) ;
#79289=CARTESIAN_POINT ( 'NONE',  ( 6.249999999999998224, -9.237604307034018802, 3.355146209984123968E-17 ) ) ;
#79293=DIRECTION ( 'NONE',  ( 0.000000000000000000, 0.000000000000000000, 1.000000000000000000 ) ) ;
#79308=CARTESIAN_POINT ( 'NONE',  ( 21.67692307692307452, 1.411358822780289120E-15, 0.000000000000000000 ) ) ;
#79316=ADVANCED_FACE ( 'NONE', ( #71273 ), #100032, .T. ) ;
#79319=EDGE_LOOP ( 'NONE', ( #63632, #100737, #65737, #29790, #38801, #37291 ) ) ;
#79351=DIRECTION ( 'NONE',  ( 0.000000000000000000, -1.000000000000000000, 0.000000000000000000 ) ) ;
#79353=DIRECTION ( 'NONE',  ( -1.000000000000000000, -0.000000000000000000, -0.000000000000000000 ) ) ;
#79355=VECTOR ( 'NONE', #19943, 999.9999999999998863 ) ;
#79360=CARTESIAN_POINT ( 'NONE',  ( 45.36923076923077502, 4.172000000000003261, 5.109226446042759579E-16 ) ) ;
#79395=DIRECTION ( 'NONE',  ( 0.000000000000000000, -1.000000000000000000, 0.000000000000000000 ) ) ;
#79410=EDGE_LOOP ( 'NONE', ( #26038, #77339, #88385, #44522, #106347, #7397 ) ) ;
#79452=ORIENTED_EDGE ( 'NONE', *, *, #90889, .T. ) ;
#79460=PLANE ( 'NONE',  #43668 ) ;
#79501=DIRECTION ( 'NONE',  ( 0.000000000000000000, 1.000000000000000000, 0.000000000000000000 ) ) ;
#79513=LINE ( 'NONE', #20811, #25285 ) ;
#79522=LINE ( 'NONE', #29942, #64889 ) ;
#79525=DIRECTION ( 'NONE',  ( 0.000000000000000000, -1.000000000000000000, 0.000000000000000000 ) ) ;
#79542=EDGE_CURVE ( 'NONE', #48048, #92227, #17306, .T. ) ;
#79560=ORIENTED_EDGE ( 'NONE', *, *, #14677, .F. ) ;
#79577=EDGE_CURVE ( 'NONE', #47740, #102923, #41518, .T. ) ;
#79583=DIRECTION ( 'NONE',  ( -1.000000000000000000, -1.224606353822377258E-16, -0.000000000000000000 ) ) ;
#79585=CIRCLE ( 'NONE', #10655, 5.000000000000002665 ) ;
#79649=AXIS2_PLACEMENT_3D ( 'NONE', #13626, #14681, #104234 ) ;
#79650=EDGE_CURVE ( 'NONE', #84725, #57214, #22093, .T. ) ;
#79663=EDGE_LOOP ( 'NONE', ( #96029, #61961, #28346, #16776, #36405 ) ) ;
#79692=EDGE_LOOP ( 'NONE', ( #60454, #30738, #91533, #63086, #1807 ) ) ;
#79709=EDGE_CURVE ( 'NONE', #44516, #42513, #105632, .T. ) ;
#79740=VERTEX_POINT ( 'NONE', #66240 ) ;
#79742=EDGE_CURVE ( 'NONE', #2025, #47740, #57054, .T. ) ;
#79776=DIRECTION ( 'NONE',  ( 0.000000000000000000, -1.000000000000000000, 0.000000000000000000 ) ) ;
#79781=CARTESIAN_POINT ( 'NONE',  ( 0.000000000000000000, 0.000000000000000000, 0.000000000000000000 ) ) ;
#79783=CARTESIAN_POINT ( 'NONE',  ( 20.77592568779148863, 5.000000000000003553, 0.000000000000000000 ) ) ;
#79824=ORIENTED_EDGE ( 'NONE', *, *, #39084, .F. ) ;
#79885=LINE ( 'NONE', #78301, #56414 ) ;
#79892=EDGE_CURVE ( 'NONE', #31549, #58193, #16632, .T. ) ;
#79919=DIRECTION ( 'NONE',  ( -1.000000000000000000, -1.224606353822377258E-16, -0.000000000000000000 ) ) ;
#79920=CARTESIAN_POINT ( 'NONE',  ( 38.86638200451619696, 1.340359594676612611E-15, 0.000000000000000000 ) ) ;
#79940=AXIS2_PLACEMENT_3D ( 'NONE', #92064, #1443, #67799 ) ;
#79946=AXIS2_PLACEMENT_3D ( 'NONE', #59316, #58787, #9668 ) ;
#79952=VERTEX_POINT ( 'NONE', #24226 ) ;
#79967=CARTESIAN_POINT ( 'NONE',  ( 6.249999999999998224, 4.618802153517004960, 7.999999999999998224 ) ) ;
#79986=AXIS2_PLACEMENT_3D ( 'NONE', #10258, #50694, #75525 ) ;
#80012=VECTOR ( 'NONE', #94229, 1000.000000000000227 ) ;
#80053=AXIS2_PLACEMENT_3D ( 'NONE', #17867, #59390, #50720 ) ;
#80089=CARTESIAN_POINT ( 'NONE',  ( 6.249999999999998224, 4.618802153517001408, -8.000000000000000000 ) ) ;
#80104=ORIENTED_EDGE ( 'NONE', *, *, #39428, .T. ) ;
#80116=DIRECTION ( 'NONE',  ( 0.000000000000000000, 0.000000000000000000, 1.000000000000000000 ) ) ;
#80132=DIRECTION ( 'NONE',  ( 1.000000000000000000, 1.224606353822377258E-16, 0.000000000000000000 ) ) ;
#80178=FACE_OUTER_BOUND ( 'NONE', #74196, .T. ) ;
#80205=VECTOR ( 'NONE', #27747, 999.9999999999998863 ) ;
#80207=CIRCLE ( 'NONE', #49249, 4.172000000000001485 ) ;
#80230=DIRECTION ( 'NONE',  ( 0.000000000000000000, -1.000000000000000000, 0.000000000000000000 ) ) ;
#80234=DIRECTION ( 'NONE',  ( 0.000000000000000000, -1.000000000000000000, 0.000000000000000000 ) ) ;
#80238=CARTESIAN_POINT ( 'NONE',  ( 23.73746414932995208, 1.482358050883964840E-15, 0.000000000000000000 ) ) ;
#80276=LINE ( 'NONE', #69692, #99339 ) ;
#80278=FACE_OUTER_BOUND ( 'NONE', #26838, .T. ) ;
#80292=ADVANCED_FACE ( 'NONE', ( #73321 ), #48521, .T. ) ;
#80293=EDGE_CURVE ( 'NONE', #15625, #86664, #88115, .T. ) ;
#80301=CARTESIAN_POINT ( 'NONE',  ( 15.17407431220850533, 6.123233995736770227E-16, -5.000000000000002665 ) ) ;
#80338=CARTESIAN_POINT ( 'NONE',  ( 32.94330508143927716, 1.340359594676612611E-15, 0.000000000000000000 ) ) ;
#80340=DIRECTION ( 'NONE',  ( 1.000000000000000000, 1.224606353822377258E-16, 0.000000000000000000 ) ) ;
#80359=AXIS2_PLACEMENT_3D ( 'NONE', #49924, #67195, #100072 ) ;
#80368=ORIENTED_EDGE ( 'NONE', *, *, #899, .F. ) ;
#80374=ORIENTED_EDGE ( 'NONE', *, *, #76773, .T. ) ;
#80421=EDGE_CURVE ( 'NONE', #17199, #91513, #16161, .T. ) ;
#80471=CARTESIAN_POINT ( 'NONE',  ( 21.67692307692307452, 1.411358822780289120E-15, 0.000000000000000000 ) ) ;
#80486=FACE_OUTER_BOUND ( 'NONE', #41769, .T. ) ;
#80503=CARTESIAN_POINT ( 'NONE',  ( 0.000000000000000000, 6.123233995736770227E-16, -5.000000000000002665 ) ) ;
#80518=ORIENTED_EDGE ( 'NONE', *, *, #24112, .T. ) ;
#80524=CONICAL_SURFACE ( 'NONE', #32287, 5.000000000000001776, 0.9599310885968803664 ) ;
#80575=CARTESIAN_POINT ( 'NONE',  ( 40.02592568779148507, 1.482358050883964840E-15, 0.000000000000000000 ) ) ;
#80581=EDGE_LOOP ( 'NONE', ( #17840, #54756, #66252, #54428, #97657 ) ) ;
#80613=CARTESIAN_POINT ( 'NONE',  ( 37.38561277374697056, 0.000000000000000000, 5.000000000000002665 ) ) ;
#80638=CIRCLE ( 'NONE', #13228, 5.000000000000001776 ) ;
#80674=DIRECTION ( 'NONE',  ( -0.5735764363510510444, -0.8191520442889883569, 0.000000000000000000 ) ) ;
#80698=AXIS2_PLACEMENT_3D ( 'NONE', #103649, #21704, #106278 ) ;
#80701=DIRECTION ( 'NONE',  ( 1.000000000000000000, 1.224606353822377258E-16, 0.000000000000000000 ) ) ;
#80745=ORIENTED_EDGE ( 'NONE', *, *, #72906, .F. ) ;
#80749=DIRECTION ( 'NONE',  ( -1.000000000000000000, -1.224606353822377258E-16, -0.000000000000000000 ) ) ;
#80757=ORIENTED_EDGE ( 'NONE', *, *, #46650, .T. ) ;
#80763=AXIS2_PLACEMENT_3D ( 'NONE', #77, #65914, #97209 ) ;
#80764=EDGE_LOOP ( 'NONE', ( #22011, #66010, #5867, #85215, #41959 ) ) ;
#80810=EDGE_LOOP ( 'NONE', ( #57638, #4298, #21811 ) ) ;
#80825=EDGE_CURVE ( 'NONE', #34834, #39269, #86275, .T. ) ;
#80826=ORIENTED_EDGE ( 'NONE', *, *, #34188, .T. ) ;
#80866=CIRCLE ( 'NONE', #98119, 5.000000000000001776 ) ;
#80882=VERTEX_POINT ( 'NONE', #16986 ) ;
#80926=ORIENTED_EDGE ( 'NONE', *, *, #88501, .T. ) ;
#80927=CARTESIAN_POINT ( 'NONE',  ( 12.21253585067004543, 6.123233995736770227E-16, -5.000000000000002665 ) ) ;
#80929=DIRECTION ( 'NONE',  ( 1.000000000000000000, 1.224606353822377258E-16, 0.000000000000000000 ) ) ;
#80949=CARTESIAN_POINT ( 'NONE',  ( 0.000000000000000000, 6.123233995736770227E-16, -5.000000000000002665 ) ) ;
#80971=EDGE_CURVE ( 'NONE', #74005, #47858, #43139, .T. ) ;
#80977=VECTOR ( 'NONE', #67179, 999.9999999999998863 ) ;
#80987=ORIENTED_EDGE ( 'NONE', *, *, #65294, .T. ) ;
#81024=DIRECTION ( 'NONE',  ( -1.000000000000000000, -1.224606353822377258E-16, -0.000000000000000000 ) ) ;
#81027=VERTEX_POINT ( 'NONE', #18599 ) ;
#81038=FACE_OUTER_BOUND ( 'NONE', #44150, .T. ) ;
#81044=DIRECTION ( 'NONE',  ( 1.000000000000000000, 1.224606353822377258E-16, 0.000000000000000000 ) ) ;
#81079=CARTESIAN_POINT ( 'NONE',  ( 45.36923076923077502, 1.411358822780289120E-15, 0.000000000000000000 ) ) ;
#81098=ORIENTED_EDGE ( 'NONE', *, *, #86062, .T. ) ;
#81105=CIRCLE ( 'NONE', #94923, 5.000000000000001776 ) ;
#81124=DIRECTION ( 'NONE',  ( 0.000000000000000000, -1.000000000000000000, 0.000000000000000000 ) ) ;
#81135=VECTOR ( 'NONE', #28014, 999.9999999999998863 ) ;
#81157=ORIENTED_EDGE ( 'NONE', *, *, #30734, .F. ) ;
#81174=DIRECTION ( 'NONE',  ( 0.000000000000000000, -1.000000000000000000, 0.000000000000000000 ) ) ;
#81179=ORIENTED_EDGE ( 'NONE', *, *, #41458, .T. ) ;
#81190=CARTESIAN_POINT ( 'NONE',  ( 31.14131030317610538, 3.851859888774471706E-31, 5.000000000000001776 ) ) ;
#81255=VECTOR ( 'NONE', #50103, 1000.000000000000000 ) ;
#81264=ORIENTED_EDGE ( 'NONE', *, *, #2931, .F. ) ;
#81280=ORIENTED_EDGE ( 'NONE', *, *, #55966, .F. ) ;
#81289=CARTESIAN_POINT ( 'NONE',  ( 6.249999999999998224, 9.237604307034018802, 0.000000000000000000 ) ) ;
#81329=CARTESIAN_POINT ( 'NONE',  ( 31.46253585067004721, 1.340359594676612611E-15, 0.000000000000000000 ) ) ;
#81339=EDGE_CURVE ( 'NONE', #41783, #80882, #85305, .T. ) ;
#81370=DIRECTION ( 'NONE',  ( 0.000000000000000000, -1.000000000000000000, 0.000000000000000000 ) ) ;
#81401=VERTEX_POINT ( 'NONE', #3862 ) ;
#81425=DIRECTION ( 'NONE',  ( -1.000000000000000000, -0.000000000000000000, 0.000000000000000000 ) ) ;
#81447=CIRCLE ( 'NONE', #52197, 5.000000000000001776 ) ;
#81465=ORIENTED_EDGE ( 'NONE', *, *, #11970, .F. ) ;
#81470=SURFACE_SIDE_STYLE ('',( #15692 ) ) ;
#81506=EDGE_LOOP ( 'NONE', ( #52983, #53020, #20441 ) ) ;
#81514=DIRECTION ( 'NONE',  ( 1.000000000000000000, 1.224606353822377258E-16, 0.000000000000000000 ) ) ;
#81522=CARTESIAN_POINT ( 'NONE',  ( 22.25669491856071858, 3.851859888774471706E-31, 5.000000000000001776 ) ) ;
#81552=DIRECTION ( 'NONE',  ( 0.000000000000000000, -1.000000000000000000, 0.000000000000000000 ) ) ;
#81575=ADVANCED_FACE ( 'NONE', ( #38370 ), #32929, .T. ) ;
#81619=DIRECTION ( 'NONE',  ( -1.000000000000000000, -1.224606353822377258E-16, -0.000000000000000000 ) ) ;
#81657=AXIS2_PLACEMENT_3D ( 'NONE', #27250, #27786, #20229 ) ;
#81669=LINE ( 'NONE', #99457, #103242 ) ;
#81677=ORIENTED_EDGE ( 'NONE', *, *, #93974, .T. ) ;
#81696=CARTESIAN_POINT ( 'NONE',  ( 11.31153846153846132, 1.411358822780289120E-15, 0.000000000000000000 ) ) ;
#81721=VECTOR ( 'NONE', #36242, 999.9999999999998863 ) ;
#81742=DIRECTION ( 'NONE',  ( 0.000000000000000000, 1.000000000000000000, 0.000000000000000000 ) ) ;
#81763=ORIENTED_EDGE ( 'NONE', *, *, #65258, .F. ) ;
#81768=AXIS2_PLACEMENT_3D ( 'NONE', #24848, #9685, #100824 ) ;
#81770=CARTESIAN_POINT ( 'NONE',  ( 41.50669491856072568, -5.000000000000000000, 6.123233995736768255E-16 ) ) ;
#81782=EDGE_CURVE ( 'NONE', #95649, #29485, #22682, .T. ) ;
#81806=CARTESIAN_POINT ( 'NONE',  ( 0.01678220608715907600, 0.7854258608507247441, -8.000000000000001776 ) ) ;
#81808=CIRCLE ( 'NONE', #6061, 5.000000000000001776 ) ;
#81824=AXIS2_PLACEMENT_3D ( 'NONE', #41014, #56104, #73359 ) ;
#81857=DIRECTION ( 'NONE',  ( -1.000000000000000000, -1.224606353822377258E-16, -0.000000000000000000 ) ) ;
#81890=VECTOR ( 'NONE', #96404, 999.9999999999998863 ) ;
#81904=DIRECTION ( 'NONE',  ( -1.000000000000000000, -1.224606353822377258E-16, -0.000000000000000000 ) ) ;
#81952=ADVANCED_FACE ( 'NONE', ( #79204 ), #93256, .T. ) ;
#82000=AXIS2_PLACEMENT_3D ( 'NONE', #53024, #93495, #102093 ) ;
#82010=CARTESIAN_POINT ( 'NONE',  ( 7.770228158362350257, 5.000000000000004441, 6.123233995736770227E-16 ) ) ;
#82045=CONICAL_SURFACE ( 'NONE', #78589, 5.000000000000001776, 0.9599310885968803664 ) ;
#82086=CARTESIAN_POINT ( 'NONE',  ( 38.54515645702225868, 1.482358050883964840E-15, 0.000000000000000000 ) ) ;
#82120=VECTOR ( 'NONE', #28619, 999.9999999999998863 ) ;
#82141=CARTESIAN_POINT ( 'NONE',  ( 41.50669491856072568, 1.482358050883964840E-15, 0.000000000000000000 ) ) ;
#82142=CARTESIAN_POINT ( 'NONE',  ( 43.30868969682389036, -5.000000000000009770, 0.000000000000000000 ) ) ;
#82143=EDGE_CURVE ( 'NONE', #93742, #68161, #10551, .T. ) ;
#82186=DIRECTION ( 'NONE',  ( 0.000000000000000000, 0.000000000000000000, -1.000000000000000000 ) ) ;
#82219=ADVANCED_FACE ( 'NONE', ( #58659 ), #83446, .F. ) ;
#82229=DIRECTION ( 'NONE',  ( -1.000000000000000000, -1.224606353822377258E-16, -0.000000000000000000 ) ) ;
#82234=ORIENTED_EDGE ( 'NONE', *, *, #62129, .F. ) ;
#82333=EDGE_CURVE ( 'NONE', #54238, #33159, #64097, .T. ) ;
#82341=EDGE_LOOP ( 'NONE', ( #7619, #17753 ) ) ;
#82350=CIRCLE ( 'NONE', #96138, 5.000000000000002665 ) ;
#82356=DIRECTION ( 'NONE',  ( 0.000000000000000000, -1.000000000000000000, 0.000000000000000000 ) ) ;
#82360=EDGE_LOOP ( 'NONE', ( #36580, #41611, #91845, #16100, #5478, #98411 ) ) ;
#82383=ORIENTED_EDGE ( 'NONE', *, *, #46901, .F. ) ;
#82401=VERTEX_POINT ( 'NONE', #64882 ) ;
#82419=CARTESIAN_POINT ( 'NONE',  ( 24.63846153846153797, 4.172000000000003261, 0.000000000000000000 ) ) ;
#82421=AXIS2_PLACEMENT_3D ( 'NONE', #19377, #20970, #85121 ) ;
#82431=DIRECTION ( 'NONE',  ( -1.000000000000000000, -1.224606353822377258E-16, -0.000000000000000000 ) ) ;
#82435=ORIENTED_EDGE ( 'NONE', *, *, #30910, .T. ) ;
#82438=DIRECTION ( 'NONE',  ( 0.000000000000000000, -1.000000000000000000, 0.000000000000000000 ) ) ;
#82440=ORIENTED_EDGE ( 'NONE', *, *, #34154, .T. ) ;
#82502=CONICAL_SURFACE ( 'NONE', #58403, 5.000000000000001776, 0.9599310885968803664 ) ;
#82534=LINE ( 'NONE', #7042, #2328 ) ;
#82552=LINE ( 'NONE', #2688, #4554 ) ;
#82601=ORIENTED_EDGE ( 'NONE', *, *, #106767, .T. ) ;
#82606=DIRECTION ( 'NONE',  ( 1.000000000000000000, 1.224606353822377258E-16, 0.000000000000000000 ) ) ;
#82608=EDGE_CURVE ( 'NONE', #98120, #97131, #74371, .T. ) ;
#82612=EDGE_CURVE ( 'NONE', #8540, #70974, #60013, .T. ) ;
#82639=AXIS2_PLACEMENT_3D ( 'NONE', #75309, #100123, #66159 ) ;
#82640=ORIENTED_EDGE ( 'NONE', *, *, #33108, .T. ) ;
#82703=AXIS2_PLACEMENT_3D ( 'NONE', #36902, #27759, #42826 ) ;
#82707=DIRECTION ( 'NONE',  ( -1.000000000000000000, -1.224606353822377258E-16, -0.000000000000000000 ) ) ;
#82709=VECTOR ( 'NONE', #53880, 1000.000000000000000 ) ;
#82724=ORIENTED_EDGE ( 'NONE', *, *, #46901, .T. ) ;
#82798=DIRECTION ( 'NONE',  ( 0.000000000000000000, -1.000000000000000000, 0.000000000000000000 ) ) ;
#82801=CARTESIAN_POINT ( 'NONE',  ( 23.15769230769230802, 1.411358822780289120E-15, 0.000000000000000000 ) ) ;
#82804=CARTESIAN_POINT ( 'NONE',  ( 0.000000000000000000, 0.000000000000000000, 0.000000000000000000 ) ) ;
#82808=DIRECTION ( 'NONE',  ( -1.000000000000000000, -1.224606353822377258E-16, -0.000000000000000000 ) ) ;
#82857=ORIENTED_EDGE ( 'NONE', *, *, #40633, .T. ) ;
#82889=DIRECTION ( 'NONE',  ( -1.000000000000000000, -1.224606353822377258E-16, -0.000000000000000000 ) ) ;
#82895=AXIS2_PLACEMENT_3D ( 'NONE', #14365, #80701, #39216 ) ;
#82906=CIRCLE ( 'NONE', #96688, 4.172000000000001485 ) ;
#82927=CARTESIAN_POINT ( 'NONE',  ( 13.37207953394533355, 5.000000000000002665, 0.000000000000000000 ) ) ;
#82933=AXIS2_PLACEMENT_3D ( 'NONE', #19960, #35595, #68472 ) ;
#82942=DIRECTION ( 'NONE',  ( -0.5735764363510510444, -0.8191520442889883569, 0.000000000000000000 ) ) ;
#82944=CARTESIAN_POINT ( 'NONE',  ( 0.000000000000000000, 1.502314598737159031E-15, -8.000000000000000000 ) ) ;
#82946=AXIS2_PLACEMENT_3D ( 'NONE', #84403, #24591, #8901 ) ;
#82948=DIRECTION ( 'NONE',  ( 1.000000000000000000, 1.224606353822377258E-16, 0.000000000000000000 ) ) ;
#82953=FACE_OUTER_BOUND ( 'NONE', #30241, .T. ) ;
#82974=DIRECTION ( 'NONE',  ( 0.000000000000000000, 0.000000000000000000, 1.000000000000000000 ) ) ;
#82979=ORIENTED_EDGE ( 'NONE', *, *, #15996, .F. ) ;
#83021=ORIENTED_EDGE ( 'NONE', *, *, #3109, .F. ) ;
#83030=VERTEX_POINT ( 'NONE', #10747 ) ;
#83045=DIRECTION ( 'NONE',  ( -1.000000000000000000, -1.224606353822377258E-16, -0.000000000000000000 ) ) ;
#83052=AXIS2_PLACEMENT_3D ( 'NONE', #49718, #98273, #9250 ) ;
#83056=DIRECTION ( 'NONE',  ( -1.000000000000000000, -1.224606353822377258E-16, -0.000000000000000000 ) ) ;
#83057=ORIENTED_EDGE ( 'NONE', *, *, #34555, .T. ) ;
#83062=CYLINDRICAL_SURFACE ( 'NONE', #53211, 5.000000000000002665 ) ;
#83085=CARTESIAN_POINT ( 'NONE',  ( 23.15769230769230802, -4.171999999999999709, 0.000000000000000000 ) ) ;
#83089=DIRECTION ( 'NONE',  ( 0.000000000000000000, -1.000000000000000000, 0.000000000000000000 ) ) ;
#83111=DIRECTION ( 'NONE',  ( -1.000000000000000000, -1.224606353822377258E-16, -0.000000000000000000 ) ) ;
#83121=EDGE_LOOP ( 'NONE', ( #65723, #47710, #17197, #47402, #106077, #103745 ) ) ;
#83153=ORIENTED_EDGE ( 'NONE', *, *, #45856, .F. ) ;
#83177=DIRECTION ( 'NONE',  ( 0.000000000000000000, 1.000000000000000000, 0.000000000000000000 ) ) ;
#83191=ORIENTED_EDGE ( 'NONE', *, *, #70882, .F. ) ;
#83210=ADVANCED_FACE ( 'NONE', ( #96997 ), #17157, .T. ) ;
#83219=DIRECTION ( 'NONE',  ( 0.5735764363510468256, 0.8191520442889913545, 0.000000000000000000 ) ) ;
#83231=ORIENTED_EDGE ( 'NONE', *, *, #6227, .F. ) ;
#83252=LINE ( 'NONE', #50873, #45996 ) ;
#83261=VECTOR ( 'NONE', #68735, 999.9999999999998863 ) ;
#83293=ORIENTED_EDGE ( 'NONE', *, *, #70545, .F. ) ;
#83306=DIRECTION ( 'NONE',  ( 0.000000000000000000, -1.000000000000000000, 0.000000000000000000 ) ) ;
#83367=CARTESIAN_POINT ( 'NONE',  ( 6.849999999999999645, 0.000000000000000000, 0.000000000000000000 ) ) ;
#83373=DIRECTION ( 'NONE',  ( 0.000000000000000000, 0.000000000000000000, 1.000000000000000000 ) ) ;
#83377=CARTESIAN_POINT ( 'NONE',  ( 44.46823338009918558, 1.482358050883964840E-15, 0.000000000000000000 ) ) ;
#83385=DIRECTION ( 'NONE',  ( 0.000000000000000000, 0.000000000000000000, -1.000000000000000000 ) ) ;
#83391=EDGE_LOOP ( 'NONE', ( #91194, #93412, #24565, #30074, #63042, #55973 ) ) ;
#83402=DIRECTION ( 'NONE',  ( 0.000000000000000000, -1.000000000000000000, 0.000000000000000000 ) ) ;
#83446=PLANE ( 'NONE',  #17513 ) ;
#83461=DIRECTION ( 'NONE',  ( -1.000000000000000000, -0.000000000000000000, -0.000000000000000000 ) ) ;
#83468=LINE ( 'NONE', #385, #77386 ) ;
#83476=CARTESIAN_POINT ( 'NONE',  ( 0.7145311798161616545, -4.618802153517262532, -8.000000000000001776 ) ) ;
#83505=CARTESIAN_POINT ( 'NONE',  ( 43.30868969682389036, 5.000000000000015099, 6.123233995736782060E-16 ) ) ;
#83506=ORIENTED_EDGE ( 'NONE', *, *, #51604, .T. ) ;
#83538=CARTESIAN_POINT ( 'NONE',  ( 42.98746414932995208, -5.000000000000000000, 6.123233995736768255E-16 ) ) ;
#83581=EDGE_CURVE ( 'NONE', #23780, #74084, #68903, .T. ) ;
#83582=PRESENTATION_STYLE_ASSIGNMENT (( #41540 ) ) ;
#83597=ORIENTED_EDGE ( 'NONE', *, *, #23335, .F. ) ;
#83611=CARTESIAN_POINT ( 'NONE',  ( 45.94900261086841198, 1.482358050883964840E-15, 0.000000000000000000 ) ) ;
#83615=CARTESIAN_POINT ( 'NONE',  ( 26.11923076923076792, 4.172000000000003261, 0.000000000000000000 ) ) ;
#83635=LINE ( 'NONE', #93349, #101901 ) ;
#83651=FACE_OUTER_BOUND ( 'NONE', #32118, .T. ) ;
#83668=EDGE_CURVE ( 'NONE', #25032, #76997, #100407, .T. ) ;
#83700=ORIENTED_EDGE ( 'NONE', *, *, #48658, .F. ) ;
#83730=FACE_OUTER_BOUND ( 'NONE', #106317, .T. ) ;
#83738=LINE ( 'NONE', #58423, #2823 ) ;
#83753=VERTEX_POINT ( 'NONE', #28325 ) ;
#83818=ORIENTED_EDGE ( 'NONE', *, *, #34199, .T. ) ;
#83819=FACE_OUTER_BOUND ( 'NONE', #11193, .T. ) ;
#83839=AXIS2_PLACEMENT_3D ( 'NONE', #93475, #79919, #79395 ) ;
#83843=AXIS2_PLACEMENT_3D ( 'NONE', #48869, #32192, #97420 ) ;
#83854=EDGE_CURVE ( 'NONE', #26294, #63024, #29906, .T. ) ;
#83857=DIRECTION ( 'NONE',  ( 0.000000000000000000, -1.000000000000000000, 0.000000000000000000 ) ) ;
#83948=CARTESIAN_POINT ( 'NONE',  ( 44.46823338009918558, 1.482358050883964840E-15, 0.000000000000000000 ) ) ;
#83964=CONICAL_SURFACE ( 'NONE', #30633, 5.000000000000001776, 0.9599310885968803664 ) ;
#83967=ORIENTED_EDGE ( 'NONE', *, *, #64618, .F. ) ;
#83974=VERTEX_POINT ( 'NONE', #13684 ) ;
#83991=CIRCLE ( 'NONE', #37534, 4.172000000000001485 ) ;
#84068=DIRECTION ( 'NONE',  ( -1.000000000000000000, -1.224606353822377258E-16, -0.000000000000000000 ) ) ;
#84102=CARTESIAN_POINT ( 'NONE',  ( 13.37207953394533355, -5.000000000000000000, 6.123233995736768255E-16 ) ) ;
#84112=DIRECTION ( 'NONE',  ( -1.000000000000000000, -0.000000000000000000, -0.000000000000000000 ) ) ;
#84149=DIRECTION ( 'NONE',  ( 0.000000000000000000, -1.000000000000000000, 0.000000000000000000 ) ) ;
#84154=ORIENTED_EDGE ( 'NONE', *, *, #2931, .T. ) ;
#84158=ORIENTED_EDGE ( 'NONE', *, *, #17456, .F. ) ;
#84186=CARTESIAN_POINT ( 'NONE',  ( 30.56153846153846132, 1.411358822780289120E-15, 0.000000000000000000 ) ) ;
#84198=CARTESIAN_POINT ( 'NONE',  ( 8.349999999999999645, 1.411358822780289120E-15, 0.000000000000000000 ) ) ;
#84219=ADVANCED_FACE ( 'NONE', ( #67459 ), #90660, .T. ) ;
#84262=VERTEX_POINT ( 'NONE', #83615 ) ;
#84271=CIRCLE ( 'NONE', #86000, 8.000000000000000000 ) ;
#84282=EDGE_CURVE ( 'NONE', #26965, #71171, #4019, .T. ) ;
#84290=CARTESIAN_POINT ( 'NONE',  ( 28.50099738913158376, -5.000000000000000000, 0.000000000000000000 ) ) ;
#84316=ORIENTED_EDGE ( 'NONE', *, *, #50736, .T. ) ;
#84335=DIRECTION ( 'NONE',  ( 0.000000000000000000, -1.000000000000000000, 0.000000000000000000 ) ) ;
#84342=EDGE_LOOP ( 'NONE', ( #41869, #69842, #106770, #100075, #102149 ) ) ;
#84347=ORIENTED_EDGE ( 'NONE', *, *, #63394, .F. ) ;
#84377=DIRECTION ( 'NONE',  ( -0.5735764363510512664, 0.8191520442889881348, 1.003171929053520309E-16 ) ) ;
#84385=DIRECTION ( 'NONE',  ( 0.000000000000000000, -1.000000000000000000, 0.000000000000000000 ) ) ;
#84390=ORIENTED_EDGE ( 'NONE', *, *, #58112, .T. ) ;
#84403=CARTESIAN_POINT ( 'NONE',  ( 10.73176661990081371, 1.340359594676612611E-15, 0.000000000000000000 ) ) ;
#84417=ORIENTED_EDGE ( 'NONE', *, *, #50847, .F. ) ;
#84425=AXIS2_PLACEMENT_3D ( 'NONE', #85312, #28174, #11398 ) ;
#84461=ORIENTED_EDGE ( 'NONE', *, *, #73204, .T. ) ;
#84463=PLANE ( 'NONE',  #17041 ) ;
#84467=VECTOR ( 'NONE', #46922, 1000.000000000000000 ) ;
#84525=FACE_OUTER_BOUND ( 'NONE', #54666, .T. ) ;
#84561=CONICAL_SURFACE ( 'NONE', #8782, 4.172000000000001485, 0.9599310885968750373 ) ;
#84565=CYLINDRICAL_SURFACE ( 'NONE', #15949, 5.000000000000002665 ) ;
#84570=EDGE_CURVE ( 'NONE', #37991, #31075, #61503, .T. ) ;
#84606=ORIENTED_EDGE ( 'NONE', *, *, #72848, .F. ) ;
#84621=VERTEX_POINT ( 'NONE', #57087 ) ;
#84638=AXIS2_PLACEMENT_3D ( 'NONE', #21793, #64360, #88618 ) ;
#84642=CARTESIAN_POINT ( 'NONE',  ( 44.78945892759311675, 1.340359594676612611E-15, 0.000000000000000000 ) ) ;
#84678=ORIENTED_EDGE ( 'NONE', *, *, #54066, .T. ) ;
#84688=ORIENTED_EDGE ( 'NONE', *, *, #105904, .F. ) ;
#84714=CARTESIAN_POINT ( 'NONE',  ( 10.73176661990081371, 0.000000000000000000, 5.000000000000002665 ) ) ;
#84721=ADVANCED_FACE ( 'NONE', ( #40383 ), #29993, .T. ) ;
#84725=VERTEX_POINT ( 'NONE', #87890 ) ;
#84753=ORIENTED_EDGE ( 'NONE', *, *, #99432, .T. ) ;
#84772=FACE_OUTER_BOUND ( 'NONE', #103918, .T. ) ;
#84793=CIRCLE ( 'NONE', #17585, 4.172000000000001485 ) ;
#84811=AXIS2_PLACEMENT_3D ( 'NONE', #626, #66468, #34676 ) ;
#84821=DIRECTION ( 'NONE',  ( 0.000000000000000000, 0.000000000000000000, -1.000000000000000000 ) ) ;
#84856=DIRECTION ( 'NONE',  ( 0.000000000000000000, -1.000000000000000000, 0.000000000000000000 ) ) ;
#84915=DIRECTION ( 'NONE',  ( -1.000000000000000000, -1.224606353822377258E-16, -0.000000000000000000 ) ) ;
#84925=ORIENTED_EDGE ( 'NONE', *, *, #93629, .T. ) ;
#84941=CIRCLE ( 'NONE', #34995, 5.000000000000002665 ) ;
#84949=CARTESIAN_POINT ( 'NONE',  ( 32.04230769230768772, -4.171999999999999709, 5.616230220889763424E-16 ) ) ;
#84968=EDGE_CURVE ( 'NONE', #57077, #106280, #105005, .T. ) ;
#85000=CARTESIAN_POINT ( 'NONE',  ( 0.7145311798163271888, -9.237604307034018802, 8.246630900752838649E-17 ) ) ;
#85008=DIRECTION ( 'NONE',  ( -1.000000000000000000, -1.224606353822377258E-16, -0.000000000000000000 ) ) ;
#85016=ORIENTED_EDGE ( 'NONE', *, *, #46986, .F. ) ;
#85062=DIRECTION ( 'NONE',  ( -1.000000000000000000, -1.224606353822377258E-16, -0.000000000000000000 ) ) ;
#85085=CONICAL_SURFACE ( 'NONE', #78145, 5.000000000000001776, 0.9599310885968803664 ) ;
#85089=ORIENTED_EDGE ( 'NONE', *, *, #3865, .F. ) ;
#85100=CARTESIAN_POINT ( 'NONE',  ( 0.000000000000000000, 0.000000000000000000, 0.000000000000000000 ) ) ;
#85116=CARTESIAN_POINT ( 'NONE',  ( 45.36923076923077502, 1.411358822780289120E-15, 0.000000000000000000 ) ) ;
#85121=DIRECTION ( 'NONE',  ( 0.000000000000000000, -1.000000000000000000, 0.000000000000000000 ) ) ;
#85144=VERTEX_POINT ( 'NONE', #73682 ) ;
#85166=DIRECTION ( 'NONE',  ( 0.5735764363510470476, -0.8191520442889911324, 1.003171929053524007E-16 ) ) ;
#85208=CARTESIAN_POINT ( 'NONE',  ( 0.3157512944565053492, -3.097794232830064498, 7.999999999999998224 ) ) ;
#85215=ORIENTED_EDGE ( 'NONE', *, *, #27984, .F. ) ;
#85217=CARTESIAN_POINT ( 'NONE',  ( 16.33361799548379523, -5.000000000000000000, 6.123233995736768255E-16 ) ) ;
#85235=VERTEX_POINT ( 'NONE', #85000 ) ;
#85264=DIRECTION ( 'NONE',  ( 0.000000000000000000, -1.000000000000000000, 0.000000000000000000 ) ) ;
#85304=DIRECTION ( 'NONE',  ( -1.000000000000000000, -0.000000000000000000, -0.000000000000000000 ) ) ;
#85305=LINE ( 'NONE', #45388, #62175 ) ;
#85306=FACE_OUTER_BOUND ( 'NONE', #91882, .T. ) ;
#85312=CARTESIAN_POINT ( 'NONE',  ( 38.54515645702225868, 1.482358050883964840E-15, 0.000000000000000000 ) ) ;
#85320=VERTEX_POINT ( 'NONE', #13214 ) ;
#85333=DIRECTION ( 'NONE',  ( 0.000000000000000000, -1.000000000000000000, 0.000000000000000000 ) ) ;
#85345=DIRECTION ( 'NONE',  ( 0.000000000000000000, 0.000000000000000000, 1.000000000000000000 ) ) ;
#85368=CARTESIAN_POINT ( 'NONE',  ( 16.65484354297773351, 1.340359594676612611E-15, 0.000000000000000000 ) ) ;
#85400=AXIS2_PLACEMENT_3D ( 'NONE', #65425, #30967, #98321 ) ;
#85404=FACE_OUTER_BOUND ( 'NONE', #15309, .T. ) ;
#85410=CYLINDRICAL_SURFACE ( 'NONE', #1028, 5.000000000000002665 ) ;
#85418=CARTESIAN_POINT ( 'NONE',  ( 25.21823338009918203, -5.000000000000000888, 6.123233995736769241E-16 ) ) ;
#85421=CARTESIAN_POINT ( 'NONE',  ( 37.38561277374697056, 1.340359594676612611E-15, 0.000000000000000000 ) ) ;
#85508=EDGE_CURVE ( 'NONE', #96901, #91513, #734, .T. ) ;
#85511=CARTESIAN_POINT ( 'NONE',  ( 19.29515645702225868, 1.482358050883964840E-15, 0.000000000000000000 ) ) ;
#85522=VERTEX_POINT ( 'NONE', #95105 ) ;
#85558=CIRCLE ( 'NONE', #83839, 5.000000000000001776 ) ;
#85562=ORIENTED_EDGE ( 'NONE', *, *, #45758, .T. ) ;
#85596=DIRECTION ( 'NONE',  ( -1.000000000000000000, -1.224606353822377258E-16, -0.000000000000000000 ) ) ;
#85621=DIRECTION ( 'NONE',  ( 0.000000000000000000, -1.000000000000000000, 0.000000000000000000 ) ) ;
#85628=AXIS2_PLACEMENT_3D ( 'NONE', #91590, #41954, #74840 ) ;
#85651=DIRECTION ( 'NONE',  ( 0.000000000000000000, 0.000000000000000000, 1.000000000000000000 ) ) ;
#85699=CIRCLE ( 'NONE', #39189, 5.000000000000001776 ) ;
#85700=CARTESIAN_POINT ( 'NONE',  ( 11.89131030317610183, 6.123233995736772199E-16, -5.000000000000001776 ) ) ;
#85723=DIRECTION ( 'NONE',  ( -1.000000000000000000, -0.000000000000000000, -0.000000000000000000 ) ) ;
#85724=VERTEX_POINT ( 'NONE', #100389 ) ;
#85740=DIRECTION ( 'NONE',  ( 0.000000000000000000, -1.000000000000000000, 0.000000000000000000 ) ) ;
#85775=EDGE_LOOP ( 'NONE', ( #25306, #80757, #60943, #8116, #14104 ) ) ;
#85816=ORIENTED_EDGE ( 'NONE', *, *, #86985, .T. ) ;
#85822=DIRECTION ( 'NONE',  ( 0.5735764363510468256, 0.8191520442889913545, 0.000000000000000000 ) ) ;
#85850=AXIS2_PLACEMENT_3D ( 'NONE', #25400, #58260, #10754 ) ;
#85853=VERTEX_POINT ( 'NONE', #33367 ) ;
#85864=AXIS2_PLACEMENT_3D ( 'NONE', #6699, #95724, #31546 ) ;
#85881=DIRECTION ( 'NONE',  ( 0.000000000000000000, -1.000000000000000000, 0.000000000000000000 ) ) ;
#85882=VERTEX_POINT ( 'NONE', #29185 ) ;
#85886=FACE_OUTER_BOUND ( 'NONE', #11122, .T. ) ;
#85900=VERTEX_POINT ( 'NONE', #45851 ) ;
#86000=AXIS2_PLACEMENT_3D ( 'NONE', #27220, #99994, #26162 ) ;
#86049=CARTESIAN_POINT ( 'NONE',  ( 41.50669491856072568, 5.000000000000003553, 0.000000000000000000 ) ) ;
#86053=DIRECTION ( 'NONE',  ( -1.000000000000000000, -1.224606353822377258E-16, -0.000000000000000000 ) ) ;
#86057=DIRECTION ( 'NONE',  ( 0.000000000000000000, -1.000000000000000000, 0.000000000000000000 ) ) ;
#86062=EDGE_CURVE ( 'NONE', #49120, #6957, #76681, .T. ) ;
#86076=DIRECTION ( 'NONE',  ( -1.000000000000000000, -0.000000000000000000, -0.000000000000000000 ) ) ;
#86083=CARTESIAN_POINT ( 'NONE',  ( 6.249999999999998224, -6.928203230275504332, 4.000000000000011546 ) ) ;
#86086=DIRECTION ( 'NONE',  ( 0.000000000000000000, -0.5000000000000013323, -0.8660254037844379305 ) ) ;
#86087=EDGE_LOOP ( 'NONE', ( #99376, #101737, #67002, #12994, #49978, #52299 ) ) ;
#86091=VECTOR ( 'NONE', #90361, 1000.000000000000000 ) ;
#86100=DIRECTION ( 'NONE',  ( -1.000000000000000000, -0.000000000000000000, -0.000000000000000000 ) ) ;
#86103=ORIENTED_EDGE ( 'NONE', *, *, #86740, .F. ) ;
#86111=EDGE_CURVE ( 'NONE', #85724, #27470, #56045, .T. ) ;
#86118=PLANE ( 'NONE',  #54478 ) ;
#86142=VERTEX_POINT ( 'NONE', #87403 ) ;
#86180=EDGE_CURVE ( 'NONE', #88567, #13709, #87034, .T. ) ;
#86220=ORIENTED_EDGE ( 'NONE', *, *, #86276, .T. ) ;
#86241=ORIENTED_EDGE ( 'NONE', *, *, #51664, .T. ) ;
#86260=ADVANCED_FACE ( 'NONE', ( #448 ), #6083, .T. ) ;
#86275=CIRCLE ( 'NONE', #12178, 5.000000000000001776 ) ;
#86276=EDGE_CURVE ( 'NONE', #2627, #19372, #40956, .T. ) ;
#86277=CARTESIAN_POINT ( 'NONE',  ( 0.4964154566687934422, 8.859816792613651515, -0.6543471694412388295 ) ) ;
#86313=CARTESIAN_POINT ( 'NONE',  ( 11.89131030317610183, 5.000000000000003553, 0.000000000000000000 ) ) ;
#86326=ORIENTED_EDGE ( 'NONE', *, *, #21550, .F. ) ;
#86418=DIRECTION ( 'NONE',  ( -1.000000000000000000, -1.224606353822377258E-16, -0.000000000000000000 ) ) ;
#86420=DIRECTION ( 'NONE',  ( -1.000000000000000000, -1.224606353822377258E-16, -0.000000000000000000 ) ) ;
#86424=DIRECTION ( 'NONE',  ( -1.000000000000000000, -1.224606353822377258E-16, -0.000000000000000000 ) ) ;
#86428=AXIS2_PLACEMENT_3D ( 'NONE', #93318, #2699, #93848 ) ;
#86441=AXIS2_PLACEMENT_3D ( 'NONE', #42475, #9038, #41944 ) ;
#86469=EDGE_CURVE ( 'NONE', #48371, #58381, #55948, .T. ) ;
#86495=DIRECTION ( 'NONE',  ( 0.000000000000000000, -1.000000000000000000, 0.000000000000000000 ) ) ;
#86533=AXIS2_PLACEMENT_3D ( 'NONE', #88788, #90373, #40228 ) ;
#86612=ORIENTED_EDGE ( 'NONE', *, *, #105991, .T. ) ;
#86618=CARTESIAN_POINT ( 'NONE',  ( 0.7145311798163271888, -9.237604307034018802, 8.246630900752838649E-17 ) ) ;
#86633=VECTOR ( 'NONE', #6092, 1000.000000000000000 ) ;
#86656=ORIENTED_EDGE ( 'NONE', *, *, #65703, .T. ) ;
#86664=VERTEX_POINT ( 'NONE', #61283 ) ;
#86722=ORIENTED_EDGE ( 'NONE', *, *, #66599, .T. ) ;
#86737=AXIS2_PLACEMENT_3D ( 'NONE', #73201, #23635, #88882 ) ;
#86740=EDGE_CURVE ( 'NONE', #23780, #45532, #105768, .T. ) ;
#86743=ADVANCED_FACE ( 'NONE', ( #31206 ), #64090, .T. ) ;
#86750=ORIENTED_EDGE ( 'NONE', *, *, #42092, .F. ) ;
#86773=VERTEX_POINT ( 'NONE', #59715 ) ;
#86783=ORIENTED_EDGE ( 'NONE', *, *, #45856, .T. ) ;
#86840=CARTESIAN_POINT ( 'NONE',  ( 44.46823338009918558, -5.000000000000000000, 6.123233995736768255E-16 ) ) ;
#86848=EDGE_CURVE ( 'NONE', #95837, #75560, #69840, .T. ) ;
#86877=CARTESIAN_POINT ( 'NONE',  ( 29.66054107240687543, 1.482358050883964840E-15, 0.000000000000000000 ) ) ;
#86886=ORIENTED_EDGE ( 'NONE', *, *, #73375, .T. ) ;
#86972=DIRECTION ( 'NONE',  ( -1.000000000000000000, -1.224606353822377258E-16, -0.000000000000000000 ) ) ;
#86985=EDGE_CURVE ( 'NONE', #99690, #24250, #103354, .T. ) ;
#86989=ORIENTED_EDGE ( 'NONE', *, *, #41133, .T. ) ;
#86992=VERTEX_POINT ( 'NONE', #69399 ) ;
#87020=VECTOR ( 'NONE', #17979, 1000.000000000000000 ) ;
#87033=DIRECTION ( 'NONE',  ( -1.000000000000000000, -1.224606353822377258E-16, -0.000000000000000000 ) ) ;
#87034=CIRCLE ( 'NONE', #105928, 5.000000000000001776 ) ;
#87039=VERTEX_POINT ( 'NONE', #94199 ) ;
#87057=DIRECTION ( 'NONE',  ( -1.000000000000000000, -0.000000000000000000, -0.000000000000000000 ) ) ;
#87093=AXIS2_PLACEMENT_3D ( 'NONE', #77014, #34998, #25866 ) ;
#87108=DIRECTION ( 'NONE',  ( 0.000000000000000000, -1.000000000000000000, 0.000000000000000000 ) ) ;
#87117=ORIENTED_EDGE ( 'NONE', *, *, #52326, .T. ) ;
#87145=ORIENTED_EDGE ( 'NONE', *, *, #18934, .F. ) ;
#87151=ORIENTED_EDGE ( 'NONE', *, *, #61779, .F. ) ;
#87171=EDGE_CURVE ( 'NONE', #84621, #95530, #40409, .T. ) ;
#87196=EDGE_CURVE ( 'NONE', #76623, #26294, #32123, .T. ) ;
#87199=B_SPLINE_CURVE_WITH_KNOTS ( 'NONE', 3,
 ( #20851, #47172, #94704, #45086, #70934, #88187, #37011, #86618 ),
 .UNSPECIFIED., .F., .F.,
 ( 4, 2, 2, 4 ),
 ( 0.004673709593152156581, 0.005837709341827645136, 0.007001709090503132824, 0.009329708587854111668 ),
 .UNSPECIFIED. ) ;
#87231=CIRCLE ( 'NONE', #32124, 5.000000000000001776 ) ;
#87236=CONICAL_SURFACE ( 'NONE', #20137, 5.000000000000001776, 0.9599310885968803664 ) ;
#87239=CARTESIAN_POINT ( 'NONE',  ( 0.000000000000000000, 0.000000000000000000, 0.000000000000000000 ) ) ;
#87242=AXIS2_PLACEMENT_3D ( 'NONE', #1787, #36869, #103167 ) ;
#87243=ORIENTED_EDGE ( 'NONE', *, *, #14201, .T. ) ;
#87249=ADVANCED_FACE ( 'NONE', ( #76276 ), #4241, .T. ) ;
#87256=DIRECTION ( 'NONE',  ( 0.5735764363510468256, 0.8191520442889913545, 0.000000000000000000 ) ) ;
#87264=DIRECTION ( 'NONE',  ( 0.000000000000000000, -1.000000000000000000, 0.000000000000000000 ) ) ;
#87279=DIRECTION ( 'NONE',  ( 0.000000000000000000, 0.000000000000000000, 1.000000000000000000 ) ) ;
#87294=LINE ( 'NONE', #69518, #13699 ) ;
#87297=CARTESIAN_POINT ( 'NONE',  ( 32.62207953394533178, 1.482358050883964840E-15, 0.000000000000000000 ) ) ;
#87300=EDGE_LOOP ( 'NONE', ( #84347, #74786, #78690, #55692, #76928 ) ) ;
#87309=FACE_OUTER_BOUND ( 'NONE', #35447, .T. ) ;
#87317=ORIENTED_EDGE ( 'NONE', *, *, #9871, .F. ) ;
#87320=ADVANCED_FACE ( 'NONE', ( #2911 ), #67977, .T. ) ;
#87322=VERTEX_POINT ( 'NONE', #36409 ) ;
#87325=DIRECTION ( 'NONE',  ( 0.000000000000000000, -1.000000000000000000, 0.000000000000000000 ) ) ;
#87342=FACE_OUTER_BOUND ( 'NONE', #29999, .T. ) ;
#87356=ORIENTED_EDGE ( 'NONE', *, *, #23428, .F. ) ;
#87369=ORIENTED_EDGE ( 'NONE', *, *, #95409, .T. ) ;
#87403=CARTESIAN_POINT ( 'NONE',  ( 17.23461538461538467, 4.172000000000003261, 0.000000000000000000 ) ) ;
#87452=CONICAL_SURFACE ( 'NONE', #94378, 5.000000000000001776, 0.9599310885968803664 ) ;
#87460=EDGE_CURVE ( 'NONE', #95530, #3257, #50210, .T. ) ;
#87474=EDGE_CURVE ( 'NONE', #29093, #61957, #71429, .T. ) ;
#87475=LINE ( 'NONE', #79360, #40619 ) ;
#87508=VECTOR ( 'NONE', #85822, 999.9999999999998863 ) ;
#87527=CARTESIAN_POINT ( 'NONE',  ( 23.73746414932995208, 1.482358050883964840E-15, 0.000000000000000000 ) ) ;
#87553=ORIENTED_EDGE ( 'NONE', *, *, #75496, .T. ) ;
#87559=ORIENTED_EDGE ( 'NONE', *, *, #60700, .T. ) ;
#87578=CARTESIAN_POINT ( 'NONE',  ( 28.50099738913158376, 1.340359594676612611E-15, 0.000000000000000000 ) ) ;
#87633=CONICAL_SURFACE ( 'NONE', #73830, 4.172000000000001485, 0.9599310885968750373 ) ;
#87637=EDGE_CURVE ( 'NONE', #25507, #25785, #60574, .T. ) ;
#87651=FACE_OUTER_BOUND ( 'NONE', #7574, .T. ) ;
#87693=CARTESIAN_POINT ( 'NONE',  ( 38.86638200451619696, -5.000000000000000000, 0.000000000000000000 ) ) ;
#87760=DIRECTION ( 'NONE',  ( 0.000000000000000000, -1.000000000000000000, 0.000000000000000000 ) ) ;
#87787=DIRECTION ( 'NONE',  ( 0.000000000000000000, -1.000000000000000000, 0.000000000000000000 ) ) ;
#87794=ORIENTED_EDGE ( 'NONE', *, *, #102067, .T. ) ;
#87810=CARTESIAN_POINT ( 'NONE',  ( -9.938519914450460599E-16, 0.3912769056150340874, 7.999999999999998224 ) ) ;
#87817=DIRECTION ( 'NONE',  ( -0.5735764363510512664, 0.8191520442889881348, 1.003171929053520309E-16 ) ) ;
#87823=LINE ( 'NONE', #81289, #70739 ) ;
#87859=CYLINDRICAL_SURFACE ( 'NONE', #14023, 5.000000000000002665 ) ;
#87863=AXIS2_PLACEMENT_3D ( 'NONE', #76976, #71010, #96369 ) ;
#87871=VERTEX_POINT ( 'NONE', #38299 ) ;
#87880=CIRCLE ( 'NONE', #51675, 4.172000000000001485 ) ;
#87885=AXIS2_PLACEMENT_3D ( 'NONE', #101497, #100421, #17403 ) ;
#87890=CARTESIAN_POINT ( 'NONE',  ( 45.36923076923077502, 4.172000000000003261, 0.000000000000000000 ) ) ;
#87917=ORIENTED_EDGE ( 'NONE', *, *, #78742, .F. ) ;
#87931=CARTESIAN_POINT ( 'NONE',  ( 37.06438722625302518, 1.482358050883964840E-15, 0.000000000000000000 ) ) ;
#87948=CARTESIAN_POINT ( 'NONE',  ( 38.86638200451619696, 6.123233995736770227E-16, -5.000000000000002665 ) ) ;
#87973=AXIS2_PLACEMENT_3D ( 'NONE', #25382, #83056, #76015 ) ;
#87987=ORIENTED_EDGE ( 'NONE', *, *, #88113, .F. ) ;
#87989=CIRCLE ( 'NONE', #46712, 8.000000000000000000 ) ;
#88008=CARTESIAN_POINT ( 'NONE',  ( 35.00384615384614762, 1.411358822780289120E-15, 0.000000000000000000 ) ) ;
#88025=VERTEX_POINT ( 'NONE', #105645 ) ;
#88030=VECTOR ( 'NONE', #59359, 1000.000000000000000 ) ;
#88056=DIRECTION ( 'NONE',  ( 1.000000000000000000, 1.224606353822377258E-16, 0.000000000000000000 ) ) ;
#88060=ADVANCED_FACE ( 'NONE', ( #31785 ), #48992, .T. ) ;
#88071=ADVANCED_FACE ( 'NONE', ( #88945 ), #23349, .T. ) ;
#88098=LINE ( 'NONE', #55689, #54253 ) ;
#88104=CIRCLE ( 'NONE', #86428, 5.000000000000002665 ) ;
#88106=EDGE_LOOP ( 'NONE', ( #18090, #12724, #67141, #21320, #44592 ) ) ;
#88110=AXIS2_PLACEMENT_3D ( 'NONE', #54629, #14709, #47610 ) ;
#88113=EDGE_CURVE ( 'NONE', #16386, #77688, #35458, .T. ) ;
#88115=CIRCLE ( 'NONE', #13790, 5.000000000000002665 ) ;
#88187=CARTESIAN_POINT ( 'NONE',  ( 0.3173508448886566691, -8.480771745766407577, -1.310872448937994150 ) ) ;
#88270=ADVANCED_FACE ( 'NONE', ( #78071 ), #69984, .T. ) ;
#88289=VECTOR ( 'NONE', #25491, 1000.000000000000000 ) ;
#88290=FACE_OUTER_BOUND ( 'NONE', #60733, .T. ) ;
#88331=CARTESIAN_POINT ( 'NONE',  ( 6.849999999999999645, 4.618802153517001408, -8.000000000000000000 ) ) ;
#88354=DIRECTION ( 'NONE',  ( 1.000000000000000000, 1.224606353822377258E-16, 0.000000000000000000 ) ) ;
#88378=EDGE_CURVE ( 'NONE', #42859, #1686, #58852, .T. ) ;
#88382=DIRECTION ( 'NONE',  ( -1.000000000000000000, -1.224606353822377258E-16, -0.000000000000000000 ) ) ;
#88385=ORIENTED_EDGE ( 'NONE', *, *, #64318, .T. ) ;
#88427=ORIENTED_EDGE ( 'NONE', *, *, #10486, .T. ) ;
#88429=LINE ( 'NONE', #31278, #53481 ) ;
#88442=CARTESIAN_POINT ( 'NONE',  ( 6.849999999999999645, -4.618802153517012954, -8.000000000000001776 ) ) ;
#88448=ORIENTED_EDGE ( 'NONE', *, *, #20283, .T. ) ;
#88457=DIRECTION ( 'NONE',  ( -1.000000000000000000, -1.224606353822377258E-16, -0.000000000000000000 ) ) ;
#88463=DIRECTION ( 'NONE',  ( 0.000000000000000000, -1.000000000000000000, 0.000000000000000000 ) ) ;
#88464=CARTESIAN_POINT ( 'NONE',  ( 32.62207953394533178, -5.000000000000000000, 6.123233995736768255E-16 ) ) ;
#88469=VERTEX_POINT ( 'NONE', #30779 ) ;
#88472=DIRECTION ( 'NONE',  ( 0.000000000000000000, -1.000000000000000000, 0.000000000000000000 ) ) ;
#88501=EDGE_CURVE ( 'NONE', #79135, #85853, #22689, .T. ) ;
#88517=ADVANCED_FACE ( 'NONE', ( #102110 ), #85410, .T. ) ;
#88528=DIRECTION ( 'NONE',  ( 0.000000000000000000, -1.000000000000000000, 0.000000000000000000 ) ) ;
#88538=ORIENTED_EDGE ( 'NONE', *, *, #103239, .T. ) ;
#88567=VERTEX_POINT ( 'NONE', #76770 ) ;
#88571=ORIENTED_EDGE ( 'NONE', *, *, #20820, .T. ) ;
#88579=CARTESIAN_POINT ( 'NONE',  ( 0.000000000000000000, 0.000000000000000000, 0.000000000000000000 ) ) ;
#88580=EDGE_CURVE ( 'NONE', #76997, #6487, #87231, .T. ) ;
#88581=CARTESIAN_POINT ( 'NONE',  ( 37.06438722625302518, 1.482358050883964840E-15, 0.000000000000000000 ) ) ;
#88618=DIRECTION ( 'NONE',  ( 0.000000000000000000, -1.000000000000000000, 0.000000000000000000 ) ) ;
#88628=VERTEX_POINT ( 'NONE', #106201 ) ;
#88669=CARTESIAN_POINT ( 'NONE',  ( 0.01688885742776513946, -6.535341423375584213, 4.680456609903975718 ) ) ;
#88724=EDGE_LOOP ( 'NONE', ( #46949, #72654, #91359 ) ) ;
#88732=ORIENTED_EDGE ( 'NONE', *, *, #32180, .T. ) ;
#88747=LINE ( 'NONE', #105458, #71654 ) ;
#88771=AXIS2_PLACEMENT_3D ( 'NONE', #31272, #32857, #90004 ) ;
#88788=CARTESIAN_POINT ( 'NONE',  ( 25.21823338009918203, 1.482358050883964840E-15, 0.000000000000000000 ) ) ;
#88816=DIRECTION ( 'NONE',  ( -1.000000000000000000, -0.000000000000000000, -0.000000000000000000 ) ) ;
#88827=DIRECTION ( 'NONE',  ( -1.000000000000000000, -1.224606353822377258E-16, -0.000000000000000000 ) ) ;
#88828=ORIENTED_EDGE ( 'NONE', *, *, #102744, .F. ) ;
#88847=CIRCLE ( 'NONE', #59604, 5.000000000000001776 ) ;
#88854=CARTESIAN_POINT ( 'NONE',  ( 35.58361799548379167, 1.482358050883964840E-15, 0.000000000000000000 ) ) ;
#88874=DIRECTION ( 'NONE',  ( 0.000000000000000000, 1.000000000000000000, 0.000000000000000000 ) ) ;
#88878=CARTESIAN_POINT ( 'NONE',  ( 0.000000000000000000, 0.000000000000000000, 0.000000000000000000 ) ) ;
#88882=DIRECTION ( 'NONE',  ( 0.000000000000000000, -1.000000000000000000, 0.000000000000000000 ) ) ;
#88890=ORIENTED_EDGE ( 'NONE', *, *, #90948, .T. ) ;
#88894=DIRECTION ( 'NONE',  ( 0.000000000000000000, 0.000000000000000000, 1.000000000000000000 ) ) ;
#88920=CONICAL_SURFACE ( 'NONE', #56151, 4.172000000000001485, 0.9599310885968750373 ) ;
#88926=ADVANCED_FACE ( 'NONE', ( #19295 ), #88920, .T. ) ;
#88927=AXIS2_PLACEMENT_3D ( 'NONE', #26512, #76603, #54295 ) ;
#88939=FACE_OUTER_BOUND ( 'NONE', #11046, .T. ) ;
#88945=FACE_OUTER_BOUND ( 'NONE', #15795, .T. ) ;
#88966=EDGE_CURVE ( 'NONE', #103450, #2566, #88747, .T. ) ;
#89039=ORIENTED_EDGE ( 'NONE', *, *, #59621, .T. ) ;
#89051=AXIS2_PLACEMENT_3D ( 'NONE', #77525, #44637, #45170 ) ;
#89113=AXIS2_PLACEMENT_3D ( 'NONE', #6762, #39682, #72557 ) ;
#89121=DIRECTION ( 'NONE',  ( 0.000000000000000000, -1.000000000000000000, 0.000000000000000000 ) ) ;
#89143=ORIENTED_EDGE ( 'NONE', *, *, #88966, .T. ) ;
#89157=DIRECTION ( 'NONE',  ( 0.000000000000000000, 1.000000000000000000, 0.000000000000000000 ) ) ;
#89158=ORIENTED_EDGE ( 'NONE', *, *, #55310, .T. ) ;
#89162=LINE ( 'NONE', #71372, #3152 ) ;
#89190=AXIS2_PLACEMENT_3D ( 'NONE', #3544, #86076, #101702 ) ;
#89195=EDGE_CURVE ( 'NONE', #12690, #22420, #73878, .T. ) ;
#89215=CARTESIAN_POINT ( 'NONE',  ( 16.65484354297773351, 1.340359594676612611E-15, 0.000000000000000000 ) ) ;
#89226=FACE_OUTER_BOUND ( 'NONE', #36417, .T. ) ;
#89247=EDGE_CURVE ( 'NONE', #43184, #71639, #39342, .T. ) ;
#89272=ADVANCED_FACE ( 'NONE', ( #31343 ), #73335, .T. ) ;
#89325=EDGE_CURVE ( 'NONE', #49147, #17674, #6825, .T. ) ;
#89342=DIRECTION ( 'NONE',  ( 1.000000000000000000, 1.224606353822377258E-16, 0.000000000000000000 ) ) ;
#89346=ORIENTED_EDGE ( 'NONE', *, *, #36551, .F. ) ;
#89356=ORIENTED_EDGE ( 'NONE', *, *, #34942, .T. ) ;
#89362=CIRCLE ( 'NONE', #73787, 8.000000000000000000 ) ;
#89366=ORIENTED_EDGE ( 'NONE', *, *, #40633, .F. ) ;
#89369=LINE ( 'NONE', #81770, #81890 ) ;
#89370=DIRECTION ( 'NONE',  ( 0.000000000000000000, -1.000000000000000000, 0.000000000000000000 ) ) ;
#89382=AXIS2_PLACEMENT_3D ( 'NONE', #101239, #93141, #1987 ) ;
#89402=EDGE_CURVE ( 'NONE', #71171, #39671, #56546, .T. ) ;
#89405=AXIS2_PLACEMENT_3D ( 'NONE', #85100, #11186, #82974 ) ;
#89416=ORIENTED_EDGE ( 'NONE', *, *, #56990, .F. ) ;
#89443=AXIS2_PLACEMENT_3D ( 'NONE', #54534, #22758, #37359 ) ;
#89444=ORIENTED_EDGE ( 'NONE', *, *, #10812, .F. ) ;
#89466=CARTESIAN_POINT ( 'NONE',  ( 0.3173508448886522837, 5.375634714784615298, -6.689127551062009402 ) ) ;
#89482=CARTESIAN_POINT ( 'NONE',  ( 0.000000000000000000, 0.000000000000000000, 0.000000000000000000 ) ) ;
#89484=AXIS2_PLACEMENT_3D ( 'NONE', #44956, #71325, #70805 ) ;
#89513=DIRECTION ( 'NONE',  ( 0.5735764363510470476, -0.8191520442889911324, 1.003171929053524007E-16 ) ) ;
#89521=EDGE_CURVE ( 'NONE', #98765, #99690, #29071, .T. ) ;
#89522=DIRECTION ( 'NONE',  ( 0.000000000000000000, -1.000000000000000000, 0.000000000000000000 ) ) ;
#89534=ORIENTED_EDGE ( 'NONE', *, *, #34188, .F. ) ;
#89599=FILL_AREA_STYLE ('',( #56676 ) ) ;
#89613=EDGE_LOOP ( 'NONE', ( #91465, #88448, #64485, #57744, #79824, #100547 ) ) ;
#89635=ORIENTED_EDGE ( 'NONE', *, *, #79577, .F. ) ;
#89650=AXIS2_PLACEMENT_3D ( 'NONE', #81329, #72716, #23674 ) ;
#89655=ORIENTED_EDGE ( 'NONE', *, *, #25097, .F. ) ;
#89726=DIRECTION ( 'NONE',  ( -0.5735764363510512664, 0.8191520442889881348, 1.003171929053520309E-16 ) ) ;
#89727=DIRECTION ( 'NONE',  ( 0.000000000000000000, -1.000000000000000000, 0.000000000000000000 ) ) ;
#89737=DIRECTION ( 'NONE',  ( -1.000000000000000000, -1.224606353822377258E-16, -0.000000000000000000 ) ) ;
#89776=ORIENTED_EDGE ( 'NONE', *, *, #69638, .T. ) ;
#89777=ADVANCED_FACE ( 'NONE', ( #6349 ), #58344, .T. ) ;
#89784=ADVANCED_FACE ( 'NONE', ( #42453 ), #101387, .T. ) ;
#89785=ORIENTED_EDGE ( 'NONE', *, *, #104133, .F. ) ;
#89799=EDGE_CURVE ( 'NONE', #31549, #85235, #99081, .T. ) ;
#89801=CONICAL_SURFACE ( 'NONE', #96643, 5.000000000000001776, 0.9599310885968803664 ) ;
#89802=ADVANCED_FACE ( 'NONE', ( #9013 ), #35469, .F. ) ;
#89817=CIRCLE ( 'NONE', #72558, 4.172000000000001485 ) ;
#89827=VERTEX_POINT ( 'NONE', #76950 ) ;
#89830=DIRECTION ( 'NONE',  ( -1.000000000000000000, -1.224606353822377258E-16, -0.000000000000000000 ) ) ;
#89833=ADVANCED_FACE ( 'NONE', ( #50011 ), #18740, .T. ) ;
#89838=CARTESIAN_POINT ( 'NONE',  ( 8.929771841637641927, 1.482358050883964840E-15, 0.000000000000000000 ) ) ;
#89843=FACE_OUTER_BOUND ( 'NONE', #16235, .T. ) ;
#89886=EDGE_LOOP ( 'NONE', ( #48569, #50971, #65884, #104612, #72219 ) ) ;
#89917=CARTESIAN_POINT ( 'NONE',  ( 45.94900261086841198, 3.851859888774471706E-31, 5.000000000000001776 ) ) ;
#89933=DIRECTION ( 'NONE',  ( -1.000000000000000000, -0.000000000000000000, -0.000000000000000000 ) ) ;
#89953=CIRCLE ( 'NONE', #103738, 5.000000000000002665 ) ;
#89969=ADVANCED_FACE ( 'NONE', ( #84525 ), #66196, .T. ) ;
#89970=CIRCLE ( 'NONE', #8960, 5.000000000000002665 ) ;
#89995=CYLINDRICAL_SURFACE ( 'NONE', #23651, 5.000000000000002665 ) ;
#90001=DIRECTION ( 'NONE',  ( 0.000000000000000000, 1.000000000000000000, 0.000000000000000000 ) ) ;
#90004=DIRECTION ( 'NONE',  ( 0.000000000000000000, -1.000000000000000000, 0.000000000000000000 ) ) ;
#90005=DIRECTION ( 'NONE',  ( 0.000000000000000000, -1.000000000000000000, 0.000000000000000000 ) ) ;
#90027=VERTEX_POINT ( 'NONE', #30023 ) ;
#90054=CARTESIAN_POINT ( 'NONE',  ( 37.38561277374697056, 1.340359594676612611E-15, 0.000000000000000000 ) ) ;
#90087=ORIENTED_EDGE ( 'NONE', *, *, #12276, .T. ) ;
#90117=DIRECTION ( 'NONE',  ( -1.000000000000000000, -1.224606353822377258E-16, -0.000000000000000000 ) ) ;
#90122=SURFACE_STYLE_USAGE ( .BOTH. , #81470 ) ;
#90146=DIRECTION ( 'NONE',  ( -1.000000000000000000, -1.224606353822377258E-16, -0.000000000000000000 ) ) ;
#90209=DIRECTION ( 'NONE',  ( -0.5735764363510510444, -0.8191520442889883569, 0.000000000000000000 ) ) ;
#90217=ORIENTED_EDGE ( 'NONE', *, *, #8335, .F. ) ;
#90218=DIRECTION ( 'NONE',  ( -1.000000000000000000, -1.224606353822377258E-16, -0.000000000000000000 ) ) ;
#90225=ORIENTED_EDGE ( 'NONE', *, *, #25794, .F. ) ;
#90229=FACE_OUTER_BOUND ( 'NONE', #5820, .T. ) ;
#90264=EDGE_LOOP ( 'NONE', ( #97650, #69575, #45365, #99017, #104745 ) ) ;
#90274=CARTESIAN_POINT ( 'NONE',  ( 33.52307692307692122, 1.411358822780289120E-15, 0.000000000000000000 ) ) ;
#90291=CARTESIAN_POINT ( 'NONE',  ( 6.849999999999999645, 0.000000000000000000, 0.000000000000000000 ) ) ;
#90300=ORIENTED_EDGE ( 'NONE', *, *, #57569, .T. ) ;
#90308=EDGE_LOOP ( 'NONE', ( #31508, #70708, #97397, #105975, #96028 ) ) ;
#90314=CARTESIAN_POINT ( 'NONE',  ( 0.000000000000000000, 0.000000000000000000, 0.000000000000000000 ) ) ;
#90316=ORIENTED_EDGE ( 'NONE', *, *, #69143, .T. ) ;
#90325=CARTESIAN_POINT ( 'NONE',  ( 0.000000000000000000, 6.123233995736770227E-16, -5.000000000000002665 ) ) ;
#90361=DIRECTION ( 'NONE',  ( -1.000000000000000000, -0.000000000000000000, -0.000000000000000000 ) ) ;
#90373=DIRECTION ( 'NONE',  ( 1.000000000000000000, 1.224606353822377258E-16, 0.000000000000000000 ) ) ;
#90382=VECTOR ( 'NONE', #100353, 999.9999999999998863 ) ;
#90393=DIRECTION ( 'NONE',  ( 1.000000000000000000, 1.224606353822377258E-16, 0.000000000000000000 ) ) ;
#90437=CARTESIAN_POINT ( 'NONE',  ( 11.89131030317610183, 3.851859888774471706E-31, 5.000000000000001776 ) ) ;
#90454=CARTESIAN_POINT ( 'NONE',  ( 29.08076923076923137, 1.411358822780289120E-15, 0.000000000000000000 ) ) ;
#90458=DIRECTION ( 'NONE',  ( -1.000000000000000000, -0.000000000000000000, -0.000000000000000000 ) ) ;
#90462=ORIENTED_EDGE ( 'NONE', *, *, #56368, .T. ) ;
#90464=VERTEX_POINT ( 'NONE', #24721 ) ;
#90465=CARTESIAN_POINT ( 'NONE',  ( 40.34715123528543046, 1.340359594676612611E-15, 0.000000000000000000 ) ) ;
#90529=AXIS2_PLACEMENT_3D ( 'NONE', #21456, #53274, #85651 ) ;
#90600=DIRECTION ( 'NONE',  ( 0.000000000000000000, 1.000000000000000000, 0.000000000000000000 ) ) ;
#90626=DIRECTION ( 'NONE',  ( 0.000000000000000000, 0.000000000000000000, 1.000000000000000000 ) ) ;
#90627=ADVANCED_FACE ( 'NONE', ( #43543 ), #3371, .T. ) ;
#90628=LINE ( 'NONE', #16733, #23503 ) ;
#90640=ORIENTED_EDGE ( 'NONE', *, *, #29535, .T. ) ;
#90660=CYLINDRICAL_SURFACE ( 'NONE', #43659, 5.000000000000002665 ) ;
#90671=ORIENTED_EDGE ( 'NONE', *, *, #93629, .F. ) ;
#90677=DIRECTION ( 'NONE',  ( 0.000000000000000000, 0.000000000000000000, 1.000000000000000000 ) ) ;
#90714=CARTESIAN_POINT ( 'NONE',  ( 18.71538461538461462, -4.171999999999999709, 0.000000000000000000 ) ) ;
#90745=CARTESIAN_POINT ( 'NONE',  ( 13.37207953394533355, 1.482358050883964840E-15, 0.000000000000000000 ) ) ;
#90793=EDGE_CURVE ( 'NONE', #16424, #60319, #58509, .T. ) ;
#90814=DIRECTION ( 'NONE',  ( 0.000000000000000000, 1.000000000000000000, 0.000000000000000000 ) ) ;
#90826=CARTESIAN_POINT ( 'NONE',  ( 33.52307692307692122, -4.171999999999999709, 5.616230220889763424E-16 ) ) ;
#90889=EDGE_CURVE ( 'NONE', #9677, #105570, #6785, .T. ) ;
#90902=FACE_OUTER_BOUND ( 'NONE', #48222, .T. ) ;
#90907=CYLINDRICAL_SURFACE ( 'NONE', #67150, 5.000000000000002665 ) ;
#90948=EDGE_CURVE ( 'NONE', #73449, #13600, #30968, .T. ) ;
#90956=DIRECTION ( 'NONE',  ( 0.000000000000000000, 1.000000000000000000, 0.000000000000000000 ) ) ;
#90967=ORIENTED_EDGE ( 'NONE', *, *, #52326, .F. ) ;
#90975=UNCERTAINTY_MEASURE_WITH_UNIT (LENGTH_MEASURE( 1.000000000000000082E-05 ), #100830, 'distance_accuracy_value', 'NONE');
#91005=CARTESIAN_POINT ( 'NONE',  ( 0.4988340113754565208, 3.871605243940355656, -8.000000000000000000 ) ) ;
#91008=DIRECTION ( 'NONE',  ( 0.000000000000000000, -1.000000000000000000, 0.000000000000000000 ) ) ;
#91019=DIRECTION ( 'NONE',  ( -1.000000000000000000, -0.000000000000000000, -0.000000000000000000 ) ) ;
#91058=CARTESIAN_POINT ( 'NONE',  ( 0.000000000000000000, 0.000000000000000000, 5.000000000000002665 ) ) ;
#91064=DIRECTION ( 'NONE',  ( -0.5735764363510510444, -0.8191520442889883569, 0.000000000000000000 ) ) ;
#91073=ADVANCED_FACE ( 'NONE', ( #94088 ), #41313, .T. ) ;
#91081=DIRECTION ( 'NONE',  ( -1.000000000000000000, -1.224606353822377258E-16, -0.000000000000000000 ) ) ;
#91108=CARTESIAN_POINT ( 'NONE',  ( 6.249999999999998224, 6.928203230275505220, 4.000000000000006217 ) ) ;
#91109=CIRCLE ( 'NONE', #104880, 5.000000000000001776 ) ;
#91131=ORIENTED_EDGE ( 'NONE', *, *, #69696, .T. ) ;
#91139=VERTEX_POINT ( 'NONE', #3488 ) ;
#91158=CARTESIAN_POINT ( 'NONE',  ( 14.85284876471456350, 1.482358050883964840E-15, 0.000000000000000000 ) ) ;
#91174=CARTESIAN_POINT ( 'NONE',  ( 13.37207953394533355, 5.000000000000003553, 0.000000000000000000 ) ) ;
#91176=CARTESIAN_POINT ( 'NONE',  ( 0.000000000000000000, 0.000000000000000000, 0.000000000000000000 ) ) ;
#91194=ORIENTED_EDGE ( 'NONE', *, *, #103518, .F. ) ;
#91218=AXIS2_PLACEMENT_3D ( 'NONE', #78583, #37651, #87760 ) ;
#91249=EDGE_CURVE ( 'NONE', #106280, #88025, #106753, .T. ) ;
#91252=FACE_OUTER_BOUND ( 'NONE', #2035, .T. ) ;
#91253=DIRECTION ( 'NONE',  ( 0.000000000000000000, -1.000000000000000000, 0.000000000000000000 ) ) ;
#91265=AXIS2_PLACEMENT_3D ( 'NONE', #3092, #78046, #59752 ) ;
#91274=CARTESIAN_POINT ( 'NONE',  ( 0.000000000000000000, 0.000000000000000000, 0.000000000000000000 ) ) ;
#91281=CIRCLE ( 'NONE', #58549, 5.000000000000002665 ) ;
#91326=AXIS2_PLACEMENT_3D ( 'NONE', #62454, #47307, #38713 ) ;
#91359=ORIENTED_EDGE ( 'NONE', *, *, #78238, .T. ) ;
#91363=ORIENTED_EDGE ( 'NONE', *, *, #94348, .F. ) ;
#91416=ORIENTED_EDGE ( 'NONE', *, *, #34942, .F. ) ;
#91465=ORIENTED_EDGE ( 'NONE', *, *, #77238, .F. ) ;
#91513=VERTEX_POINT ( 'NONE', #26609 ) ;
#91533=ORIENTED_EDGE ( 'NONE', *, *, #35936, .T. ) ;
#91545=VECTOR ( 'NONE', #106512, 1000.000000000000000 ) ;
#91547=DIRECTION ( 'NONE',  ( 0.000000000000000000, -1.000000000000000000, 0.000000000000000000 ) ) ;
#91561=CARTESIAN_POINT ( 'NONE',  ( 30.56153846153846132, 1.411358822780289120E-15, 0.000000000000000000 ) ) ;
#91568=CARTESIAN_POINT ( 'NONE',  ( 10.41054107240687188, 3.851859888774471706E-31, 5.000000000000001776 ) ) ;
#91584=CIRCLE ( 'NONE', #45096, 4.172000000000001485 ) ;
#91590=CARTESIAN_POINT ( 'NONE',  ( 20.77592568779148863, 1.482358050883964840E-15, 0.000000000000000000 ) ) ;
#91624=DIRECTION ( 'NONE',  ( 0.000000000000000000, -1.000000000000000000, 0.000000000000000000 ) ) ;
#91639=CARTESIAN_POINT ( 'NONE',  ( 45.36923076923077502, -4.171999999999999709, 5.616230220889763424E-16 ) ) ;
#91658=CONICAL_SURFACE ( 'NONE', #86533, 5.000000000000001776, 0.9599310885968803664 ) ;
#91693=LINE ( 'NONE', #91174, #69579 ) ;
#91703=DIRECTION ( 'NONE',  ( -1.000000000000000000, -0.000000000000000000, 0.000000000000000000 ) ) ;
#91748=FACE_OUTER_BOUND ( 'NONE', #15347, .T. ) ;
#91756=ORIENTED_EDGE ( 'NONE', *, *, #20418, .T. ) ;
#91777=CARTESIAN_POINT ( 'NONE',  ( 33.52307692307692122, -4.171999999999999709, 0.000000000000000000 ) ) ;
#91788=ORIENTED_EDGE ( 'NONE', *, *, #5946, .F. ) ;
#91793=CARTESIAN_POINT ( 'NONE',  ( 35.00384615384614762, 1.411358822780289120E-15, 0.000000000000000000 ) ) ;
#91802=EDGE_CURVE ( 'NONE', #39269, #76220, #62142, .T. ) ;
#91809=DIRECTION ( 'NONE',  ( -1.000000000000000000, -1.224606353822377258E-16, -0.000000000000000000 ) ) ;
#91827=VECTOR ( 'NONE', #8867, 1000.000000000000000 ) ;
#91830=DIRECTION ( 'NONE',  ( 0.000000000000000000, -1.000000000000000000, 0.000000000000000000 ) ) ;
#91845=ORIENTED_EDGE ( 'NONE', *, *, #3865, .T. ) ;
#91881=DIRECTION ( 'NONE',  ( -0.000000000000000000, 1.000000000000000000, 1.877893248421449036E-16 ) ) ;
#91882=EDGE_LOOP ( 'NONE', ( #86612, #73890, #25349, #12573, #76345, #24897 ) ) ;
#91895=CIRCLE ( 'NONE', #4051, 4.172000000000001485 ) ;
#91932=ORIENTED_EDGE ( 'NONE', *, *, #36831, .F. ) ;
#91938=EDGE_CURVE ( 'NONE', #99464, #45751, #50173, .T. ) ;
#91946=ORIENTED_EDGE ( 'NONE', *, *, #23416, .T. ) ;
#91960=DIRECTION ( 'NONE',  ( -1.000000000000000000, -1.224606353822377258E-16, -0.000000000000000000 ) ) ;
#91989=CARTESIAN_POINT ( 'NONE',  ( 38.54515645702225868, 5.000000000000003553, 0.000000000000000000 ) ) ;
#91993=EDGE_CURVE ( 'NONE', #83753, #26189, #38051, .T. ) ;
#92064=CARTESIAN_POINT ( 'NONE',  ( 35.90484354297773706, 1.340359594676612611E-15, 0.000000000000000000 ) ) ;
#92075=AXIS2_PLACEMENT_3D ( 'NONE', #67136, #25653, #100020 ) ;
#92130=ORIENTED_EDGE ( 'NONE', *, *, #37586, .T. ) ;
#92149=DIRECTION ( 'NONE',  ( -0.5735764363510512664, 0.8191520442889881348, 1.003171929053520309E-16 ) ) ;
#92192=ORIENTED_EDGE ( 'NONE', *, *, #65258, .T. ) ;
#92227=VERTEX_POINT ( 'NONE', #93833 ) ;
#92231=DIRECTION ( 'NONE',  ( -1.000000000000000000, -1.224606353822377258E-16, -0.000000000000000000 ) ) ;
#92250=CARTESIAN_POINT ( 'NONE',  ( 13.37207953394533355, 1.482358050883964840E-15, 0.000000000000000000 ) ) ;
#92302=CONICAL_SURFACE ( 'NONE', #88927, 4.172000000000001485, 0.9599310885968750373 ) ;
#92312=EDGE_CURVE ( 'NONE', #79135, #55161, #15670, .T. ) ;
#92315=CARTESIAN_POINT ( 'NONE',  ( 0.000000000000000000, 6.123233995736770227E-16, -5.000000000000002665 ) ) ;
#92376=AXIS2_PLACEMENT_3D ( 'NONE', #3885, #97642, #72324 ) ;
#92379=CARTESIAN_POINT ( 'NONE',  ( 0.000000000000000000, 0.000000000000000000, 5.000000000000002665 ) ) ;
#92444=CIRCLE ( 'NONE', #40778, 8.000000000000000000 ) ;
#92483=CARTESIAN_POINT ( 'NONE',  ( 31.46253585067004721, 1.340359594676612611E-15, 0.000000000000000000 ) ) ;
#92492=ORIENTED_EDGE ( 'NONE', *, *, #102819, .T. ) ;
#92505=AXIS2_PLACEMENT_3D ( 'NONE', #64363, #81044, #89157 ) ;
#92585=VECTOR ( 'NONE', #86086, 999.9999999999998863 ) ;
#92588=ORIENTED_EDGE ( 'NONE', *, *, #56990, .T. ) ;
#92605=CARTESIAN_POINT ( 'NONE',  ( 33.52307692307692122, 1.411358822780289120E-15, 0.000000000000000000 ) ) ;
#92611=AXIS2_PLACEMENT_3D ( 'NONE', #77066, #3180, #68995 ) ;
#92648=AXIS2_PLACEMENT_3D ( 'NONE', #56262, #56807, #97273 ) ;
#92651=DIRECTION ( 'NONE',  ( -0.5735764363510512664, 0.8191520442889881348, 1.003171929053520309E-16 ) ) ;
#92677=VECTOR ( 'NONE', #64953, 999.9999999999998863 ) ;
#92686=ORIENTED_EDGE ( 'NONE', *, *, #71346, .F. ) ;
#92693=EDGE_CURVE ( 'NONE', #13812, #44516, #87989, .T. ) ;
#92697=DIRECTION ( 'NONE',  ( 0.000000000000000000, -1.000000000000000000, 0.000000000000000000 ) ) ;
#92715=AXIS2_PLACEMENT_3D ( 'NONE', #69509, #102395, #28545 ) ;
#92722=CARTESIAN_POINT ( 'NONE',  ( 28.17977184163764193, 1.482358050883964840E-15, 0.000000000000000000 ) ) ;
#92723=CARTESIAN_POINT ( 'NONE',  ( 0.000000000000000000, 0.000000000000000000, 5.000000000000002665 ) ) ;
#92735=AXIS2_PLACEMENT_3D ( 'NONE', #42943, #101181, #18697 ) ;
#92752=CARTESIAN_POINT ( 'NONE',  ( 6.849999999999999645, 0.000000000000000000, 0.000000000000000000 ) ) ;
#92764=FACE_OUTER_BOUND ( 'NONE', #13783, .T. ) ;
#92765=DIRECTION ( 'NONE',  ( 0.000000000000000000, -1.000000000000000000, 0.000000000000000000 ) ) ;
#92814=CARTESIAN_POINT ( 'NONE',  ( 17.81438722625302518, 1.482358050883964840E-15, 0.000000000000000000 ) ) ;
#92822=DIRECTION ( 'NONE',  ( 0.000000000000000000, 1.000000000000000000, 0.000000000000000000 ) ) ;
#92849=AXIS2_PLACEMENT_3D ( 'NONE', #104583, #4306, #62553 ) ;
#92864=DIRECTION ( 'NONE',  ( -0.5735764363510510444, -0.8191520442889883569, 0.000000000000000000 ) ) ;
#92877=CIRCLE ( 'NONE', #20653, 4.172000000000001485 ) ;
#92920=EDGE_LOOP ( 'NONE', ( #86241, #104875, #45207, #84158, #43754 ) ) ;
#92935=ORIENTED_EDGE ( 'NONE', *, *, #65982, .F. ) ;
#92950=EDGE_CURVE ( 'NONE', #62030, #63004, #69140, .T. ) ;
#92953=CARTESIAN_POINT ( 'NONE',  ( 37.96538461538461462, 1.411358822780289120E-15, 0.000000000000000000 ) ) ;
#92965=AXIS2_PLACEMENT_3D ( 'NONE', #57931, #41756, #33693 ) ;
#92998=ORIENTED_EDGE ( 'NONE', *, *, #94779, .F. ) ;
#93041=CONICAL_SURFACE ( 'NONE', #72403, 5.000000000000001776, 0.9599310885968803664 ) ;
#93048=CIRCLE ( 'NONE', #25886, 4.172000000000001485 ) ;
#93067=EDGE_CURVE ( 'NONE', #87322, #54320, #33035, .T. ) ;
#93141=DIRECTION ( 'NONE',  ( 1.000000000000000000, 0.000000000000000000, 0.000000000000000000 ) ) ;
#93147=LINE ( 'NONE', #75350, #38484 ) ;
#93148=DIRECTION ( 'NONE',  ( 0.000000000000000000, -1.000000000000000000, 0.000000000000000000 ) ) ;
#93217=EDGE_CURVE ( 'NONE', #4337, #85522, #23740, .T. ) ;
#93221=AXIS2_PLACEMENT_3D ( 'NONE', #22980, #47215, #104945 ) ;
#93247=ORIENTED_EDGE ( 'NONE', *, *, #910, .T. ) ;
#93248=LINE ( 'NONE', #4771, #58666 ) ;
#93256=CONICAL_SURFACE ( 'NONE', #53675, 4.172000000000001485, 0.9599310885968750373 ) ;
#93258=AXIS2_PLACEMENT_3D ( 'NONE', #40066, #50785, #16863 ) ;
#93280=DIRECTION ( 'NONE',  ( 0.000000000000000000, 0.000000000000000000, 1.000000000000000000 ) ) ;
#93314=DIRECTION ( 'NONE',  ( 0.000000000000000000, 0.000000000000000000, 1.000000000000000000 ) ) ;
#93318=CARTESIAN_POINT ( 'NONE',  ( 18.13561277374696701, 1.340359594676612611E-15, 0.000000000000000000 ) ) ;
#93349=CARTESIAN_POINT ( 'NONE',  ( 44.46823338009918558, 5.000000000000003553, 0.000000000000000000 ) ) ;
#93394=DIRECTION ( 'NONE',  ( 1.000000000000000000, 0.000000000000000000, 0.000000000000000000 ) ) ;
#93412=ORIENTED_EDGE ( 'NONE', *, *, #23726, .T. ) ;
#93421=DIRECTION ( 'NONE',  ( -1.000000000000000000, -0.000000000000000000, -0.000000000000000000 ) ) ;
#93429=VECTOR ( 'NONE', #14403, 1000.000000000000000 ) ;
#93443=EDGE_CURVE ( 'NONE', #22430, #6957, #60877, .T. ) ;
#93447=DIRECTION ( 'NONE',  ( -0.7071067811865315855, 8.659560562355127608E-17, -0.7071067811865634489 ) ) ;
#93475=CARTESIAN_POINT ( 'NONE',  ( 26.69900261086841198, 1.482358050883964840E-15, 0.000000000000000000 ) ) ;
#93494=VERTEX_POINT ( 'NONE', #31575 ) ;
#93495=DIRECTION ( 'NONE',  ( -1.000000000000000000, -0.000000000000000000, -0.000000000000000000 ) ) ;
#93510=AXIS2_PLACEMENT_3D ( 'NONE', #82086, #73997, #75051 ) ;
#93540=CARTESIAN_POINT ( 'NONE',  ( 27.02022815836235026, 1.340359594676612611E-15, 0.000000000000000000 ) ) ;
#93606=DIRECTION ( 'NONE',  ( 1.000000000000000000, 0.000000000000000000, -0.000000000000000000 ) ) ;
#93629=EDGE_CURVE ( 'NONE', #103302, #52464, #79585, .T. ) ;
#93691=EDGE_CURVE ( 'NONE', #36720, #16452, #98583, .T. ) ;
#93692=DIRECTION ( 'NONE',  ( -1.000000000000000000, -1.224606353822377258E-16, -0.000000000000000000 ) ) ;
#93741=CARTESIAN_POINT ( 'NONE',  ( 22.25669491856071858, -5.000000000000000888, 6.123233995736769241E-16 ) ) ;
#93742=VERTEX_POINT ( 'NONE', #3434 ) ;
#93767=CARTESIAN_POINT ( 'NONE',  ( 0.000000000000000000, 0.000000000000000000, 5.000000000000002665 ) ) ;
#93833=CARTESIAN_POINT ( 'NONE',  ( 22.57792046605466041, -5.000000000000000000, 0.000000000000000000 ) ) ;
#93835=CARTESIAN_POINT ( 'NONE',  ( 36.48461538461538822, -4.171999999999999709, 0.000000000000000000 ) ) ;
#93841=CIRCLE ( 'NONE', #35362, 5.000000000000002665 ) ;
#93848=DIRECTION ( 'NONE',  ( 0.000000000000000000, -1.000000000000000000, 0.000000000000000000 ) ) ;
#93853=DIRECTION ( 'NONE',  ( 0.000000000000000000, -1.000000000000000000, 0.000000000000000000 ) ) ;
#93881=CARTESIAN_POINT ( 'NONE',  ( 28.17977184163764193, 1.482358050883964840E-15, 0.000000000000000000 ) ) ;
#93920=ADVANCED_FACE ( 'NONE', ( #78902 ), #6600, .T. ) ;
#93945=AXIS2_PLACEMENT_3D ( 'NONE', #88878, #39806, #74276 ) ;
#93952=AXIS2_PLACEMENT_3D ( 'NONE', #53488, #102572, #102026 ) ;
#93974=EDGE_CURVE ( 'NONE', #51590, #7932, #33184, .T. ) ;
#93995=DIRECTION ( 'NONE',  ( 0.000000000000000000, -1.000000000000000000, 0.000000000000000000 ) ) ;
#94003=CIRCLE ( 'NONE', #63060, 5.000000000000002665 ) ;
#94012=DIRECTION ( 'NONE',  ( 1.000000000000000000, 1.224606353822377258E-16, 0.000000000000000000 ) ) ;
#94062=ORIENTED_EDGE ( 'NONE', *, *, #97424, .T. ) ;
#94088=FACE_OUTER_BOUND ( 'NONE', #51057, .T. ) ;
#94161=EDGE_CURVE ( 'NONE', #26151, #29545, #58898, .T. ) ;
#94170=DIRECTION ( 'NONE',  ( -1.000000000000000000, -1.224606353822377258E-16, -0.000000000000000000 ) ) ;
#94186=VERTEX_POINT ( 'NONE', #7132 ) ;
#94196=ORIENTED_EDGE ( 'NONE', *, *, #73604, .T. ) ;
#94199=CARTESIAN_POINT ( 'NONE',  ( 25.53945892759312031, 5.000000000000004441, 6.123233995736770227E-16 ) ) ;
#94211=ORIENTED_EDGE ( 'NONE', *, *, #54219, .T. ) ;
#94213=CARTESIAN_POINT ( 'NONE',  ( 11.89131030317610183, 1.482358050883964840E-15, 0.000000000000000000 ) ) ;
#94229=DIRECTION ( 'NONE',  ( -0.5735764363510512664, 0.8191520442889881348, 1.003171929053520309E-16 ) ) ;
#94260=CARTESIAN_POINT ( 'NONE',  ( 20.19615384615384457, 4.172000000000003261, 5.109226446042759579E-16 ) ) ;
#94272=AXIS2_PLACEMENT_3D ( 'NONE', #55418, #95374, #80230 ) ;
#94278=DIRECTION ( 'NONE',  ( 0.000000000000000000, -1.000000000000000000, 0.000000000000000000 ) ) ;
#94281=DIRECTION ( 'NONE',  ( -1.000000000000000000, -1.224606353822377258E-16, -0.000000000000000000 ) ) ;
#94292=VERTEX_POINT ( 'NONE', #11370 ) ;
#94314=ORIENTED_EDGE ( 'NONE', *, *, #91802, .F. ) ;
#94348=EDGE_CURVE ( 'NONE', #77934, #6808, #102280, .T. ) ;
#94373=CARTESIAN_POINT ( 'NONE',  ( 35.58361799548379167, 1.482358050883964840E-15, 0.000000000000000000 ) ) ;
#94378=AXIS2_PLACEMENT_3D ( 'NONE', #95811, #80132, #94764 ) ;
#94383=DIRECTION ( 'NONE',  ( -1.000000000000000000, -0.000000000000000000, -0.000000000000000000 ) ) ;
#94388=AXIS2_PLACEMENT_3D ( 'NONE', #9083, #81904, #81370 ) ;
#94399=CARTESIAN_POINT ( 'NONE',  ( 32.62207953394533178, 1.482358050883964840E-15, 0.000000000000000000 ) ) ;
#94439=DIRECTION ( 'NONE',  ( -1.000000000000000000, -1.224606353822377258E-16, -0.000000000000000000 ) ) ;
#94440=EDGE_CURVE ( 'NONE', #13812, #95088, #94747, .T. ) ;
#94478=CIRCLE ( 'NONE', #1427, 4.172000000000001485 ) ;
#94489=ORIENTED_EDGE ( 'NONE', *, *, #57976, .T. ) ;
#94500=CONICAL_SURFACE ( 'NONE', #8384, 8.000000000000000000, 1.047197551196600296 ) ;
#94504=DIRECTION ( 'NONE',  ( 1.000000000000000000, 0.000000000000000000, -0.000000000000000000 ) ) ;
#94528=UNCERTAINTY_MEASURE_WITH_UNIT (LENGTH_MEASURE( 1.000000000000000082E-05 ), #73383, 'distance_accuracy_value', 'NONE');
#94534=CONICAL_SURFACE ( 'NONE', #18795, 5.000000000000001776, 0.9599310885968803664 ) ;
#94547=AXIS2_PLACEMENT_3D ( 'NONE', #25244, #58099, #99622 ) ;
#94575=EDGE_CURVE ( 'NONE', #102923, #29452, #29800, .T. ) ;
#94588=AXIS2_PLACEMENT_3D ( 'NONE', #91274, #93394, #34653 ) ;
#94620=CARTESIAN_POINT ( 'NONE',  ( 0.000000000000000000, 0.000000000000000000, 0.000000000000000000 ) ) ;
#94624=AXIS2_PLACEMENT_3D ( 'NONE', #50825, #42753, #28212 ) ;
#94675=CARTESIAN_POINT ( 'NONE',  ( 34.42407431220851066, 1.340359594676612611E-15, 0.000000000000000000 ) ) ;
#94694=CARTESIAN_POINT ( 'NONE',  ( 0.000000000000000000, 0.000000000000000000, 0.000000000000000000 ) ) ;
#94699=ORIENTED_EDGE ( 'NONE', *, *, #40415, .F. ) ;
#94704=CARTESIAN_POINT ( 'NONE',  ( 0.01688885742776976423, -7.321065037175430668, -3.319543390096034052 ) ) ;
#94716=EDGE_LOOP ( 'NONE', ( #81677, #42455, #94211, #1912, #53234 ) ) ;
#94721=DIRECTION ( 'NONE',  ( -0.5735764363510512664, 0.8191520442889881348, 1.003171929053520309E-16 ) ) ;
#94730=CARTESIAN_POINT ( 'NONE',  ( 6.249999999999998224, 4.618802153517004960, 7.999999999999998224 ) ) ;
#94745=EDGE_CURVE ( 'NONE', #60803, #50381, #50387, .T. ) ;
#94747=LINE ( 'NONE', #28428, #14278 ) ;
#94762=DIRECTION ( 'NONE',  ( -1.000000000000000000, -1.224606353822377258E-16, -0.000000000000000000 ) ) ;
#94764=DIRECTION ( 'NONE',  ( 0.000000000000000000, 1.000000000000000000, 0.000000000000000000 ) ) ;
#94767=CARTESIAN_POINT ( 'NONE',  ( 29.66054107240687543, 3.851859888774471706E-31, 5.000000000000001776 ) ) ;
#94779=EDGE_CURVE ( 'NONE', #55395, #35042, #100355, .T. ) ;
#94784=DIRECTION ( 'NONE',  ( 0.000000000000000000, -1.000000000000000000, 0.000000000000000000 ) ) ;
#94801=ORIENTED_EDGE ( 'NONE', *, *, #41743, .F. ) ;
#94814=ORIENTED_EDGE ( 'NONE', *, *, #6750, .T. ) ;
#94820=EDGE_CURVE ( 'NONE', #29485, #25032, #67405, .T. ) ;
#94839=CARTESIAN_POINT ( 'NONE',  ( 35.90484354297773706, 5.000000000000004441, 6.123233995736770227E-16 ) ) ;
#94851=EDGE_LOOP ( 'NONE', ( #33330, #15730, #37958, #86326, #48083 ) ) ;
#94860=AXIS2_PLACEMENT_3D ( 'NONE', #54892, #39804, #71612 ) ;
#94889=DIRECTION ( 'NONE',  ( 0.000000000000000000, -1.000000000000000000, 0.000000000000000000 ) ) ;
#94923=AXIS2_PLACEMENT_3D ( 'NONE', #20562, #29169, #70105 ) ;
#94929=VECTOR ( 'NONE', #91019, 1000.000000000000000 ) ;
#94938=CARTESIAN_POINT ( 'NONE',  ( 27.59999999999999787, 1.411358822780289120E-15, 0.000000000000000000 ) ) ;
#94959=EDGE_CURVE ( 'NONE', #36949, #94292, #95296, .T. ) ;
#94977=CARTESIAN_POINT ( 'NONE',  ( 39.44615384615384812, 1.411358822780289120E-15, 0.000000000000000000 ) ) ;
#95014=VECTOR ( 'NONE', #18922, 1000.000000000000000 ) ;
#95028=ORIENTED_EDGE ( 'NONE', *, *, #28448, .F. ) ;
#95034=ADVANCED_FACE ( 'NONE', ( #100808 ), #43622, .T. ) ;
#95046=CIRCLE ( 'NONE', #2007, 5.000000000000002665 ) ;
#95073=CARTESIAN_POINT ( 'NONE',  ( 40.92692307692308162, 4.172000000000003261, 0.000000000000000000 ) ) ;
#95088=VERTEX_POINT ( 'NONE', #38759 ) ;
#95105=CARTESIAN_POINT ( 'NONE',  ( 35.58361799548379167, -5.000000000000000888, 6.123233995736769241E-16 ) ) ;
#95123=VECTOR ( 'NONE', #93421, 1000.000000000000000 ) ;
#95125=AXIS2_PLACEMENT_3D ( 'NONE', #16329, #75082, #7697 ) ;
#95175=ORIENTED_EDGE ( 'NONE', *, *, #45199, .T. ) ;
#95181=CARTESIAN_POINT ( 'NONE',  ( 10.41054107240687188, 5.000000000000003553, 0.000000000000000000 ) ) ;
#95227=ORIENTED_EDGE ( 'NONE', *, *, #2307, .F. ) ;
#95233=ORIENTED_EDGE ( 'NONE', *, *, #34496, .F. ) ;
#95280=ORIENTED_EDGE ( 'NONE', *, *, #14830, .T. ) ;
#95296=CIRCLE ( 'NONE', #12589, 4.172000000000001485 ) ;
#95309=EDGE_LOOP ( 'NONE', ( #50150, #77254 ) ) ;
#95321=ORIENTED_EDGE ( 'NONE', *, *, #14582, .F. ) ;
#95368=VERTEX_POINT ( 'NONE', #48675 ) ;
#95374=DIRECTION ( 'NONE',  ( -1.000000000000000000, -1.224606353822377258E-16, -0.000000000000000000 ) ) ;
#95404=CARTESIAN_POINT ( 'NONE',  ( 0.7145311798163270778, 9.237604307034018802, 2.885982852862873934E-16 ) ) ;
#95409=EDGE_CURVE ( 'NONE', #22420, #73528, #26492, .T. ) ;
#95431=AXIS2_PLACEMENT_3D ( 'NONE', #42718, #11393, #75612 ) ;
#95452=ORIENTED_EDGE ( 'NONE', *, *, #57569, .F. ) ;
#95466=ORIENTED_EDGE ( 'NONE', *, *, #21865, .F. ) ;
#95470=CIRCLE ( 'NONE', #79986, 5.000000000000001776 ) ;
#95471=APPLICATION_CONTEXT ( 'automotive_design' ) ;
#95495=ORIENTED_EDGE ( 'NONE', *, *, #86848, .F. ) ;
#95498=DIRECTION ( 'NONE',  ( -1.000000000000000000, -1.224606353822377258E-16, -0.000000000000000000 ) ) ;
#95499=DIRECTION ( 'NONE',  ( -1.000000000000000000, -1.224606353822377258E-16, -0.000000000000000000 ) ) ;
#95530=VERTEX_POINT ( 'NONE', #100959 ) ;
#95540=VECTOR ( 'NONE', #87817, 1000.000000000000227 ) ;
#95544=EDGE_CURVE ( 'NONE', #56015, #96494, #19567, .T. ) ;
#95604=ORIENTED_EDGE ( 'NONE', *, *, #64618, .T. ) ;
#95619=ORIENTED_EDGE ( 'NONE', *, *, #70232, .T. ) ;
#95640=EDGE_LOOP ( 'NONE', ( #67674, #51103, #84688, #85089, #54985 ) ) ;
#95643=DIRECTION ( 'NONE',  ( 0.5735764363510468256, 0.8191520442889913545, 0.000000000000000000 ) ) ;
#95649=VERTEX_POINT ( 'NONE', #33464 ) ;
#95651=ORIENTED_EDGE ( 'NONE', *, *, #23726, .F. ) ;
#95724=DIRECTION ( 'NONE',  ( -1.000000000000000000, -1.224606353822377258E-16, -0.000000000000000000 ) ) ;
#95754=EDGE_CURVE ( 'NONE', #24684, #73958, #91693, .T. ) ;
#95776=AXIS2_PLACEMENT_3D ( 'NONE', #27924, #85596, #60790 ) ;
#95777=ORIENTED_EDGE ( 'NONE', *, *, #77722, .T. ) ;
#95782=CIRCLE ( 'NONE', #57617, 5.000000000000001776 ) ;
#95786=ORIENTED_EDGE ( 'NONE', *, *, #29786, .F. ) ;
#95811=CARTESIAN_POINT ( 'NONE',  ( 41.50669491856072568, 1.482358050883964840E-15, 0.000000000000000000 ) ) ;
#95821=VERTEX_POINT ( 'NONE', #73351 ) ;
#95837=VERTEX_POINT ( 'NONE', #19968 ) ;
#95841=EDGE_CURVE ( 'NONE', #84725, #51711, #53997, .T. ) ;
#95843=CARTESIAN_POINT ( 'NONE',  ( 14.85284876471456350, 6.123233995736772199E-16, -5.000000000000001776 ) ) ;
#95862=ORIENTED_EDGE ( 'NONE', *, *, #52312, .F. ) ;
#95872=ORIENTED_EDGE ( 'NONE', *, *, #59348, .T. ) ;
#95898=EDGE_CURVE ( 'NONE', #74084, #91139, #21331, .T. ) ;
#96001=CONICAL_SURFACE ( 'NONE', #37450, 4.172000000000001485, 0.9599310885968750373 ) ;
#96009=AXIS2_PLACEMENT_3D ( 'NONE', #42225, #10384, #43301 ) ;
#96026=CARTESIAN_POINT ( 'NONE',  ( 26.11923076923076792, -4.171999999999999709, 0.000000000000000000 ) ) ;
#96028=ORIENTED_EDGE ( 'NONE', *, *, #88113, .T. ) ;
#96029=ORIENTED_EDGE ( 'NONE', *, *, #65294, .F. ) ;
#96056=FACE_OUTER_BOUND ( 'NONE', #31294, .T. ) ;
#96080=CARTESIAN_POINT ( 'NONE',  ( -3.325451350920383131E-15, 6.534749472788146107, 4.681481898397001906 ) ) ;
#96093=DIRECTION ( 'NONE',  ( 0.000000000000000000, -1.000000000000000000, 0.000000000000000000 ) ) ;
#96096=DIRECTION ( 'NONE',  ( 0.000000000000000000, -1.000000000000000000, 0.000000000000000000 ) ) ;
#96101=CIRCLE ( 'NONE', #46149, 5.000000000000001776 ) ;
#96105=DIRECTION ( 'NONE',  ( 1.000000000000000000, 0.000000000000000000, 0.000000000000000000 ) ) ;
#96138=AXIS2_PLACEMENT_3D ( 'NONE', #92752, #91703, #30164 ) ;
#96165=ADVANCED_FACE ( 'NONE', ( #40345 ), #9034, .T. ) ;
#96177=CARTESIAN_POINT ( 'NONE',  ( 14.85284876471456350, 3.851859888774471706E-31, 5.000000000000001776 ) ) ;
#96180=CARTESIAN_POINT ( 'NONE',  ( 22.57792046605466041, 1.340359594676612611E-15, 0.000000000000000000 ) ) ;
#96198=AXIS2_PLACEMENT_3D ( 'NONE', #20055, #53441, #36764 ) ;
#96204=ORIENTED_EDGE ( 'NONE', *, *, #78132, .T. ) ;
#96213=VECTOR ( 'NONE', #530, 1000.000000000000227 ) ;
#96223=CIRCLE ( 'NONE', #2954, 5.000000000000002665 ) ;
#96224=DIRECTION ( 'NONE',  ( -1.000000000000000000, -1.224606353822377258E-16, -0.000000000000000000 ) ) ;
#96244=ADVANCED_FACE ( 'NONE', ( #50947 ), #34825, .T. ) ;
#96250=CARTESIAN_POINT ( 'NONE',  ( 0.08224679563971126761, -6.145890662064649845, 5.355005115540901528 ) ) ;
#96255=EDGE_CURVE ( 'NONE', #85724, #23116, #50417, .T. ) ;
#96266=ORIENTED_EDGE ( 'NONE', *, *, #74293, .T. ) ;
#96296=ORIENTED_EDGE ( 'NONE', *, *, #64504, .F. ) ;
#96298=CARTESIAN_POINT ( 'NONE',  ( 0.1306530452038101031, 7.903938623646867612, 2.309976723937613663 ) ) ;
#96301=EDGE_LOOP ( 'NONE', ( #58716, #50223, #46345, #72535, #89655 ) ) ;
#96322=DIRECTION ( 'NONE',  ( 0.000000000000000000, 0.5000000000000007772, -0.8660254037844381525 ) ) ;
#96340=ORIENTED_EDGE ( 'NONE', *, *, #104047, .F. ) ;
#96369=DIRECTION ( 'NONE',  ( 0.000000000000000000, 1.000000000000000000, 0.000000000000000000 ) ) ;
#96372=CIRCLE ( 'NONE', #43008, 5.000000000000001776 ) ;
#96404=DIRECTION ( 'NONE',  ( 0.5735764363510470476, -0.8191520442889911324, 1.003171929053524007E-16 ) ) ;
#96437=CIRCLE ( 'NONE', #31014, 4.172000000000001485 ) ;
#96441=CARTESIAN_POINT ( 'NONE',  ( 21.67692307692307452, 4.172000000000003261, 5.109226446042759579E-16 ) ) ;
#96446=EDGE_LOOP ( 'NONE', ( #15582, #70443, #100175, #55630, #83700 ) ) ;
#96459=ORIENTED_EDGE ( 'NONE', *, *, #8144, .F. ) ;
#96463=DIRECTION ( 'NONE',  ( 1.000000000000000000, 1.224606353822377258E-16, 0.000000000000000000 ) ) ;
#96464=VERTEX_POINT ( 'NONE', #25956 ) ;
#96474=LINE ( 'NONE', #102431, #60193 ) ;
#96482=DIRECTION ( 'NONE',  ( 0.000000000000000000, 0.000000000000000000, 1.000000000000000000 ) ) ;
#96494=VERTEX_POINT ( 'NONE', #17825 ) ;
#96511=CARTESIAN_POINT ( 'NONE',  ( 37.38561277374697056, -5.000000000000000000, 0.000000000000000000 ) ) ;
#96519=AXIS2_PLACEMENT_3D ( 'NONE', #75287, #8431, #15456 ) ;
#96594=EDGE_CURVE ( 'NONE', #75282, #32993, #98589, .T. ) ;
#96595=DIRECTION ( 'NONE',  ( 0.000000000000000000, -1.000000000000000000, 0.000000000000000000 ) ) ;
#96607=VERTEX_POINT ( 'NONE', #9572 ) ;
#96618=DIRECTION ( 'NONE',  ( -1.000000000000000000, -0.000000000000000000, -0.000000000000000000 ) ) ;
#96623=CIRCLE ( 'NONE', #32898, 8.000000000000000000 ) ;
#96640=CARTESIAN_POINT ( 'NONE',  ( 41.82792046605465686, 6.123233995736770227E-16, -5.000000000000002665 ) ) ;
#96643=AXIS2_PLACEMENT_3D ( 'NONE', #90745, #8751, #83177 ) ;
#96688=AXIS2_PLACEMENT_3D ( 'NONE', #41786, #8353, #83306 ) ;
#96699=CARTESIAN_POINT ( 'NONE',  ( 0.000000000000000000, -6.928203230275503444, 4.000000000000010658 ) ) ;
#96704=ORIENTED_EDGE ( 'NONE', *, *, #44073, .T. ) ;
#96757=DIRECTION ( 'NONE',  ( -1.000000000000000000, -1.224606353822377258E-16, -0.000000000000000000 ) ) ;
#96773=EDGE_CURVE ( 'NONE', #52464, #85320, #49317, .T. ) ;
#96794=CARTESIAN_POINT ( 'NONE',  ( 36.48461538461538822, -4.171999999999999709, 5.616230220889763424E-16 ) ) ;
#96826=CARTESIAN_POINT ( 'NONE',  ( 16.33361799548379523, 1.482358050883964840E-15, 0.000000000000000000 ) ) ;
#96853=EDGE_LOOP ( 'NONE', ( #55411, #61512, #98654, #56318, #84417, #35962 ) ) ;
#96859=ORIENTED_EDGE ( 'NONE', *, *, #72149, .T. ) ;
#96864=ORIENTED_EDGE ( 'NONE', *, *, #63933, .T. ) ;
#96885=ADVANCED_FACE ( 'NONE', ( #83819 ), #45322, .T. ) ;
#96896=CARTESIAN_POINT ( 'NONE',  ( 27.59999999999999787, -4.171999999999999709, 0.000000000000000000 ) ) ;
#96901=VERTEX_POINT ( 'NONE', #75186 ) ;
#96906=DIRECTION ( 'NONE',  ( 0.000000000000000000, 1.000000000000000000, 0.000000000000000000 ) ) ;
#96952=CARTESIAN_POINT ( 'NONE',  ( 0.01678220609565910307, 0.7854258609844483319, 8.000000000000001776 ) ) ;
#96954=EDGE_CURVE ( 'NONE', #20871, #55395, #96977, .T. ) ;
#96977=CIRCLE ( 'NONE', #33240, 5.000000000000001776 ) ;
#96997=FACE_OUTER_BOUND ( 'NONE', #51364, .T. ) ;
#97111=ORIENTED_EDGE ( 'NONE', *, *, #59439, .T. ) ;
#97117=CARTESIAN_POINT ( 'NONE',  ( 25.21823338009918203, 6.123233995736772199E-16, -5.000000000000001776 ) ) ;
#97131=VERTEX_POINT ( 'NONE', #2372 ) ;
#97135=LINE ( 'NONE', #80949, #70501 ) ;
#97146=COLOUR_RGB ( '', 0.31764706, 0.68627451, 0.89019608) ;
#97152=ORIENTED_EDGE ( 'NONE', *, *, #103239, .F. ) ;
#97176=EDGE_CURVE ( 'NONE', #90464, #19124, #14340, .T. ) ;
#97192=DIRECTION ( 'NONE',  ( 0.000000000000000000, -1.000000000000000000, 0.000000000000000000 ) ) ;
#97196=ORIENTED_EDGE ( 'NONE', *, *, #1768, .F. ) ;
#97209=DIRECTION ( 'NONE',  ( 0.000000000000000000, -1.000000000000000000, 0.000000000000000000 ) ) ;
#97227=LINE ( 'NONE', #56214, #103573 ) ;
#97265=ORIENTED_EDGE ( 'NONE', *, *, #94348, .T. ) ;
#97273=DIRECTION ( 'NONE',  ( 0.000000000000000000, -1.000000000000000000, 0.000000000000000000 ) ) ;
#97285=ORIENTED_EDGE ( 'NONE', *, *, #88378, .F. ) ;
#97288=AXIS2_PLACEMENT_3D ( 'NONE', #20063, #27083, #59968 ) ;
#97296=ADVANCED_FACE ( 'NONE', ( #70843 ), #27775, .T. ) ;
#97354=EDGE_CURVE ( 'NONE', #7932, #79952, #28188, .T. ) ;
#97397=ORIENTED_EDGE ( 'NONE', *, *, #48658, .T. ) ;
#97401=CARTESIAN_POINT ( 'NONE',  ( 25.21823338009918203, 1.482358050883964840E-15, 0.000000000000000000 ) ) ;
#97420=DIRECTION ( 'NONE',  ( 0.000000000000000000, -1.000000000000000000, 0.000000000000000000 ) ) ;
#97424=EDGE_CURVE ( 'NONE', #16452, #19990, #61168, .T. ) ;
#97526=AXIS2_PLACEMENT_3D ( 'NONE', #23961, #40626, #73512 ) ;
#97528=CARTESIAN_POINT ( 'NONE',  ( 6.249999999999998224, -4.618802153517012954, -8.000000000000001776 ) ) ;
#97541=DIRECTION ( 'NONE',  ( -1.000000000000000000, -1.224606353822377258E-16, -0.000000000000000000 ) ) ;
#97545=ORIENTED_EDGE ( 'NONE', *, *, #34229, .F. ) ;
#97607=AXIS2_PLACEMENT_3D ( 'NONE', #62294, #101281, #61770 ) ;
#97608=CARTESIAN_POINT ( 'NONE',  ( 28.17977184163764193, 1.482358050883964840E-15, 0.000000000000000000 ) ) ;
#97620=DIRECTION ( 'NONE',  ( -1.000000000000000000, -1.224606353822377258E-16, -0.000000000000000000 ) ) ;
#97642=DIRECTION ( 'NONE',  ( 1.000000000000000000, 0.000000000000000000, 0.000000000000000000 ) ) ;
#97650=ORIENTED_EDGE ( 'NONE', *, *, #98100, .F. ) ;
#97655=DIRECTION ( 'NONE',  ( -1.000000000000000000, -0.000000000000000000, -0.000000000000000000 ) ) ;
#97657=ORIENTED_EDGE ( 'NONE', *, *, #52053, .F. ) ;
#97659=EDGE_CURVE ( 'NONE', #101395, #103450, #21405, .T. ) ;
#97683=CIRCLE ( 'NONE', #42572, 5.000000000000001776 ) ;
#97732=CARTESIAN_POINT ( 'NONE',  ( 27.02022815836235026, 6.123233995736770227E-16, -5.000000000000002665 ) ) ;
#97763=VERTEX_POINT ( 'NONE', #19310 ) ;
#97796=DIRECTION ( 'NONE',  ( 0.000000000000000000, -1.000000000000000000, 0.000000000000000000 ) ) ;
#97797=DIRECTION ( 'NONE',  ( -1.000000000000000000, -0.000000000000000000, -0.000000000000000000 ) ) ;
#97842=DIRECTION ( 'NONE',  ( 0.000000000000000000, 0.000000000000000000, 1.000000000000000000 ) ) ;
#97876=DIRECTION ( 'NONE',  ( -0.5735764363510510444, -0.8191520442889883569, 0.000000000000000000 ) ) ;
#97892=VECTOR ( 'NONE', #95643, 999.9999999999998863 ) ;
#97897=CIRCLE ( 'NONE', #77269, 4.172000000000001485 ) ;
#97926=DIRECTION ( 'NONE',  ( 0.5735764363510468256, 0.8191520442889913545, 0.000000000000000000 ) ) ;
#97935=CIRCLE ( 'NONE', #20558, 4.172000000000001485 ) ;
#97959=EDGE_CURVE ( 'NONE', #48048, #29468, #31096, .T. ) ;
#97977=ORIENTED_EDGE ( 'NONE', *, *, #93443, .T. ) ;
#98018=CONICAL_SURFACE ( 'NONE', #6698, 4.172000000000001485, 0.9599310885968750373 ) ;
#98022=DIRECTION ( 'NONE',  ( 0.000000000000000000, -0.5000000000000008882, 0.8660254037844382635 ) ) ;
#98027=CARTESIAN_POINT ( 'NONE',  ( 0.000000000000000000, 6.123233995736770227E-16, -5.000000000000002665 ) ) ;
#98044=ADVANCED_FACE ( 'NONE', ( #105471 ), #31772, .T. ) ;
#98059=CARTESIAN_POINT ( 'NONE',  ( 22.57792046605466041, 0.000000000000000000, 5.000000000000002665 ) ) ;
#98064=CARTESIAN_POINT ( 'NONE',  ( 29.66054107240687543, -5.000000000000000888, 6.123233995736769241E-16 ) ) ;
#98078=VECTOR ( 'NONE', #2987, 1000.000000000000000 ) ;
#98100=EDGE_CURVE ( 'NONE', #36949, #35464, #8763, .T. ) ;
#98119=AXIS2_PLACEMENT_3D ( 'NONE', #103401, #104452, #64027 ) ;
#98120=VERTEX_POINT ( 'NONE', #10353 ) ;
#98191=CARTESIAN_POINT ( 'NONE',  ( 34.10284876471455817, 1.482358050883964840E-15, 0.000000000000000000 ) ) ;
#98225=CIRCLE ( 'NONE', #5242, 5.000000000000001776 ) ;
#98247=CARTESIAN_POINT ( 'NONE',  ( 6.249999999999998224, 9.237604307034018802, 0.000000000000000000 ) ) ;
#98259=AXIS2_PLACEMENT_3D ( 'NONE', #90314, #64978, #16422 ) ;
#98273=DIRECTION ( 'NONE',  ( -1.000000000000000000, -1.224606353822377258E-16, -0.000000000000000000 ) ) ;
#98321=DIRECTION ( 'NONE',  ( 0.000000000000000000, -1.000000000000000000, 0.000000000000000000 ) ) ;
#98355=EDGE_LOOP ( 'NONE', ( #62884, #15362, #96266, #2653, #44843 ) ) ;
#98357=ADVANCED_FACE ( 'NONE', ( #24330 ), #64497, .T. ) ;
#98358=DIRECTION ( 'NONE',  ( 0.000000000000000000, -1.000000000000000000, 0.000000000000000000 ) ) ;
#98368=AXIS2_PLACEMENT_3D ( 'NONE', #90465, #51051, #91547 ) ;
#98391=CARTESIAN_POINT ( 'NONE',  ( -3.476223215531647803E-15, 7.124194613927619990, 3.660532965668822580 ) ) ;
#98409=VECTOR ( 'NONE', #38113, 1000.000000000000000 ) ;
#98411=ORIENTED_EDGE ( 'NONE', *, *, #97176, .F. ) ;
#98432=ORIENTED_EDGE ( 'NONE', *, *, #24112, .F. ) ;
#98438=ORIENTED_EDGE ( 'NONE', *, *, #80293, .F. ) ;
#98446=DIRECTION ( 'NONE',  ( -1.000000000000000000, -1.224606353822377258E-16, -0.000000000000000000 ) ) ;
#98452=CARTESIAN_POINT ( 'NONE',  ( 28.17977184163764193, 1.482358050883964840E-15, 0.000000000000000000 ) ) ;
#98476=ORIENTED_EDGE ( 'NONE', *, *, #24868, .F. ) ;
#98538=CARTESIAN_POINT ( 'NONE',  ( 0.000000000000000000, 1.502314598737159031E-15, -8.000000000000000000 ) ) ;
#98565=CIRCLE ( 'NONE', #5568, 5.000000000000002665 ) ;
#98566=EDGE_CURVE ( 'NONE', #92227, #78717, #831, .T. ) ;
#98583=CIRCLE ( 'NONE', #105455, 4.172000000000001485 ) ;
#98589=LINE ( 'NONE', #99110, #35031 ) ;
#98593=DIRECTION ( 'NONE',  ( 0.000000000000000000, 1.000000000000000000, 0.000000000000000000 ) ) ;
#98602=ADVANCED_FACE ( 'NONE', ( #50662 ), #38779, .T. ) ;
#98623=ORIENTED_EDGE ( 'NONE', *, *, #34689, .T. ) ;
#98651=DIRECTION ( 'NONE',  ( 0.000000000000000000, -1.000000000000000000, 0.000000000000000000 ) ) ;
#98654=ORIENTED_EDGE ( 'NONE', *, *, #74195, .T. ) ;
#98655=VERTEX_POINT ( 'NONE', #27529 ) ;
#98708=ORIENTED_EDGE ( 'NONE', *, *, #15124, .T. ) ;
#98720=LINE ( 'NONE', #24873, #15144 ) ;
#98728=DIRECTION ( 'NONE',  ( -1.000000000000000000, -1.224606353822377258E-16, -0.000000000000000000 ) ) ;
#98742=DIRECTION ( 'NONE',  ( -1.000000000000000000, -0.000000000000000000, -0.000000000000000000 ) ) ;
#98761=VECTOR ( 'NONE', #15479, 1000.000000000000000 ) ;
#98765=VERTEX_POINT ( 'NONE', #53355 ) ;
#98771=EDGE_CURVE ( 'NONE', #1686, #51764, #53347, .T. ) ;
#98813=CARTESIAN_POINT ( 'NONE',  ( 14.27307692307692299, 1.411358822780289120E-15, 0.000000000000000000 ) ) ;
#98828=DIRECTION ( 'NONE',  ( 0.000000000000000000, -1.000000000000000000, 0.000000000000000000 ) ) ;
#98831=CARTESIAN_POINT ( 'NONE',  ( 46.85000000000000142, 0.000000000000000000, 0.000000000000000000 ) ) ;
#98844=VERTEX_POINT ( 'NONE', #81190 ) ;
#98884=ORIENTED_EDGE ( 'NONE', *, *, #65982, .T. ) ;
#98886=ADVANCED_FACE ( 'NONE', ( #90902 ), #14630, .T. ) ;
#98944=ORIENTED_EDGE ( 'NONE', *, *, #1768, .T. ) ;
#98960=DIRECTION ( 'NONE',  ( -0.5735764363510510444, -0.8191520442889883569, 0.000000000000000000 ) ) ;
#98966=VERTEX_POINT ( 'NONE', #52021 ) ;
#98972=DIRECTION ( 'NONE',  ( 0.000000000000000000, -1.000000000000000000, 0.000000000000000000 ) ) ;
#98975=CARTESIAN_POINT ( 'NONE',  ( 19.61638200451619696, 1.340359594676612611E-15, 0.000000000000000000 ) ) ;
#99008=DIRECTION ( 'NONE',  ( 1.000000000000000000, 1.224606353822377258E-16, 0.000000000000000000 ) ) ;
#99017=ORIENTED_EDGE ( 'NONE', *, *, #27110, .F. ) ;
#99038=CARTESIAN_POINT ( 'NONE',  ( 8.349999999999999645, 1.411358822780289120E-15, 0.000000000000000000 ) ) ;
#99045=ORIENTED_EDGE ( 'NONE', *, *, #35630, .F. ) ;
#99046=CIRCLE ( 'NONE', #56231, 5.000000000000001776 ) ;
#99068=LINE ( 'NONE', #58090, #94929 ) ;
#99081=LINE ( 'NONE', #34933, #66981 ) ;
#99101=DIRECTION ( 'NONE',  ( -1.000000000000000000, -1.224606353822377258E-16, -0.000000000000000000 ) ) ;
#99102=AXIS2_PLACEMENT_3D ( 'NONE', #12488, #11421, #45941 ) ;
#99110=CARTESIAN_POINT ( 'NONE',  ( 33.52307692307692122, 4.172000000000003261, 5.109226446042759579E-16 ) ) ;
#99115=CARTESIAN_POINT ( 'NONE',  ( 10.41054107240687188, -5.000000000000000888, 6.123233995736769241E-16 ) ) ;
#99125=AXIS2_PLACEMENT_3D ( 'NONE', #97608, #74925, #90600 ) ;
#99161=CARTESIAN_POINT ( 'NONE',  ( 28.50099738913158376, 1.340359594676612611E-15, 0.000000000000000000 ) ) ;
#99171=ORIENTED_EDGE ( 'NONE', *, *, #17161, .F. ) ;
#99286=AXIS2_PLACEMENT_3D ( 'NONE', #94373, #20535, #98593 ) ;
#99305=DIRECTION ( 'NONE',  ( 0.000000000000000000, -1.000000000000000000, 0.000000000000000000 ) ) ;
#99317=CARTESIAN_POINT ( 'NONE',  ( 0.000000000000000000, 0.000000000000000000, 5.000000000000002665 ) ) ;
#99339=VECTOR ( 'NONE', #102584, 1000.000000000000000 ) ;
#99360=CARTESIAN_POINT ( 'NONE',  ( 24.05868969682389036, 0.000000000000000000, 5.000000000000002665 ) ) ;
#99370=ORIENTED_EDGE ( 'NONE', *, *, #104133, .T. ) ;
#99376=ORIENTED_EDGE ( 'NONE', *, *, #17834, .F. ) ;
#99404=ADVANCED_FACE ( 'NONE', ( #55067 ), #2637, .T. ) ;
#99432=EDGE_CURVE ( 'NONE', #41783, #92227, #62945, .T. ) ;
#99453=CARTESIAN_POINT ( 'NONE',  ( 19.61638200451619696, 1.340359594676612611E-15, 0.000000000000000000 ) ) ;
#99457=CARTESIAN_POINT ( 'NONE',  ( 30.56153846153846132, -4.171999999999999709, 0.000000000000000000 ) ) ;
#99461=ORIENTED_EDGE ( 'NONE', *, *, #2275, .T. ) ;
#99464=VERTEX_POINT ( 'NONE', #4953 ) ;
#99480=EDGE_LOOP ( 'NONE', ( #95466, #54409, #99370, #17774, #88828 ) ) ;
#99514=CARTESIAN_POINT ( 'NONE',  ( 12.79230769230769305, 1.411358822780289120E-15, 0.000000000000000000 ) ) ;
#99555=CIRCLE ( 'NONE', #53079, 4.172000000000001485 ) ;
#99567=ORIENTED_EDGE ( 'NONE', *, *, #5586, .T. ) ;
#99580=AXIS2_PLACEMENT_3D ( 'NONE', #84186, #83111, #42116 ) ;
#99604=FACE_OUTER_BOUND ( 'NONE', #66918, .T. ) ;
#99611=ORIENTED_EDGE ( 'NONE', *, *, #96954, .T. ) ;
#99622=DIRECTION ( 'NONE',  ( 0.000000000000000000, 0.000000000000000000, 1.000000000000000000 ) ) ;
#99626=CIRCLE ( 'NONE', #4943, 5.000000000000002665 ) ;
#99653=FACE_OUTER_BOUND ( 'NONE', #87300, .T. ) ;
#99690=VERTEX_POINT ( 'NONE', #76565 ) ;
#99729=CARTESIAN_POINT ( 'NONE',  ( 9.830769230769229594, 1.411358822780289120E-15, 0.000000000000000000 ) ) ;
#99756=DIRECTION ( 'NONE',  ( -1.000000000000000000, -1.224606353822377258E-16, -0.000000000000000000 ) ) ;
#99764=AXIS2_PLACEMENT_3D ( 'NONE', #73864, #37971, #32378 ) ;
#99813=ORIENTED_EDGE ( 'NONE', *, *, #48765, .F. ) ;
#99817=CARTESIAN_POINT ( 'NONE',  ( 16.33361799548379523, -5.000000000000000888, 6.123233995736769241E-16 ) ) ;
#99819=DIRECTION ( 'NONE',  ( 0.000000000000000000, -1.000000000000000000, 0.000000000000000000 ) ) ;
#99822=DIRECTION ( 'NONE',  ( 0.000000000000000000, -1.000000000000000000, 0.000000000000000000 ) ) ;
#99844=DIRECTION ( 'NONE',  ( -1.000000000000000000, -1.224606353822377258E-16, -0.000000000000000000 ) ) ;
#99863=EDGE_CURVE ( 'NONE', #7084, #74084, #61341, .T. ) ;
#99872=DIRECTION ( 'NONE',  ( 0.000000000000000000, -1.000000000000000000, 0.000000000000000000 ) ) ;
#99927=VERTEX_POINT ( 'NONE', #83476 ) ;
#99994=DIRECTION ( 'NONE',  ( -1.000000000000000000, -0.000000000000000000, -0.000000000000000000 ) ) ;
#100005=DIRECTION ( 'NONE',  ( -1.000000000000000000, -1.224606353822377258E-16, -0.000000000000000000 ) ) ;
#100020=DIRECTION ( 'NONE',  ( 0.000000000000000000, -1.000000000000000000, 0.000000000000000000 ) ) ;
#100032=CONICAL_SURFACE ( 'NONE', #46606, 4.172000000000001485, 0.9599310885968750373 ) ;
#100044=CARTESIAN_POINT ( 'NONE',  ( 0.000000000000000000, 0.000000000000000000, 0.000000000000000000 ) ) ;
#100072=DIRECTION ( 'NONE',  ( 0.000000000000000000, -1.000000000000000000, 0.000000000000000000 ) ) ;
#100075=ORIENTED_EDGE ( 'NONE', *, *, #39111, .T. ) ;
#100123=DIRECTION ( 'NONE',  ( -1.000000000000000000, -0.000000000000000000, -0.000000000000000000 ) ) ;
#100132=CARTESIAN_POINT ( 'NONE',  ( 14.27307692307692299, 1.411358822780289120E-15, 0.000000000000000000 ) ) ;
#100139=ORIENTED_EDGE ( 'NONE', *, *, #89195, .T. ) ;
#100147=ORIENTED_EDGE ( 'NONE', *, *, #71528, .F. ) ;
#100157=EDGE_LOOP ( 'NONE', ( #28414, #26688, #104819, #62675, #25351 ) ) ;
#100163=ORIENTED_EDGE ( 'NONE', *, *, #13664, .F. ) ;
#100175=ORIENTED_EDGE ( 'NONE', *, *, #20829, .T. ) ;
#100229=CARTESIAN_POINT ( 'NONE',  ( 7.770228158362352033, -5.000000000000000000, 0.000000000000000000 ) ) ;
#100270=CARTESIAN_POINT ( 'NONE',  ( 9.250997389131581983, 6.123233995736770227E-16, -5.000000000000002665 ) ) ;
#100292=VECTOR ( 'NONE', #70964, 1000.000000000000227 ) ;
#100300=CARTESIAN_POINT ( 'NONE',  ( 20.19615384615384457, 1.411358822780289120E-15, 0.000000000000000000 ) ) ;
#100306=SHAPE_REPRESENTATION_RELATIONSHIP ( 'NONE' , 'NONE' ,  #44072, #4890 ) ;
#100353=DIRECTION ( 'NONE',  ( 0.5735764363510470476, -0.8191520442889911324, 1.003171929053524007E-16 ) ) ;
#100355=CIRCLE ( 'NONE', #7343, 5.000000000000001776 ) ;
#100360=EDGE_CURVE ( 'NONE', #81401, #96494, #49286, .T. ) ;
#100378=CARTESIAN_POINT ( 'NONE',  ( 45.94900261086841198, 6.123233995736772199E-16, -5.000000000000001776 ) ) ;
#100389=CARTESIAN_POINT ( 'NONE',  ( 6.249999999999998224, -4.618802153516998743, 7.999999999999998224 ) ) ;
#100392=ORIENTED_EDGE ( 'NONE', *, *, #106607, .F. ) ;
#100407=CIRCLE ( 'NONE', #60787, 5.000000000000001776 ) ;
#100409=CIRCLE ( 'NONE', #50505, 5.000000000000002665 ) ;
#100421=DIRECTION ( 'NONE',  ( -1.000000000000000000, -1.224606353822377258E-16, -0.000000000000000000 ) ) ;
#100427=ORIENTED_EDGE ( 'NONE', *, *, #1253, .F. ) ;
#100431=CARTESIAN_POINT ( 'NONE',  ( 0.000000000000000000, 0.000000000000000000, 5.000000000000002665 ) ) ;
#100433=AXIS2_PLACEMENT_3D ( 'NONE', #1827, #17518, #50379 ) ;
#100458=CARTESIAN_POINT ( 'NONE',  ( 0.000000000000000000, 0.000000000000000000, 0.000000000000000000 ) ) ;
#100500=AXIS2_PLACEMENT_3D ( 'NONE', #36547, #94762, #52672 ) ;
#100547=ORIENTED_EDGE ( 'NONE', *, *, #43845, .F. ) ;
#100572=DIRECTION ( 'NONE',  ( 0.000000000000000000, -1.000000000000000000, 0.000000000000000000 ) ) ;
#100580=CARTESIAN_POINT ( 'NONE',  ( 33.52307692307692122, 1.411358822780289120E-15, 0.000000000000000000 ) ) ;
#100581=CARTESIAN_POINT ( 'NONE',  ( 0.000000000000000000, 6.123233995736770227E-16, -5.000000000000002665 ) ) ;
#100609=AXIS2_PLACEMENT_3D ( 'NONE', #10042, #75840, #34888 ) ;
#100668=ORIENTED_EDGE ( 'NONE', *, *, #104609, .T. ) ;
#100674=ORIENTED_EDGE ( 'NONE', *, *, #35352, .F. ) ;
#100694=VECTOR ( 'NONE', #75203, 1000.000000000000227 ) ;
#100737=ORIENTED_EDGE ( 'NONE', *, *, #78028, .T. ) ;
#100761=EDGE_CURVE ( 'NONE', #39668, #77688, #73966, .T. ) ;
#100807=DIRECTION ( 'NONE',  ( 0.000000000000000000, -1.000000000000000000, 0.000000000000000000 ) ) ;
#100808=FACE_OUTER_BOUND ( 'NONE', #20883, .T. ) ;
#100824=DIRECTION ( 'NONE',  ( 0.000000000000000000, -1.000000000000000000, 0.000000000000000000 ) ) ;
#100830=( LENGTH_UNIT ( ) NAMED_UNIT ( * ) SI_UNIT ( .MILLI., .METRE. ) );
#100849=LINE ( 'NONE', #93835, #95014 ) ;
#100852=EDGE_CURVE ( 'NONE', #47541, #8878, #23738, .T. ) ;
#100854=CIRCLE ( 'NONE', #54333, 5.000000000000002665 ) ;
#100859=CARTESIAN_POINT ( 'NONE',  ( 0.000000000000000000, 0.000000000000000000, 0.000000000000000000 ) ) ;
#100885=CARTESIAN_POINT ( 'NONE',  ( 34.10284876471455817, 1.482358050883964840E-15, 0.000000000000000000 ) ) ;
#100904=CARTESIAN_POINT ( 'NONE',  ( 17.81438722625302518, 1.482358050883964840E-15, 0.000000000000000000 ) ) ;
#100941=DIRECTION ( 'NONE',  ( -1.000000000000000000, -1.224606353822377258E-16, -0.000000000000000000 ) ) ;
#100949=CIRCLE ( 'NONE', #13086, 5.000000000000001776 ) ;
#100957=LINE ( 'NONE', #77223, #34325 ) ;
#100959=CARTESIAN_POINT ( 'NONE',  ( 11.31153846153846132, -4.171999999999999709, 5.616230220889763424E-16 ) ) ;
#100969=ORIENTED_EDGE ( 'NONE', *, *, #83668, .T. ) ;
#101010=DIRECTION ( 'NONE',  ( 0.000000000000000000, -1.000000000000000000, 0.000000000000000000 ) ) ;
#101105=CARTESIAN_POINT ( 'NONE',  ( 31.14131030317610538, -5.000000000000000888, 6.123233995736769241E-16 ) ) ;
#101148=DIRECTION ( 'NONE',  ( 0.000000000000000000, -1.000000000000000000, 0.000000000000000000 ) ) ;
#101175=CARTESIAN_POINT ( 'NONE',  ( 25.21823338009918203, 3.851859888774471706E-31, 5.000000000000001776 ) ) ;
#101181=DIRECTION ( 'NONE',  ( -1.000000000000000000, -1.224606353822377258E-16, -0.000000000000000000 ) ) ;
#101189=AXIS2_PLACEMENT_3D ( 'NONE', #33991, #25918, #64858 ) ;
#101199=ORIENTED_EDGE ( 'NONE', *, *, #22161, .F. ) ;
#101201=ORIENTED_EDGE ( 'NONE', *, *, #26863, .T. ) ;
#101233=EDGE_CURVE ( 'NONE', #13709, #72287, #40832, .T. ) ;
#101239=CARTESIAN_POINT ( 'NONE',  ( 0.000000000000000000, 0.000000000000000000, 0.000000000000000000 ) ) ;
#101244=DIRECTION ( 'NONE',  ( 0.000000000000000000, -1.000000000000000000, 0.000000000000000000 ) ) ;
#101246=AXIS2_PLACEMENT_3D ( 'NONE', #65863, #98742, #90677 ) ;
#101250=AXIS2_PLACEMENT_3D ( 'NONE', #8011, #66800, #90005 ) ;
#101281=DIRECTION ( 'NONE',  ( 1.000000000000000000, 0.000000000000000000, -0.000000000000000000 ) ) ;
#101291=ADVANCED_FACE ( 'NONE', ( #21001 ), #18460, .T. ) ;
#101324=CARTESIAN_POINT ( 'NONE',  ( 16.65484354297773351, 6.123233995736770227E-16, -5.000000000000002665 ) ) ;
#101341=ORIENTED_EDGE ( 'NONE', *, *, #94820, .F. ) ;
#101387=CONICAL_SURFACE ( 'NONE', #44587, 5.000000000000001776, 0.9599310885968803664 ) ;
#101395=VERTEX_POINT ( 'NONE', #45647 ) ;
#101399=DIRECTION ( 'NONE',  ( 0.000000000000000000, -1.000000000000000000, 0.000000000000000000 ) ) ;
#101491=CARTESIAN_POINT ( 'NONE',  ( 44.46823338009918558, 3.851859888774471706E-31, 5.000000000000001776 ) ) ;
#101497=CARTESIAN_POINT ( 'NONE',  ( 7.770228158362351145, 1.340359594676612611E-15, 0.000000000000000000 ) ) ;
#101501=DIRECTION ( 'NONE',  ( -0.7071067811865315855, 0.000000000000000000, 0.7071067811865634489 ) ) ;
#101518=CIRCLE ( 'NONE', #58481, 8.000000000000000000 ) ;
#101544=EDGE_CURVE ( 'NONE', #96494, #81401, #52925, .T. ) ;
#101589=ORIENTED_EDGE ( 'NONE', *, *, #13782, .F. ) ;
#101614=ORIENTED_EDGE ( 'NONE', *, *, #17456, .T. ) ;
#101624=AXIS2_PLACEMENT_3D ( 'NONE', #11554, #101651, #54659 ) ;
#101633=ORIENTED_EDGE ( 'NONE', *, *, #42908, .F. ) ;
#101651=DIRECTION ( 'NONE',  ( -1.000000000000000000, -1.224606353822377258E-16, -0.000000000000000000 ) ) ;
#101662=AXIS2_PLACEMENT_3D ( 'NONE', #4410, #94504, #12485 ) ;
#101665=CIRCLE ( 'NONE', #87885, 5.000000000000002665 ) ;
#101684=DIRECTION ( 'NONE',  ( -1.000000000000000000, -1.224606353822377258E-16, -0.000000000000000000 ) ) ;
#101685=CARTESIAN_POINT ( 'NONE',  ( 14.27307692307692299, 1.411358822780289120E-15, 0.000000000000000000 ) ) ;
#101702=DIRECTION ( 'NONE',  ( 0.000000000000000000, 0.000000000000000000, 1.000000000000000000 ) ) ;
#101737=ORIENTED_EDGE ( 'NONE', *, *, #78742, .T. ) ;
#101776=DIRECTION ( 'NONE',  ( -1.000000000000000000, -0.000000000000000000, -0.000000000000000000 ) ) ;
#101790=DIRECTION ( 'NONE',  ( 0.5735764363510468256, 0.8191520442889913545, 0.000000000000000000 ) ) ;
#101827=DIRECTION ( 'NONE',  ( -1.000000000000000000, -1.224606353822377258E-16, -0.000000000000000000 ) ) ;
#101830=VECTOR ( 'NONE', #89513, 999.9999999999998863 ) ;
#101841=LINE ( 'NONE', #3154, #5198 ) ;
#101898=CARTESIAN_POINT ( 'NONE',  ( 19.29515645702225868, 1.482358050883964840E-15, 0.000000000000000000 ) ) ;
#101901=VECTOR ( 'NONE', #10804, 999.9999999999998863 ) ;
#101966=ORIENTED_EDGE ( 'NONE', *, *, #899, .T. ) ;
#101986=FACE_OUTER_BOUND ( 'NONE', #96853, .T. ) ;
#102017=CARTESIAN_POINT ( 'NONE',  ( 45.36923076923077502, 1.411358822780289120E-15, 0.000000000000000000 ) ) ;
#102026=DIRECTION ( 'NONE',  ( 0.000000000000000000, -1.000000000000000000, 0.000000000000000000 ) ) ;
#102067=EDGE_CURVE ( 'NONE', #99464, #23643, #38758, .T. ) ;
#102091=FACE_OUTER_BOUND ( 'NONE', #45291, .T. ) ;
#102093=DIRECTION ( 'NONE',  ( 0.000000000000000000, 0.000000000000000000, 1.000000000000000000 ) ) ;
#102110=FACE_OUTER_BOUND ( 'NONE', #47885, .T. ) ;
#102149=ORIENTED_EDGE ( 'NONE', *, *, #22873, .T. ) ;
#102154=CARTESIAN_POINT ( 'NONE',  ( 29.66054107240687543, 1.482358050883964840E-15, 0.000000000000000000 ) ) ;
#102173=DIRECTION ( 'NONE',  ( 0.000000000000000000, 0.000000000000000000, 1.000000000000000000 ) ) ;
#102184=EDGE_CURVE ( 'NONE', #21850, #23846, #19245, .T. ) ;
#102190=ADVANCED_FACE ( 'NONE', ( #78480 ), #4073, .T. ) ;
#102280=LINE ( 'NONE', #21396, #5670 ) ;
#102312=LINE ( 'NONE', #4157, #11192 ) ;
#102322=PLANE ( 'NONE',  #89051 ) ;
#102333=EDGE_CURVE ( 'NONE', #33830, #54910, #54669, .T. ) ;
#102337=EDGE_CURVE ( 'NONE', #71240, #75630, #8181, .T. ) ;
#102353=VECTOR ( 'NONE', #10873, 1000.000000000000227 ) ;
#102395=DIRECTION ( 'NONE',  ( -1.000000000000000000, -1.224606353822377258E-16, -0.000000000000000000 ) ) ;
#102431=CARTESIAN_POINT ( 'NONE',  ( 6.249999999999998224, 4.618802153517001408, -8.000000000000000000 ) ) ;
#102434=ADVANCED_FACE ( 'NONE', ( #6742 ), #70520, .T. ) ;
#102446=DIRECTION ( 'NONE',  ( 1.000000000000000000, 1.224606353822377258E-16, 0.000000000000000000 ) ) ;
#102488=CIRCLE ( 'NONE', #16326, 5.000000000000002665 ) ;
#102563=LINE ( 'NONE', #43787, #49762 ) ;
#102568=EDGE_CURVE ( 'NONE', #93742, #32720, #81669, .T. ) ;
#102572=DIRECTION ( 'NONE',  ( -1.000000000000000000, -1.224606353822377258E-16, -0.000000000000000000 ) ) ;
#102580=FACE_OUTER_BOUND ( 'NONE', #72770, .T. ) ;
#102584=DIRECTION ( 'NONE',  ( -0.5735764363510510444, -0.8191520442889883569, 0.000000000000000000 ) ) ;
#102632=AXIS2_PLACEMENT_3D ( 'NONE', #7087, #39999, #72873 ) ;
#102636=ORIENTED_EDGE ( 'NONE', *, *, #77466, .F. ) ;
#102644=CONICAL_SURFACE ( 'NONE', #57811, 4.171999999999999709, 0.7853981633974708165 ) ;
#102689=CYLINDRICAL_SURFACE ( 'NONE', #25331, 5.000000000000002665 ) ;
#102724=ORIENTED_EDGE ( 'NONE', *, *, #41088, .F. ) ;
#102732=DIRECTION ( 'NONE',  ( 0.000000000000000000, 1.000000000000000000, 0.000000000000000000 ) ) ;
#102744=EDGE_CURVE ( 'NONE', #48691, #87871, #61919, .T. ) ;
#102746=CARTESIAN_POINT ( 'NONE',  ( 25.53945892759312031, 0.000000000000000000, 5.000000000000002665 ) ) ;
#102763=ORIENTED_EDGE ( 'NONE', *, *, #8754, .T. ) ;
#102793=DIRECTION ( 'NONE',  ( 0.000000000000000000, 0.000000000000000000, 1.000000000000000000 ) ) ;
#102805=ORIENTED_EDGE ( 'NONE', *, *, #47328, .F. ) ;
#102819=EDGE_CURVE ( 'NONE', #44784, #25785, #18893, .T. ) ;
#102824=CONICAL_SURFACE ( 'NONE', #104494, 4.172000000000001485, 0.9599310885968750373 ) ;
#102825=DIRECTION ( 'NONE',  ( -1.000000000000000000, -0.000000000000000000, -0.000000000000000000 ) ) ;
#102856=DIRECTION ( 'NONE',  ( -1.000000000000000000, -1.224606353822377258E-16, -0.000000000000000000 ) ) ;
#102857=CYLINDRICAL_SURFACE ( 'NONE', #91265, 5.000000000000002665 ) ;
#102861=AXIS2_PLACEMENT_3D ( 'NONE', #6104, #71911, #23387 ) ;
#102896=ORIENTED_EDGE ( 'NONE', *, *, #98566, .F. ) ;
#102923=VERTEX_POINT ( 'NONE', #100270 ) ;
#102924=EDGE_CURVE ( 'NONE', #47940, #6569, #93248, .T. ) ;
#102948=EDGE_CURVE ( 'NONE', #7097, #63004, #13368, .T. ) ;
#102970=CARTESIAN_POINT ( 'NONE',  ( 0.000000000000000000, 6.928203230275505220, -4.000000000000007994 ) ) ;
#102980=CONICAL_SURFACE ( 'NONE', #75401, 5.000000000000001776, 0.9599310885968803664 ) ;
#102989=ORIENTED_EDGE ( 'NONE', *, *, #57168, .F. ) ;
#103039=AXIS2_PLACEMENT_3D ( 'NONE', #48503, #32896, #98651 ) ;
#103040=EDGE_LOOP ( 'NONE', ( #60594, #30018, #89366 ) ) ;
#103046=AXIS2_PLACEMENT_3D ( 'NONE', #52913, #2753, #51299 ) ;
#103053=CARTESIAN_POINT ( 'NONE',  ( 41.82792046605465686, 1.340359594676612611E-15, 0.000000000000000000 ) ) ;
#103076=VECTOR ( 'NONE', #87256, 999.9999999999998863 ) ;
#103092=VECTOR ( 'NONE', #75422, 1000.000000000000000 ) ;
#103133=CARTESIAN_POINT ( 'NONE',  ( 43.88846153846154152, 4.172000000000003261, 0.000000000000000000 ) ) ;
#103147=EDGE_CURVE ( 'NONE', #42028, #20871, #34584, .T. ) ;
#103157=LINE ( 'NONE', #29302, #103092 ) ;
#103167=DIRECTION ( 'NONE',  ( 0.000000000000000000, -1.000000000000000000, 0.000000000000000000 ) ) ;
#103177=CARTESIAN_POINT ( 'NONE',  ( 31.14131030317610538, 1.482358050883964840E-15, 0.000000000000000000 ) ) ;
#103180=CARTESIAN_POINT ( 'NONE',  ( 42.98746414932995208, 5.000000000000002665, 0.000000000000000000 ) ) ;
#103207=ADVANCED_FACE ( 'NONE', ( #47861 ), #73193, .T. ) ;
#103212=DIRECTION ( 'NONE',  ( -1.000000000000000000, -1.224606353822377258E-16, -0.000000000000000000 ) ) ;
#103239=EDGE_CURVE ( 'NONE', #57394, #45889, #87823, .T. ) ;
#103242=VECTOR ( 'NONE', #97876, 1000.000000000000000 ) ;
#103267=CIRCLE ( 'NONE', #89484, 5.000000000000002665 ) ;
#103281=DIRECTION ( 'NONE',  ( -1.000000000000000000, -0.000000000000000000, -0.000000000000000000 ) ) ;
#103302=VERTEX_POINT ( 'NONE', #63554 ) ;
#103304=ADVANCED_FACE ( 'NONE', ( #23100 ), #72433, .T. ) ;
#103322=ORIENTED_EDGE ( 'NONE', *, *, #38723, .F. ) ;
#103325=FACE_OUTER_BOUND ( 'NONE', #73252, .T. ) ;
#103340=LINE ( 'NONE', #104381, #100292 ) ;
#103347=EDGE_CURVE ( 'NONE', #29313, #35464, #62228, .T. ) ;
#103354=LINE ( 'NONE', #70457, #31980 ) ;
#103359=ORIENTED_EDGE ( 'NONE', *, *, #14677, .T. ) ;
#103373=DIRECTION ( 'NONE',  ( 0.000000000000000000, -1.000000000000000000, 0.000000000000000000 ) ) ;
#103388=FACE_OUTER_BOUND ( 'NONE', #48982, .T. ) ;
#103401=CARTESIAN_POINT ( 'NONE',  ( 42.98746414932995208, 1.482358050883964840E-15, 0.000000000000000000 ) ) ;
#103426=CIRCLE ( 'NONE', #89650, 5.000000000000002665 ) ;
#103450=VERTEX_POINT ( 'NONE', #18745 ) ;
#103462=ORIENTED_EDGE ( 'NONE', *, *, #82608, .F. ) ;
#103478=ORIENTED_EDGE ( 'NONE', *, *, #42760, .F. ) ;
#103518=EDGE_CURVE ( 'NONE', #39589, #30622, #99068, .T. ) ;
#103523=EDGE_LOOP ( 'NONE', ( #75734, #67579, #79055, #22892, #54362 ) ) ;
#103534=DIRECTION ( 'NONE',  ( -1.000000000000000000, -0.000000000000000000, -0.000000000000000000 ) ) ;
#103573=VECTOR ( 'NONE', #22852, 1000.000000000000000 ) ;
#103587=ORIENTED_EDGE ( 'NONE', *, *, #81782, .T. ) ;
#103649=CARTESIAN_POINT ( 'NONE',  ( 6.249999999999998224, 0.000000000000000000, 0.000000000000000000 ) ) ;
#103652=EDGE_CURVE ( 'NONE', #9392, #48472, #10518, .T. ) ;
#103665=ADVANCED_FACE ( 'NONE', ( #15385 ), #54771, .T. ) ;
#103668=ADVANCED_FACE ( 'NONE', ( #38120 ), #168, .T. ) ;
#103726=CIRCLE ( 'NONE', #95125, 5.000000000000001776 ) ;
#103735=CARTESIAN_POINT ( 'NONE',  ( 0.000000000000000000, 0.000000000000000000, 0.000000000000000000 ) ) ;
#103738=AXIS2_PLACEMENT_3D ( 'NONE', #85421, #20200, #11505 ) ;
#103743=EDGE_LOOP ( 'NONE', ( #105802, #62204, #9268, #19675, #19146 ) ) ;
#103745=ORIENTED_EDGE ( 'NONE', *, *, #10619, .F. ) ;
#103749=ORIENTED_EDGE ( 'NONE', *, *, #35630, .T. ) ;
#103783=DIRECTION ( 'NONE',  ( 0.5735764363510468256, 0.8191520442889913545, 0.000000000000000000 ) ) ;
#103790=ORIENTED_EDGE ( 'NONE', *, *, #4122, .F. ) ;
#103800=LINE ( 'NONE', #30471, #46550 ) ;
#103816=DIRECTION ( 'NONE',  ( -1.000000000000000000, -1.224606353822377258E-16, -0.000000000000000000 ) ) ;
#103826=EDGE_CURVE ( 'NONE', #13133, #58498, #1843, .T. ) ;
#103835=ORIENTED_EDGE ( 'NONE', *, *, #71011, .T. ) ;
#103862=CARTESIAN_POINT ( 'NONE',  ( 42.40769230769231513, 1.411358822780289120E-15, 0.000000000000000000 ) ) ;
#103917=EDGE_CURVE ( 'NONE', #86142, #28378, #82906, .T. ) ;
#103918=EDGE_LOOP ( 'NONE', ( #18594, #32778, #32195, #23088, #31922, #54168 ) ) ;
#103950=VECTOR ( 'NONE', #14971, 1000.000000000000000 ) ;
#103975=ORIENTED_EDGE ( 'NONE', *, *, #106108, .T. ) ;
#103977=CARTESIAN_POINT ( 'NONE',  ( 12.21253585067004543, 1.340359594676612611E-15, 0.000000000000000000 ) ) ;
#104000=DIRECTION ( 'NONE',  ( 0.000000000000000000, -1.000000000000000000, 0.000000000000000000 ) ) ;
#104030=DIRECTION ( 'NONE',  ( 0.000000000000000000, 1.000000000000000000, 0.000000000000000000 ) ) ;
#104036=CARTESIAN_POINT ( 'NONE',  ( 16.33361799548379523, 1.482358050883964840E-15, 0.000000000000000000 ) ) ;
#104047=EDGE_CURVE ( 'NONE', #52425, #28015, #42613, .T. ) ;
#104056=LINE ( 'NONE', #79783, #49563 ) ;
#104103=CARTESIAN_POINT ( 'NONE',  ( 28.17977184163764193, 3.851859888774471706E-31, 5.000000000000001776 ) ) ;
#104133=EDGE_CURVE ( 'NONE', #53057, #101395, #100849, .T. ) ;
#104159=AXIS2_PLACEMENT_3D ( 'NONE', #66420, #1127, #99305 ) ;
#104168=CARTESIAN_POINT ( 'NONE',  ( 8.349999999999999645, 1.411358822780289120E-15, 0.000000000000000000 ) ) ;
#104174=DIRECTION ( 'NONE',  ( -1.000000000000000000, -1.224606353822377258E-16, -0.000000000000000000 ) ) ;
#104234=DIRECTION ( 'NONE',  ( 0.000000000000000000, 0.000000000000000000, 1.000000000000000000 ) ) ;
#104238=VECTOR ( 'NONE', #27353, 999.9999999999998863 ) ;
#104239=CIRCLE ( 'NONE', #66356, 5.000000000000001776 ) ;
#104254=DIRECTION ( 'NONE',  ( -1.000000000000000000, -1.224606353822377258E-16, -0.000000000000000000 ) ) ;
#104291=ORIENTED_EDGE ( 'NONE', *, *, #60644, .F. ) ;
#104318=CIRCLE ( 'NONE', #28608, 5.000000000000001776 ) ;
#104324=CARTESIAN_POINT ( 'NONE',  ( 13.69330508143927538, 0.000000000000000000, 5.000000000000002665 ) ) ;
#104356=CARTESIAN_POINT ( 'NONE',  ( 0.01688885742776671806, 7.321065037175427115, 3.319543390096037605 ) ) ;
#104370=CIRCLE ( 'NONE', #9657, 5.000000000000002665 ) ;
#104380=VERTEX_POINT ( 'NONE', #99115 ) ;
#104381=CARTESIAN_POINT ( 'NONE',  ( 8.349999999999999645, 4.172000000000003261, 5.109226446042759579E-16 ) ) ;
#104400=CIRCLE ( 'NONE', #6231, 5.000000000000001776 ) ;
#104410=AXIS2_PLACEMENT_3D ( 'NONE', #65801, #99756, #17795 ) ;
#104417=CIRCLE ( 'NONE', #44149, 5.000000000000001776 ) ;
#104452=DIRECTION ( 'NONE',  ( -1.000000000000000000, -1.224606353822377258E-16, -0.000000000000000000 ) ) ;
#104493=LINE ( 'NONE', #88331, #93429 ) ;
#104494=AXIS2_PLACEMENT_3D ( 'NONE', #48221, #103816, #81124 ) ;
#104504=CARTESIAN_POINT ( 'NONE',  ( 0.4988340113715863944, 3.871605243926953488, 8.000000000000000000 ) ) ;
#104513=ORIENTED_EDGE ( 'NONE', *, *, #79892, .F. ) ;
#104557=CARTESIAN_POINT ( 'NONE',  ( 0.000000000000000000, 6.123233995736770227E-16, -5.000000000000002665 ) ) ;
#104578=CIRCLE ( 'NONE', #77106, 5.000000000000001776 ) ;
#104582=ORIENTED_EDGE ( 'NONE', *, *, #57883, .T. ) ;
#104583=CARTESIAN_POINT ( 'NONE',  ( 26.69900261086841198, 1.482358050883964840E-15, 0.000000000000000000 ) ) ;
#104597=ORIENTED_EDGE ( 'NONE', *, *, #59004, .F. ) ;
#104609=EDGE_CURVE ( 'NONE', #48268, #58994, #67187, .T. ) ;
#104612=ORIENTED_EDGE ( 'NONE', *, *, #39428, .F. ) ;
#104620=ORIENTED_EDGE ( 'NONE', *, *, #10161, .F. ) ;
#104669=AXIS2_PLACEMENT_3D ( 'NONE', #21888, #14275, #78488 ) ;
#104672=ORIENTED_EDGE ( 'NONE', *, *, #53359, .T. ) ;
#104698=ORIENTED_EDGE ( 'NONE', *, *, #14487, .T. ) ;
#104706=LINE ( 'NONE', #14088, #3307 ) ;
#104720=VERTEX_POINT ( 'NONE', #17576 ) ;
#104729=CIRCLE ( 'NONE', #39314, 4.172000000000001485 ) ;
#104745=ORIENTED_EDGE ( 'NONE', *, *, #59348, .F. ) ;
#104755=DIRECTION ( 'NONE',  ( 1.000000000000000000, 1.224606353822377258E-16, 0.000000000000000000 ) ) ;
#104763=ORIENTED_EDGE ( 'NONE', *, *, #33671, .F. ) ;
#104764=CARTESIAN_POINT ( 'NONE',  ( 17.81438722625302518, 1.482358050883964840E-15, 0.000000000000000000 ) ) ;
#104770=ORIENTED_EDGE ( 'NONE', *, *, #86740, .T. ) ;
#104771=AXIS2_PLACEMENT_3D ( 'NONE', #92722, #34530, #52256 ) ;
#104778=DIRECTION ( 'NONE',  ( 0.000000000000000000, -1.000000000000000000, 0.000000000000000000 ) ) ;
#104779=AXIS2_PLACEMENT_3D ( 'NONE', #75623, #11946, #2249 ) ;
#104819=ORIENTED_EDGE ( 'NONE', *, *, #74065, .T. ) ;
#104862=EDGE_LOOP ( 'NONE', ( #64117, #81465, #84154, #31325, #44542 ) ) ;
#104874=CONICAL_SURFACE ( 'NONE', #6692, 5.000000000000001776, 0.9599310885968803664 ) ;
#104875=ORIENTED_EDGE ( 'NONE', *, *, #29791, .T. ) ;
#104880=AXIS2_PLACEMENT_3D ( 'NONE', #51848, #42702, #99872 ) ;
#104894=CONICAL_SURFACE ( 'NONE', #15337, 4.172000000000001485, 0.9599310885968750373 ) ;
#104896=LINE ( 'NONE', #6714, #92677 ) ;
#104944=ORIENTED_EDGE ( 'NONE', *, *, #86469, .F. ) ;
#104945=DIRECTION ( 'NONE',  ( 0.000000000000000000, -1.000000000000000000, 0.000000000000000000 ) ) ;
#104948=CIRCLE ( 'NONE', #17094, 5.000000000000001776 ) ;
#104966=ADVANCED_FACE ( 'NONE', ( #667 ), #67351, .T. ) ;
#104980=AXIS2_PLACEMENT_3D ( 'NONE', #103177, #104755, #55644 ) ;
#105005=LINE ( 'NONE', #55881, #47113 ) ;
#105007=DIRECTION ( 'NONE',  ( 0.000000000000000000, 0.000000000000000000, 1.000000000000000000 ) ) ;
#105051=DIRECTION ( 'NONE',  ( -1.000000000000000000, -0.000000000000000000, -0.000000000000000000 ) ) ;
#105054=ORIENTED_EDGE ( 'NONE', *, *, #49072, .F. ) ;
#105077=CARTESIAN_POINT ( 'NONE',  ( 17.23461538461538467, 1.411358822780289120E-15, 0.000000000000000000 ) ) ;
#105079=DIRECTION ( 'NONE',  ( 0.000000000000000000, 1.000000000000000000, 0.000000000000000000 ) ) ;
#105109=CARTESIAN_POINT ( 'NONE',  ( 19.29515645702225868, 1.482358050883964840E-15, 0.000000000000000000 ) ) ;
#105167=DIRECTION ( 'NONE',  ( 0.000000000000000000, 1.000000000000000000, 0.000000000000000000 ) ) ;
#105196=EDGE_CURVE ( 'NONE', #7253, #88567, #40512, .T. ) ;
#105219=CARTESIAN_POINT ( 'NONE',  ( 8.929771841637641927, 1.482358050883964840E-15, 0.000000000000000000 ) ) ;
#105238=CARTESIAN_POINT ( 'NONE',  ( 38.54515645702225868, 1.482358050883964840E-15, 0.000000000000000000 ) ) ;
#105261=CIRCLE ( 'NONE', #88110, 5.000000000000002665 ) ;
#105336=FACE_OUTER_BOUND ( 'NONE', #104862, .T. ) ;
#105372=DIRECTION ( 'NONE',  ( 0.000000000000000000, -1.000000000000000000, 0.000000000000000000 ) ) ;
#105376=AXIS2_PLACEMENT_3D ( 'NONE', #55623, #106306, #16792 ) ;
#105426=EDGE_CURVE ( 'NONE', #70974, #88567, #81105, .T. ) ;
#105427=ORIENTED_EDGE ( 'NONE', *, *, #43770, .F. ) ;
#105434=ADVANCED_FACE ( 'NONE', ( #88290 ), #53633, .T. ) ;
#105445=DIRECTION ( 'NONE',  ( 0.000000000000000000, -1.000000000000000000, 0.000000000000000000 ) ) ;
#105455=AXIS2_PLACEMENT_3D ( 'NONE', #7782, #40688, #65508 ) ;
#105458=CARTESIAN_POINT ( 'NONE',  ( 0.000000000000000000, 0.000000000000000000, 5.000000000000002665 ) ) ;
#105471=FACE_OUTER_BOUND ( 'NONE', #14077, .T. ) ;
#105473=ADVANCED_FACE ( 'NONE', ( #53399 ), #43315, .T. ) ;
#105508=ORIENTED_EDGE ( 'NONE', *, *, #25025, .T. ) ;
#105531=ORIENTED_EDGE ( 'NONE', *, *, #21550, .T. ) ;
#105538=ORIENTED_EDGE ( 'NONE', *, *, #47870, .T. ) ;
#105569=ORIENTED_EDGE ( 'NONE', *, *, #84968, .T. ) ;
#105570=VERTEX_POINT ( 'NONE', #41315 ) ;
#105592=FACE_OUTER_BOUND ( 'NONE', #95309, .T. ) ;
#105597=DIRECTION ( 'NONE',  ( -1.000000000000000000, -0.000000000000000000, -0.000000000000000000 ) ) ;
#105632=LINE ( 'NONE', #38795, #13941 ) ;
#105635=AXIS2_PLACEMENT_3D ( 'NONE', #2096, #54353, #70582 ) ;
#105645=CARTESIAN_POINT ( 'NONE',  ( 16.33361799548379523, 5.000000000000002665, 0.000000000000000000 ) ) ;
#105696=ORIENTED_EDGE ( 'NONE', *, *, #37072, .T. ) ;
#105700=CARTESIAN_POINT ( 'NONE',  ( 27.59999999999999787, 1.411358822780289120E-15, 0.000000000000000000 ) ) ;
#105768=CIRCLE ( 'NONE', #14693, 5.000000000000002665 ) ;
#105802=ORIENTED_EDGE ( 'NONE', *, *, #86276, .F. ) ;
#105814=LINE ( 'NONE', #72904, #34052 ) ;
#105833=CARTESIAN_POINT ( 'NONE',  ( 11.89131030317610183, 5.000000000000002665, 0.000000000000000000 ) ) ;
#105835=CARTESIAN_POINT ( 'NONE',  ( 0.3167204509598374740, -8.479269695850863542, 1.313474075707213640 ) ) ;
#105840=ORIENTED_EDGE ( 'NONE', *, *, #88580, .T. ) ;
#105904=EDGE_CURVE ( 'NONE', #26151, #23846, #34813, .T. ) ;
#105905=AXIS2_PLACEMENT_3D ( 'NONE', #68043, #100941, #20081 ) ;
#105927=ORIENTED_EDGE ( 'NONE', *, *, #9871, .T. ) ;
#105928=AXIS2_PLACEMENT_3D ( 'NONE', #15607, #88457, #14533 ) ;
#105933=CARTESIAN_POINT ( 'NONE',  ( 28.17977184163764193, 6.123233995736772199E-16, -5.000000000000001776 ) ) ;
#105943=CARTESIAN_POINT ( 'NONE',  ( 0.4969600502617519400, 8.860760056385744932, 0.6527133886630308579 ) ) ;
#105971=DIRECTION ( 'NONE',  ( -1.000000000000000000, -1.224606353822377258E-16, -0.000000000000000000 ) ) ;
#105975=ORIENTED_EDGE ( 'NONE', *, *, #9145, .T. ) ;
#105987=CIRCLE ( 'NONE', #105905, 5.000000000000002665 ) ;
#105991=EDGE_CURVE ( 'NONE', #99690, #69241, #24492, .T. ) ;
#106006=DIRECTION ( 'NONE',  ( 1.000000000000000000, 1.224606353822377258E-16, 0.000000000000000000 ) ) ;
#106020=ORIENTED_EDGE ( 'NONE', *, *, #3686, .T. ) ;
#106045=CIRCLE ( 'NONE', #69964, 5.000000000000001776 ) ;
#106072=CIRCLE ( 'NONE', #26907, 5.000000000000001776 ) ;
#106077=ORIENTED_EDGE ( 'NONE', *, *, #82333, .F. ) ;
#106090=CARTESIAN_POINT ( 'NONE',  ( 0.000000000000000000, 0.000000000000000000, 0.000000000000000000 ) ) ;
#106092=CARTESIAN_POINT ( 'NONE',  ( 0.000000000000000000, 0.000000000000000000, 0.000000000000000000 ) ) ;
#106095=ORIENTED_EDGE ( 'NONE', *, *, #58791, .F. ) ;
#106108=EDGE_CURVE ( 'NONE', #40649, #35868, #74329, .T. ) ;
#106154=VERTEX_POINT ( 'NONE', #17871 ) ;
#106158=CARTESIAN_POINT ( 'NONE',  ( 0.000000000000000000, 0.000000000000000000, 0.000000000000000000 ) ) ;
#106160=VERTEX_POINT ( 'NONE', #58308 ) ;
#106201=CARTESIAN_POINT ( 'NONE',  ( 0.7145311798163210826, 4.618802153517001408, -8.000000000000000000 ) ) ;
#106213=EDGE_LOOP ( 'NONE', ( #2069, #65927, #45202, #63742 ) ) ;
#106240=CARTESIAN_POINT ( 'NONE',  ( 26.11923076923076792, 1.411358822780289120E-15, 0.000000000000000000 ) ) ;
#106243=EDGE_CURVE ( 'NONE', #7878, #95368, #83635, .T. ) ;
#106278=DIRECTION ( 'NONE',  ( 0.000000000000000000, 0.000000000000000000, 1.000000000000000000 ) ) ;
#106280=VERTEX_POINT ( 'NONE', #26522 ) ;
#106306=DIRECTION ( 'NONE',  ( -1.000000000000000000, -1.224606353822377258E-16, -0.000000000000000000 ) ) ;
#106310=AXIS2_PLACEMENT_3D ( 'NONE', #31983, #39541, #17787 ) ;
#106317=EDGE_LOOP ( 'NONE', ( #69817, #20325, #76147, #37251, #96296, #52794 ) ) ;
#106347=ORIENTED_EDGE ( 'NONE', *, *, #105426, .F. ) ;
#106362=ORIENTED_EDGE ( 'NONE', *, *, #28208, .F. ) ;
#106393=FACE_OUTER_BOUND ( 'NONE', #25343, .T. ) ;
#106411=FACE_OUTER_BOUND ( 'NONE', #9168, .T. ) ;
#106422=CARTESIAN_POINT ( 'NONE',  ( 0.000000000000000000, -6.928203230275503444, 4.000000000000010658 ) ) ;
#106424=ADVANCED_FACE ( 'NONE', ( #47426 ), #32345, .F. ) ;
#106444=CARTESIAN_POINT ( 'NONE',  ( 14.85284876471456350, 1.482358050883964840E-15, 0.000000000000000000 ) ) ;
#106457=CARTESIAN_POINT ( 'NONE',  ( 18.13561277374696701, -5.000000000000000000, 0.000000000000000000 ) ) ;
#106475=ORIENTED_EDGE ( 'NONE', *, *, #17288, .T. ) ;
#106498=CONICAL_SURFACE ( 'NONE', #60037, 5.000000000000001776, 0.9599310885968803664 ) ;
#106503=DIRECTION ( 'NONE',  ( 0.000000000000000000, -1.000000000000000000, 0.000000000000000000 ) ) ;
#106508=EDGE_LOOP ( 'NONE', ( #59205, #2717, #11150, #12271, #45629 ) ) ;
#106512=DIRECTION ( 'NONE',  ( -1.000000000000000000, -0.000000000000000000, -0.000000000000000000 ) ) ;
#106542=FACE_OUTER_BOUND ( 'NONE', #692, .T. ) ;
#106564=DIRECTION ( 'NONE',  ( 0.000000000000000000, 0.8660254037844379305, -0.5000000000000014433 ) ) ;
#106601=LINE ( 'NONE', #65624, #6655 ) ;
#106607=EDGE_CURVE ( 'NONE', #52182, #87322, #45185, .T. ) ;
#106624=DIRECTION ( 'NONE',  ( -1.000000000000000000, -1.224606353822377258E-16, -0.000000000000000000 ) ) ;
#106626=CARTESIAN_POINT ( 'NONE',  ( 18.13561277374696701, 0.000000000000000000, 5.000000000000002665 ) ) ;
#106655=CARTESIAN_POINT ( 'NONE',  ( 0.000000000000000000, 0.000000000000000000, 0.000000000000000000 ) ) ;
#106696=VERTEX_POINT ( 'NONE', #44140 ) ;
#106709=ORIENTED_EDGE ( 'NONE', *, *, #14362, .F. ) ;
#106720=CARTESIAN_POINT ( 'NONE',  ( 0.000000000000000000, -6.928203230275509661, -3.999999999999999112 ) ) ;
#106735=CIRCLE ( 'NONE', #53333, 5.000000000000001776 ) ;
#106750=EDGE_LOOP ( 'NONE', ( #49878, #95777, #4271, #71821, #33968 ) ) ;
#106753=CIRCLE ( 'NONE', #34514, 5.000000000000001776 ) ;
#106767=EDGE_CURVE ( 'NONE', #39668, #60839, #15469, .T. ) ;
#106770=ORIENTED_EDGE ( 'NONE', *, *, #8287, .T. ) ;
ENDSEC;
END-ISO-10303-21;
